ISO-10303-21;
HEADER;
FILE_DESCRIPTION (('STEP AP214'),
    '1' );
FILE_NAME ('spur gear 1_iso_ISO - Spur gear 3M 40T 20PA 10FW ---S40A75H50L60.0N.step',
    '2026-10-24T07:08:27',
    ( '' ),
    ( '' ),
    'SwSTEP 2.0',
    'SolidWorks 2026',
    '' );
FILE_SCHEMA (( 'AUTOMOTIVE_DESIGN' ));
ENDSEC;

DATA;
#4=EDGE_LOOP ( 'NONE', ( #4761, #14101, #16845, #5340 ) ) ;
#8=CYLINDRICAL_SURFACE ( 'NONE', #267, 56.24900000005625600 ) ;
#12=EDGE_CURVE ( 'NONE', #10921, #8874, #11145, .T. ) ;
#14=DIRECTION ( 'NONE',  ( 0.000000000000000000, 0.000000000000000000, 1.000000000000000000 ) ) ;
#19=VERTEX_POINT ( 'NONE', #12878 ) ;
#20=DIRECTION ( 'NONE',  ( 0.000000000000000000, 0.8910065241883657894, 0.4539904997395510788 ) ) ;
#23=AXIS2_PLACEMENT_3D ( 'NONE', #13268, #7449, #2893 ) ;
#27=ORIENTED_EDGE ( 'NONE', *, *, #4590, .T. ) ;
#28=CARTESIAN_POINT ( 'NONE',  ( 0.000000000000000000, -56.23315539212691050, 1.335003989221430487 ) ) ;
#29=CARTESIAN_POINT ( 'NONE',  ( 10.00000000000000000, 24.33982105418971642, -50.71018745830419050 ) ) ;
#33=LINE ( 'NONE', #10310, #12031 ) ;
#35=CYLINDRICAL_SURFACE ( 'NONE', #9712, 56.24900000005625600 ) ;
#37=CYLINDRICAL_SURFACE ( 'NONE', #14858, 56.24900000005625600 ) ;
#40=ORIENTED_EDGE ( 'NONE', *, *, #3069, .F. ) ;
#45=CARTESIAN_POINT ( 'NONE',  ( 0.000000000000000000, -53.29895248911688554, 18.38754094778222026 ) ) ;
#47=DIRECTION ( 'NONE',  ( 0.000000000000000000, 0.000000000000000000, 1.000000000000000000 ) ) ;
#50=EDGE_CURVE ( 'NONE', #3645, #6188, #5249, .T. ) ;
#51=DIRECTION ( 'NONE',  ( 0.000000000000000000, 0.000000000000000000, 1.000000000000000000 ) ) ;
#56=CARTESIAN_POINT ( 'NONE',  ( -10.00000000000000000, 0.000000000000000000, 0.000000000000000000 ) ) ;
#57=EDGE_CURVE ( 'NONE', #1536, #5010, #18293, .T. ) ;
#58=CARTESIAN_POINT ( 'NONE',  ( 0.000000000000000000, 26.71881558261731016, 49.49802920186233024 ) ) ;
#59=CARTESIAN_POINT ( 'NONE',  ( 10.00000000000000000, 42.79754323328179311, -13.90576474687299680 ) ) ;
#60=ORIENTED_EDGE ( 'NONE', *, *, #8774, .T. ) ;
#64=ORIENTED_EDGE ( 'NONE', *, *, #16565, .T. ) ;
#66=EDGE_CURVE ( 'NONE', #4445, #9928, #18675, .T. ) ;
#67=EDGE_CURVE ( 'NONE', #3123, #6017, #15305, .T. ) ;
#68=DIRECTION ( 'NONE',  ( 0.000000000000000000, 0.9510565162951520879, 0.3090169943749517811 ) ) ;
#78=ORIENTED_EDGE ( 'NONE', *, *, #5790, .T. ) ;
#79=VERTEX_POINT ( 'NONE', #8211 ) ;
#80=DIRECTION ( 'NONE',  ( -1.000000000000000000, 0.000000000000000000, 0.000000000000000000 ) ) ;
#81=CARTESIAN_POINT ( 'NONE',  ( 10.00000000000000000, -16.45250512421895550, 53.92768374110886498 ) ) ;
#88=CIRCLE ( 'NONE', #6774, 2.650000000000001243 ) ;
#90=EDGE_CURVE ( 'NONE', #11121, #10536, #17145, .T. ) ;
#95=CARTESIAN_POINT ( 'NONE',  ( 10.00000000000000000, 57.83923611457319680, 24.97244012287522352 ) ) ;
#97=ORIENTED_EDGE ( 'NONE', *, *, #4908, .F. ) ;
#99=CIRCLE ( 'NONE', #8612, 2.649999999999999467 ) ;
#101=CYLINDRICAL_SURFACE ( 'NONE', #6763, 24.00000000002400213 ) ;
#106=CARTESIAN_POINT ( 'NONE',  ( 10.00000000000000000, 61.47135697633778761, 13.79392154159156725 ) ) ;
#111=EDGE_CURVE ( 'NONE', #13893, #5833, #5452, .T. ) ;
#112=EDGE_CURVE ( 'NONE', #16490, #11963, #8906, .T. ) ;
#113=VECTOR ( 'NONE', #7369, 1000.000000000000000 ) ;
#115=CARTESIAN_POINT ( 'NONE',  ( 0.000000000000000000, 38.81885513160045065, -40.70683587897917022 ) ) ;
#117=EDGE_LOOP ( 'NONE', ( #5102, #5293 ) ) ;
#123=ORIENTED_EDGE ( 'NONE', *, *, #10744, .F. ) ;
#129=ADVANCED_FACE ( 'NONE', ( #1437, #5995, #2963, #8762, #10290, #1707, #8940 ), #14754, .F. ) ;
#130=PRODUCT_CONTEXT ( 'NONE', #17652, 'mechanical' ) ;
#134=CARTESIAN_POINT ( 'NONE',  ( 0.000000000000000000, -18.38754094778278869, 53.29895248911668659 ) ) ;
#136=CARTESIAN_POINT ( 'NONE',  ( 5.000000000000000000, -32.11449294037235802, 54.20017844242499905 ) ) ;
#141=EDGE_CURVE ( 'NONE', #9382, #18009, #4302, .T. ) ;
#145=ORIENTED_EDGE ( 'NONE', *, *, #12203, .T. ) ;
#146=ORIENTED_EDGE ( 'NONE', *, *, #2272, .F. ) ;
#149=DIRECTION ( 'NONE',  ( 0.000000000000000000, 0.000000000000000000, -1.000000000000000000 ) ) ;
#150=ORIENTED_EDGE ( 'NONE', *, *, #4149, .F. ) ;
#151=AXIS2_PLACEMENT_3D ( 'NONE', #17609, #7507, #3331 ) ;
#155=DIRECTION ( 'NONE',  ( -1.000000000000000000, 0.000000000000000000, -0.000000000000000000 ) ) ;
#156=ORIENTED_EDGE ( 'NONE', *, *, #8629, .F. ) ;
#169=CARTESIAN_POINT ( 'NONE',  ( 10.00000000000000000, 10.11537145609457156, -55.33199130079773909 ) ) ;
#170=ADVANCED_FACE ( 'NONE', ( #11899 ), #15915, .T. ) ;
#171=ORIENTED_EDGE ( 'NONE', *, *, #3220, .F. ) ;
#173=AXIS2_PLACEMENT_3D ( 'NONE', #16539, #10357, #10634 ) ;
#175=CIRCLE ( 'NONE', #12635, 2.649999999999999467 ) ;
#182=DIRECTION ( 'NONE',  ( 0.000000000000000000, 0.9876883405951371042, 0.1564344650402347547 ) ) ;
#188=CARTESIAN_POINT ( 'NONE',  ( 10.00000000000000000, -53.89344778774800915, -16.10733642026540480 ) ) ;
#189=FACE_OUTER_BOUND ( 'NONE', #10900, .T. ) ;
#191=DIRECTION ( 'NONE',  ( 0.000000000000000000, 0.000000000000000000, 1.000000000000000000 ) ) ;
#194=AXIS2_PLACEMENT_3D ( 'NONE', #3141, #10184, #17431 ) ;
#197=DIRECTION ( 'NONE',  ( 0.000000000000000000, 0.000000000000000000, 1.000000000000000000 ) ) ;
#201=AXIS2_PLACEMENT_3D ( 'NONE', #1014, #18051, #5099 ) ;
#206=CARTESIAN_POINT ( 'NONE',  ( 10.00000000000000000, 13.79392154159134165, 61.47135697633784446 ) ) ;
#209=CARTESIAN_POINT ( 'NONE',  ( 0.000000000000000000, -26.45033635316118747, 33.75576474687270689 ) ) ;
#210=AXIS2_PLACEMENT_3D ( 'NONE', #17149, #4374, #9896 ) ;
#212=ORIENTED_EDGE ( 'NONE', *, *, #1109, .T. ) ;
#216=VECTOR ( 'NONE', #7709, 1000.000000000000000 ) ;
#218=ORIENTED_EDGE ( 'NONE', *, *, #8699, .T. ) ;
#219=VECTOR ( 'NONE', #13244, 1000.000000000000000 ) ;
#225=CARTESIAN_POINT ( 'NONE',  ( 10.00000000000000000, -39.14194549634336084, -40.58063702438384013 ) ) ;
#229=CARTESIAN_POINT ( 'NONE',  ( 0.000000000000000000, 26.45033635316149301, 36.40576474687247099 ) ) ;
#233=CARTESIAN_POINT ( 'NONE',  ( -10.00000000000000000, 0.000000000000000000, 0.000000000000000000 ) ) ;
#235=EDGE_CURVE ( 'NONE', #17488, #2222, #5868, .T. ) ;
#237=CARTESIAN_POINT ( 'NONE',  ( 10.00000000000000000, -55.51919907100644735, -9.823366686501268319 ) ) ;
#239=ORIENTED_EDGE ( 'NONE', *, *, #9480, .F. ) ;
#246=DIRECTION ( 'NONE',  ( 0.000000000000000000, 0.000000000000000000, 1.000000000000000000 ) ) ;
#247=LINE ( 'NONE', #16244, #12318 ) ;
#249=DIRECTION ( 'NONE',  ( 0.000000000000000000, 0.000000000000000000, 1.000000000000000000 ) ) ;
#261=DIRECTION ( 'NONE',  ( 0.000000000000000000, -0.1564344650402171299, -0.9876883405951399908 ) ) ;
#263=FACE_OUTER_BOUND ( 'NONE', #4095, .T. ) ;
#267=AXIS2_PLACEMENT_3D ( 'NONE', #15816, #9999, #2765 ) ;
#268=VECTOR ( 'NONE', #16945, 1000.000000000000000 ) ;
#269=ADVANCED_FACE ( 'NONE', ( #12188 ), #18082, .T. ) ;
#271=DIRECTION ( 'NONE',  ( -1.000000000000000000, -0.000000000000000000, 0.000000000000000000 ) ) ;
#275=CIRCLE ( 'NONE', #6366, 63.00000000006298961 ) ;
#282=AXIS2_PLACEMENT_3D ( 'NONE', #13219, #16170, #3319 ) ;
#291=EDGE_CURVE ( 'NONE', #7622, #9920, #13522, .T. ) ;
#293=CARTESIAN_POINT ( 'NONE',  ( 0.000000000000000000, 0.000000000000000000, 0.000000000000000000 ) ) ;
#304=DIRECTION ( 'NONE',  ( -1.000000000000000000, 0.000000000000000000, -0.000000000000000000 ) ) ;
#311=CARTESIAN_POINT ( 'NONE',  ( 10.00000000000000000, 33.95787273855309252, -45.00825343884985585 ) ) ;
#313=CARTESIAN_POINT ( 'NONE',  ( 10.00000000000000000, -46.20417134726108088, -32.31183295104820985 ) ) ;
#314=ORIENTED_EDGE ( 'NONE', *, *, #13333, .F. ) ;
#318=AXIS2_PLACEMENT_3D ( 'NONE', #9764, #18617, #15573 ) ;
#319=ORIENTED_EDGE ( 'NONE', *, *, #6313, .F. ) ;
#321=DIRECTION ( 'NONE',  ( -1.000000000000000000, 0.000000000000000000, -0.000000000000000000 ) ) ;
#323=DIRECTION ( 'NONE',  ( -1.000000000000000000, 0.000000000000000000, 0.000000000000000000 ) ) ;
#324=ADVANCED_FACE ( 'NONE', ( #3519 ), #10462, .T. ) ;
#325=CYLINDRICAL_SURFACE ( 'NONE', #2758, 56.24900000005625600 ) ;
#327=DIRECTION ( 'NONE',  ( 1.000000000000000000, 0.000000000000000000, 0.000000000000000000 ) ) ;
#336=CYLINDRICAL_SURFACE ( 'NONE', #2323, 63.00000000006298961 ) ;
#339=CARTESIAN_POINT ( 'NONE',  ( 10.00000000000000000, 39.14194549634364506, 40.58063702438359144 ) ) ;
#345=FACE_OUTER_BOUND ( 'NONE', #959, .T. ) ;
#347=DIRECTION ( 'NONE',  ( -1.000000000000000000, -0.000000000000000000, 0.000000000000000000 ) ) ;
#356=EDGE_LOOP ( 'NONE', ( #2421, #4949, #7612, #4912 ) ) ;
#357=CYLINDRICAL_SURFACE ( 'NONE', #5137, 56.24900000005625600 ) ;
#359=ORIENTED_EDGE ( 'NONE', *, *, #90, .T. ) ;
#360=ORIENTED_EDGE ( 'NONE', *, *, #3516, .T. ) ;
#361=DIRECTION ( 'NONE',  ( 0.000000000000000000, 0.000000000000000000, 1.000000000000000000 ) ) ;
#363=DIRECTION ( 'NONE',  ( 0.000000000000000000, -0.5877852522924801315, 0.8090169943749422332 ) ) ;
#366=VECTOR ( 'NONE', #1757, 1000.000000000000000 ) ;
#369=DIRECTION ( 'NONE',  ( -1.000000000000000000, -0.000000000000000000, -0.000000000000000000 ) ) ;
#370=ORIENTED_EDGE ( 'NONE', *, *, #11687, .F. ) ;
#371=DIRECTION ( 'NONE',  ( 0.000000000000000000, 0.8090169943749444537, 0.5877852522924770229 ) ) ;
#373=DIRECTION ( 'NONE',  ( 0.000000000000000000, 0.000000000000000000, 1.000000000000000000 ) ) ;
#376=EDGE_LOOP ( 'NONE', ( #4569, #16538, #11504, #3822 ) ) ;
#380=VERTEX_POINT ( 'NONE', #571 ) ;
#383=EDGE_CURVE ( 'NONE', #6075, #13137, #5526, .T. ) ;
#384=CIRCLE ( 'NONE', #18634, 24.00000000002399503 ) ;
#385=ORIENTED_EDGE ( 'NONE', *, *, #14014, .F. ) ;
#394=ORIENTED_EDGE ( 'NONE', *, *, #4067, .T. ) ;
#396=EDGE_CURVE ( 'NONE', #5722, #407, #9783, .T. ) ;
#404=AXIS2_PLACEMENT_3D ( 'NONE', #6381, #13801, #4663 ) ;
#407=VERTEX_POINT ( 'NONE', #17057 ) ;
#411=DIRECTION ( 'NONE',  ( 0.000000000000000000, 0.000000000000000000, -1.000000000000000000 ) ) ;
#412=AXIS2_PLACEMENT_3D ( 'NONE', #11583, #15864, #4156 ) ;
#417=VERTEX_POINT ( 'NONE', #3999 ) ;
#418=DIRECTION ( 'NONE',  ( 0.000000000000000000, 0.000000000000000000, 1.000000000000000000 ) ) ;
#428=VECTOR ( 'NONE', #12992, 1000.000000000000000 ) ;
#429=DIRECTION ( 'NONE',  ( 1.000000000000000000, 0.000000000000000000, 0.000000000000000000 ) ) ;
#431=DIRECTION ( 'NONE',  ( 0.000000000000000000, 0.000000000000000000, 1.000000000000000000 ) ) ;
#442=ORIENTED_EDGE ( 'NONE', *, *, #7354, .T. ) ;
#445=VERTEX_POINT ( 'NONE', #2658 ) ;
#449=LINE ( 'NONE', #1790, #13535 ) ;
#450=VECTOR ( 'NONE', #13418, 1000.000000000000000 ) ;
#451=VERTEX_POINT ( 'NONE', #957 ) ;
#452=EDGE_LOOP ( 'NONE', ( #14640, #10438, #12655, #9702 ) ) ;
#454=CYLINDRICAL_SURFACE ( 'NONE', #8359, 24.00000000002399503 ) ;
#455=DIRECTION ( 'NONE',  ( 0.000000000000000000, 0.000000000000000000, 1.000000000000000000 ) ) ;
#456=EDGE_CURVE ( 'NONE', #1332, #4270, #14353, .T. ) ;
#465=EDGE_CURVE ( 'NONE', #13362, #5083, #18469, .T. ) ;
#467=CIRCLE ( 'NONE', #2900, 63.00000000006298961 ) ;
#471=CIRCLE ( 'NONE', #1989, 63.00000000006298961 ) ;
#474=AXIS2_PLACEMENT_3D ( 'NONE', #3777, #18252, #9676 ) ;
#475=VERTEX_POINT ( 'NONE', #13899 ) ;
#478=VERTEX_POINT ( 'NONE', #18182 ) ;
#483=CARTESIAN_POINT ( 'NONE',  ( 0.000000000000000000, -58.55669782892479702, 23.24033432160416268 ) ) ;
#484=VERTEX_POINT ( 'NONE', #14087 ) ;
#487=CARTESIAN_POINT ( 'NONE',  ( 10.00000000000000000, 55.83748330407397020, 7.813799127874245798 ) ) ;
#488=ORIENTED_EDGE ( 'NONE', *, *, #10454, .T. ) ;
#489=CIRCLE ( 'NONE', #2924, 2.649999999999999467 ) ;
#490=AXIS2_PLACEMENT_3D ( 'NONE', #8974, #8892, #9173 ) ;
#491=AXIS2_PLACEMENT_3D ( 'NONE', #7155, #9741, #8314 ) ;
#499=CYLINDRICAL_SURFACE ( 'NONE', #6283, 63.00000000006298961 ) ;
#500=ADVANCED_FACE ( 'NONE', ( #12472 ), #2370, .T. ) ;
#503=CIRCLE ( 'NONE', #18134, 63.00000000006298961 ) ;
#504=DIRECTION ( 'NONE',  ( 0.000000000000000000, 0.7071067811865436870, 0.7071067811865513475 ) ) ;
#509=CARTESIAN_POINT ( 'NONE',  ( 10.00000000000000000, 0.000000000000000000, 0.000000000000000000 ) ) ;
#512=ORIENTED_EDGE ( 'NONE', *, *, #112, .F. ) ;
#513=DIRECTION ( 'NONE',  ( 0.000000000000000000, 0.000000000000000000, 1.000000000000000000 ) ) ;
#515=ADVANCED_FACE ( 'NONE', ( #11123 ), #8371, .T. ) ;
#521=ORIENTED_EDGE ( 'NONE', *, *, #9953, .T. ) ;
#524=EDGE_CURVE ( 'NONE', #2625, #7275, #2184, .T. ) ;
#537=VECTOR ( 'NONE', #11015, 1000.000000000000000 ) ;
#538=VERTEX_POINT ( 'NONE', #10338 ) ;
#541=EDGE_CURVE ( 'NONE', #11202, #728, #9483, .T. ) ;
#553=AXIS2_PLACEMENT_3D ( 'NONE', #134, #7279, #17465 ) ;
#556=ORIENTED_EDGE ( 'NONE', *, *, #3480, .T. ) ;
#557=CARTESIAN_POINT ( 'NONE',  ( 0.000000000000000000, -26.71881558261694778, -49.49802920186251498 ) ) ;
#558=CARTESIAN_POINT ( 'NONE',  ( 0.000000000000000000, -13.79392154159090111, -61.47135697633794393 ) ) ;
#559=LINE ( 'NONE', #10649, #2964 ) ;
#562=EDGE_CURVE ( 'NONE', #1723, #7149, #1596, .T. ) ;
#568=CYLINDRICAL_SURFACE ( 'NONE', #2631, 63.00000000006298961 ) ;
#569=ORIENTED_EDGE ( 'NONE', *, *, #13463, .T. ) ;
#571=CARTESIAN_POINT ( 'NONE',  ( 10.00000000000000000, 61.03368945066435458, 15.61693798565518421 ) ) ;
#575=AXIS2_PLACEMENT_3D ( 'NONE', #233, #3180, #513 ) ;
#579=AXIS2_PLACEMENT_3D ( 'NONE', #4765, #8860, #4862 ) ;
#583=DIRECTION ( 'NONE',  ( 0.000000000000000000, 0.000000000000000000, 1.000000000000000000 ) ) ;
#586=DIRECTION ( 'NONE',  ( -1.000000000000000000, 0.000000000000000000, -0.000000000000000000 ) ) ;
#588=CYLINDRICAL_SURFACE ( 'NONE', #9094, 56.24900000005625600 ) ;
#590=AXIS2_PLACEMENT_3D ( 'NONE', #16022, #7347, #5916 ) ;
#593=CIRCLE ( 'NONE', #16724, 63.00000000006298961 ) ;
#595=ORIENTED_EDGE ( 'NONE', *, *, #18213, .F. ) ;
#605=DIRECTION ( 'NONE',  ( 0.000000000000000000, 0.000000000000000000, -1.000000000000000000 ) ) ;
#606=CYLINDRICAL_SURFACE ( 'NONE', #1990, 56.24900000005625600 ) ;
#607=VERTEX_POINT ( 'NONE', #6230 ) ;
#610=DIRECTION ( 'NONE',  ( 0.000000000000000000, 0.000000000000000000, 1.000000000000000000 ) ) ;
#615=EDGE_CURVE ( 'NONE', #3160, #417, #7117, .T. ) ;
#618=CARTESIAN_POINT ( 'NONE',  ( 10.00000000000000000, -13.79392154159089756, -61.47135697633793683 ) ) ;
#619=EDGE_CURVE ( 'NONE', #16309, #3893, #687, .T. ) ;
#620=EDGE_LOOP ( 'NONE', ( #239, #4608, #6454, #6087 ) ) ;
#622=STYLED_ITEM('',(#18869),#9854);
#623=ADVANCED_FACE ( 'NONE', ( #3105 ), #12035, .T. ) ;
#625=DIRECTION ( 'NONE',  ( 0.000000000000000000, 0.000000000000000000, 1.000000000000000000 ) ) ;
#627=CARTESIAN_POINT ( 'NONE',  ( 10.00000000000000000, 62.87238730325621106, -4.007856633823605463 ) ) ;
#629=CARTESIAN_POINT ( 'NONE',  ( -10.00000000000000000, 0.000000000000000000, 0.000000000000000000 ) ) ;
#630=EDGE_CURVE ( 'NONE', #2530, #13928, #2807, .T. ) ;
#632=UNCERTAINTY_MEASURE_WITH_UNIT (LENGTH_MEASURE( 1.000000000000000082E-05 ), #16986, 'distance_accuracy_value', 'NONE');
#638=CARTESIAN_POINT ( 'NONE',  ( 10.00000000000000000, -42.79754323328189969, -13.90576474687263264 ) ) ;
#639=ORIENTED_EDGE ( 'NONE', *, *, #13733, .F. ) ;
#648=EDGE_CURVE ( 'NONE', #13033, #17129, #9085, .T. ) ;
#655=CARTESIAN_POINT ( 'NONE',  ( 0.000000000000000000, -61.03368945066446827, 15.61693798565473656 ) ) ;
#657=VERTEX_POINT ( 'NONE', #4189 ) ;
#658=CARTESIAN_POINT ( 'NONE',  ( 0.000000000000000000, 1.335003989222417697, -56.23315539212688918 ) ) ;
#661=DIRECTION ( 'NONE',  ( 1.000000000000000000, -0.000000000000000000, 0.000000000000000000 ) ) ;
#663=AXIS2_PLACEMENT_3D ( 'NONE', #15792, #17214, #4171 ) ;
#664=CARTESIAN_POINT ( 'NONE',  ( 10.00000000000000000, -31.97297851452457351, 46.27827401617392411 ) ) ;
#665=EDGE_LOOP ( 'NONE', ( #4697, #15423, #2436, #2254 ) ) ;
#668=CIRCLE ( 'NONE', #12855, 24.00000000002400569 ) ;
#669=EDGE_CURVE ( 'NONE', #2958, #2652, #11537, .T. ) ;
#670=ORIENTED_EDGE ( 'NONE', *, *, #3951, .F. ) ;
#675=DIRECTION ( 'NONE',  ( 1.000000000000000000, -0.000000000000000000, 0.000000000000000000 ) ) ;
#679=ORIENTED_EDGE ( 'NONE', *, *, #1431, .F. ) ;
#680=DIRECTION ( 'NONE',  ( 0.000000000000000000, 0.000000000000000000, -1.000000000000000000 ) ) ;
#683=CARTESIAN_POINT ( 'NONE',  ( 0.000000000000000000, 0.000000000000000000, 0.000000000000000000 ) ) ;
#687=CIRCLE ( 'NONE', #9492, 63.00000000006298961 ) ;
#691=AXIS2_PLACEMENT_3D ( 'NONE', #509, #9078, #10601 ) ;
#692=ORIENTED_EDGE ( 'NONE', *, *, #5967, .F. ) ;
#693=DIRECTION ( 'NONE',  ( 1.000000000000000000, 0.000000000000000000, 0.000000000000000000 ) ) ;
#697=CARTESIAN_POINT ( 'NONE',  ( -10.00000000000000000, 0.000000000000000000, 0.000000000000000000 ) ) ;
#699=DIRECTION ( 'NONE',  ( 1.000000000000000000, 0.000000000000000000, 0.000000000000000000 ) ) ;
#701=VERTEX_POINT ( 'NONE', #3192 ) ;
#707=CARTESIAN_POINT ( 'NONE',  ( 10.00000000000000000, -26.49895292618039377, 49.76630880786299826 ) ) ;
#709=ORIENTED_EDGE ( 'NONE', *, *, #3804, .F. ) ;
#711=AXIS2_PLACEMENT_3D ( 'NONE', #11816, #4571, #11718 ) ;
#712=DIRECTION ( 'NONE',  ( 0.000000000000000000, 0.000000000000000000, 1.000000000000000000 ) ) ;
#715=DIRECTION ( 'NONE',  ( 0.000000000000000000, 0.000000000000000000, 1.000000000000000000 ) ) ;
#717=EDGE_CURVE ( 'NONE', #18313, #13820, #6667, .T. ) ;
#719=CARTESIAN_POINT ( 'NONE',  ( 5.000000000000000000, -61.47135697633769524, -13.79392154159199713 ) ) ;
#723=ADVANCED_FACE ( 'NONE', ( #3576 ), #9271, .T. ) ;
#728=VERTEX_POINT ( 'NONE', #12518 ) ;
#729=EDGE_CURVE ( 'NONE', #10240, #1960, #467, .T. ) ;
#730=ADVANCED_FACE ( 'NONE', ( #12316 ), #15275, .T. ) ;
#732=DIRECTION ( 'NONE',  ( -1.000000000000000000, 0.000000000000000000, 0.000000000000000000 ) ) ;
#733=ORIENTED_EDGE ( 'NONE', *, *, #13326, .T. ) ;
#734=EDGE_LOOP ( 'NONE', ( #4079, #5320, #4537, #1238 ) ) ;
#735=DIRECTION ( 'NONE',  ( 0.000000000000000000, -0.5877852522924801315, 0.8090169943749422332 ) ) ;
#739=CARTESIAN_POINT ( 'NONE',  ( -10.00000000000000000, 0.000000000000000000, 0.000000000000000000 ) ) ;
#740=EDGE_CURVE ( 'NONE', #12029, #728, #5327, .T. ) ;
#743=VERTEX_POINT ( 'NONE', #618 ) ;
#747=EDGE_CURVE ( 'NONE', #16326, #1501, #17400, .T. ) ;
#750=CARTESIAN_POINT ( 'NONE',  ( 0.000000000000000000, -62.87238730325623948, 4.007856633823172032 ) ) ;
#755=DIRECTION ( 'NONE',  ( 0.000000000000000000, 0.8910065241883688980, -0.4539904997395446951 ) ) ;
#756=DIRECTION ( 'NONE',  ( 0.000000000000000000, 0.000000000000000000, 1.000000000000000000 ) ) ;
#757=ORIENTED_EDGE ( 'NONE', *, *, #10060, .F. ) ;
#763=DIRECTION ( 'NONE',  ( 0.000000000000000000, 0.000000000000000000, -1.000000000000000000 ) ) ;
#765=AXIS2_PLACEMENT_3D ( 'NONE', #14091, #5531, #7226 ) ;
#767=EDGE_CURVE ( 'NONE', #3669, #4773, #5758, .T. ) ;
#770=DIRECTION ( 'NONE',  ( -1.000000000000000000, 0.000000000000000000, 0.000000000000000000 ) ) ;
#788=ORIENTED_EDGE ( 'NONE', *, *, #9868, .T. ) ;
#789=CARTESIAN_POINT ( 'NONE',  ( 10.00000000000000000, -55.33199130079777461, -10.11537145609435306 ) ) ;
#794=CARTESIAN_POINT ( 'NONE',  ( 0.000000000000000000, -49.76630880786327538, 26.49895292617986797 ) ) ;
#796=AXIS2_PLACEMENT_3D ( 'NONE', #12535, #16739, #5001 ) ;
#798=ORIENTED_EDGE ( 'NONE', *, *, #12607, .T. ) ;
#803=EDGE_CURVE ( 'NONE', #11858, #8925, #7390, .T. ) ;
#805=DIRECTION ( 'NONE',  ( -1.000000000000000000, 0.000000000000000000, 0.000000000000000000 ) ) ;
#810=CIRCLE ( 'NONE', #12974, 24.00000000002399858 ) ;
#812=DIRECTION ( 'NONE',  ( -1.000000000000000000, 0.000000000000000000, 0.000000000000000000 ) ) ;
#815=EDGE_CURVE ( 'NONE', #11178, #15913, #15657, .T. ) ;
#822=ORIENTED_EDGE ( 'NONE', *, *, #2491, .F. ) ;
#827=CARTESIAN_POINT ( 'NONE',  ( 10.00000000000000000, 5.876895005582430720, 62.72529079327808432 ) ) ;
#830=CARTESIAN_POINT ( 'NONE',  ( 0.000000000000000000, 0.000000000000000000, 0.000000000000000000 ) ) ;
#831=CARTESIAN_POINT ( 'NONE',  ( 0.000000000000000000, 54.20017844242556748, -32.11449294037138458 ) ) ;
#838=ORIENTED_EDGE ( 'NONE', *, *, #5277, .F. ) ;
#844=DIRECTION ( 'NONE',  ( -1.000000000000000000, 0.000000000000000000, -0.000000000000000000 ) ) ;
#855=ORIENTED_EDGE ( 'NONE', *, *, #1389, .F. ) ;
#866=ADVANCED_FACE ( 'NONE', ( #11278 ), #4139, .T. ) ;
#869=CIRCLE ( 'NONE', #10578, 24.00000000002400213 ) ;
#871=ADVANCED_FACE ( 'NONE', ( #10038 ), #1003, .T. ) ;
#872=VERTEX_POINT ( 'NONE', #17186 ) ;
#875=DIRECTION ( 'NONE',  ( 0.000000000000000000, 0.5877852522924742473, -0.8090169943749465631 ) ) ;
#876=DIRECTION ( 'NONE',  ( -1.000000000000000000, -0.000000000000000000, -0.000000000000000000 ) ) ;
#878=CARTESIAN_POINT ( 'NONE',  ( 0.000000000000000000, 34.13306034420185853, 44.70888270294173594 ) ) ;
#883=DIRECTION ( 'NONE',  ( 1.000000000000000000, -0.000000000000000000, -0.000000000000000000 ) ) ;
#885=AXIS2_PLACEMENT_3D ( 'NONE', #11911, #4767, #7626 ) ;
#888=CARTESIAN_POINT ( 'NONE',  ( 0.000000000000000000, -39.14194549634393638, 40.58063702438330722 ) ) ;
#889=EDGE_CURVE ( 'NONE', #4270, #8736, #1731, .T. ) ;
#893=ORIENTED_EDGE ( 'NONE', *, *, #17398, .F. ) ;
#894=CIRCLE ( 'NONE', #765, 63.00000000006298961 ) ;
#895=AXIS2_PLACEMENT_3D ( 'NONE', #12553, #12357, #2264 ) ;
#896=EDGE_CURVE ( 'NONE', #9406, #17827, #5654, .T. ) ;
#897=ORIENTED_EDGE ( 'NONE', *, *, #12369, .F. ) ;
#899=FACE_OUTER_BOUND ( 'NONE', #8207, .T. ) ;
#902=CYLINDRICAL_SURFACE ( 'NONE', #8214, 63.00000000006298961 ) ;
#908=ORIENTED_EDGE ( 'NONE', *, *, #630, .T. ) ;
#909=VECTOR ( 'NONE', #15611, 1000.000000000000000 ) ;
#915=DIRECTION ( 'NONE',  ( 0.000000000000000000, 0.000000000000000000, 1.000000000000000000 ) ) ;
#918=AXIS2_PLACEMENT_3D ( 'NONE', #739, #8350, #13974 ) ;
#919=FACE_OUTER_BOUND ( 'NONE', #1318, .T. ) ;
#920=CARTESIAN_POINT ( 'NONE',  ( 0.000000000000000000, 55.74967257055882186, 7.478235706489174461 ) ) ;
#927=LINE ( 'NONE', #5287, #18650 ) ;
#929=AXIS2_PLACEMENT_3D ( 'NONE', #6910, #2336, #1890 ) ;
#938=EDGE_CURVE ( 'NONE', #1081, #872, #7506, .T. ) ;
#943=CIRCLE ( 'NONE', #1542, 30.00000000000000000 ) ;
#946=FACE_OUTER_BOUND ( 'NONE', #13197, .T. ) ;
#951=CARTESIAN_POINT ( 'NONE',  ( 0.000000000000000000, -38.81885513159959800, -40.70683587897998734 ) ) ;
#953=EDGE_LOOP ( 'NONE', ( #7629, #7949, #7760, #5155 ) ) ;
#957=CARTESIAN_POINT ( 'NONE',  ( 0.000000000000000000, -15.61693798565540625, 61.03368945066429774 ) ) ;
#959=EDGE_LOOP ( 'NONE', ( #11211, #1552, #16308, #16327 ) ) ;
#968=CARTESIAN_POINT ( 'NONE',  ( 0.000000000000000000, 42.79754323328179311, -11.25576474687299644 ) ) ;
#971=CARTESIAN_POINT ( 'NONE',  ( 10.00000000000000000, 15.61693798565496749, 61.03368945066440432 ) ) ;
#975=DIRECTION ( 'NONE',  ( -1.000000000000000000, -0.000000000000000000, 0.000000000000000000 ) ) ;
#980=VERTEX_POINT ( 'NONE', #11039 ) ;
#983=CARTESIAN_POINT ( 'NONE',  ( 10.00000000000000000, 0.000000000000000000, 0.000000000000000000 ) ) ;
#985=DIRECTION ( 'NONE',  ( -1.000000000000000000, 0.000000000000000000, -0.000000000000000000 ) ) ;
#986=EDGE_CURVE ( 'NONE', #1108, #15167, #9015, .T. ) ;
#987=LINE ( 'NONE', #4467, #16642 ) ;
#989=CARTESIAN_POINT ( 'NONE',  ( 0.000000000000000000, 48.50907078259439942, -40.19788616105557111 ) ) ;
#993=DIRECTION ( 'NONE',  ( -1.000000000000000000, 0.000000000000000000, -0.000000000000000000 ) ) ;
#997=DIRECTION ( 'NONE',  ( 1.000000000000000000, 0.000000000000000000, 0.000000000000000000 ) ) ;
#1001=EDGE_CURVE ( 'NONE', #1864, #17712, #2279, .T. ) ;
#1003=CYLINDRICAL_SURFACE ( 'NONE', #14209, 56.24900000005625600 ) ;
#1007=CARTESIAN_POINT ( 'NONE',  ( 10.00000000000000000, 0.000000000000000000, 0.000000000000000000 ) ) ;
#1010=CIRCLE ( 'NONE', #18331, 63.00000000006298961 ) ;
#1014=CARTESIAN_POINT ( 'NONE',  ( 0.000000000000000000, 0.000000000000000000, 0.000000000000000000 ) ) ;
#1017=ORIENTED_EDGE ( 'NONE', *, *, #815, .T. ) ;
#1025=DIRECTION ( 'NONE',  ( -1.000000000000000000, -0.000000000000000000, -0.000000000000000000 ) ) ;
#1026=DIRECTION ( 'NONE',  ( -1.000000000000000000, 0.000000000000000000, -0.000000000000000000 ) ) ;
#1028=DIRECTION ( 'NONE',  ( -1.000000000000000000, -0.000000000000000000, -0.000000000000000000 ) ) ;
#1037=AXIS2_PLACEMENT_3D ( 'NONE', #6039, #12130, #16426 ) ;
#1047=ADVANCED_FACE ( 'NONE', ( #3810 ), #12571, .T. ) ;
#1048=ORIENTED_EDGE ( 'NONE', *, *, #7143, .T. ) ;
#1050=CARTESIAN_POINT ( 'NONE',  ( 10.00000000000000000, -5.876895005582881026, 62.72529079327804169 ) ) ;
#1052=CARTESIAN_POINT ( 'NONE',  ( 10.00000000000000000, -9.823366686500245137, -55.51919907100663920 ) ) ;
#1053=FACE_BOUND ( 'NONE', #18533, .T. ) ;
#1054=ADVANCED_FACE ( 'NONE', ( #18092 ), #18374, .T. ) ;
#1055=DIRECTION ( 'NONE',  ( -1.000000000000000000, 0.000000000000000000, 0.000000000000000000 ) ) ;
#1060=CYLINDRICAL_SURFACE ( 'NONE', #7471, 63.00000000006298961 ) ;
#1065=EDGE_LOOP ( 'NONE', ( #3298, #16949, #2745, #15966 ) ) ;
#1066=EDGE_CURVE ( 'NONE', #16979, #9984, #13601, .T. ) ;
#1067=EDGE_LOOP ( 'NONE', ( #18299, #7502, #7090, #2569 ) ) ;
#1077=FACE_OUTER_BOUND ( 'NONE', #3375, .T. ) ;
#1081=VERTEX_POINT ( 'NONE', #13808 ) ;
#1082=CARTESIAN_POINT ( 'NONE',  ( 10.00000000000000000, 0.000000000000000000, 0.000000000000000000 ) ) ;
#1084=CARTESIAN_POINT ( 'NONE',  ( 10.00000000000000000, 0.000000000000000000, 0.000000000000000000 ) ) ;
#1085=CARTESIAN_POINT ( 'NONE',  ( 10.00000000000000000, 57.83923611457354497, -24.97244012287440640 ) ) ;
#1093=AXIS2_PLACEMENT_3D ( 'NONE', #13536, #6293, #8000 ) ;
#1094=EDGE_CURVE ( 'NONE', #9382, #7210, #11467, .T. ) ;
#1099=DIRECTION ( 'NONE',  ( -1.000000000000000000, 0.000000000000000000, 0.000000000000000000 ) ) ;
#1100=CIRCLE ( 'NONE', #7769, 63.00000000006298961 ) ;
#1107=AXIS2_PLACEMENT_3D ( 'NONE', #18507, #18599, #1363 ) ;
#1108=VERTEX_POINT ( 'NONE', #12950 ) ;
#1109=EDGE_CURVE ( 'NONE', #8874, #6557, #18464, .T. ) ;
#1111=CARTESIAN_POINT ( 'NONE',  ( 0.000000000000000000, -24.33982105418865061, -50.71018745830470920 ) ) ;
#1112=DIRECTION ( 'NONE',  ( 1.000000000000000000, -0.000000000000000000, -0.000000000000000000 ) ) ;
#1114=ORIENTED_EDGE ( 'NONE', *, *, #90, .F. ) ;
#1116=CARTESIAN_POINT ( 'NONE',  ( 0.000000000000000000, -24.68609584167124282, -50.69000562871667626 ) ) ;
#1120=EDGE_CURVE ( 'NONE', #3525, #5795, #18757, .T. ) ;
#1129=CARTESIAN_POINT ( 'NONE',  ( 10.00000000000000000, -61.03368945066446116, 15.61693798565474012 ) ) ;
#1130=DIRECTION ( 'NONE',  ( -1.000000000000000000, -0.000000000000000000, 0.000000000000000000 ) ) ;
#1132=CIRCLE ( 'NONE', #8970, 24.00000000002400213 ) ;
#1136=VECTOR ( 'NONE', #675, 1000.000000000000000 ) ;
#1138=CYLINDRICAL_SURFACE ( 'NONE', #11634, 56.24900000005625600 ) ;
#1139=CIRCLE ( 'NONE', #8731, 56.24900000005626310 ) ;
#1141=ORIENTED_EDGE ( 'NONE', *, *, #12608, .F. ) ;
#1142=AXIS2_PLACEMENT_3D ( 'NONE', #6761, #12283, #583 ) ;
#1143=DIRECTION ( 'NONE',  ( -1.000000000000000000, 0.000000000000000000, 0.000000000000000000 ) ) ;
#1145=DIRECTION ( 'NONE',  ( 0.000000000000000000, 0.000000000000000000, 1.000000000000000000 ) ) ;
#1146=DIRECTION ( 'NONE',  ( 0.000000000000000000, -0.4539904997395351471, -0.8910065241883737830 ) ) ;
#1150=VECTOR ( 'NONE', #4790, 1000.000000000000000 ) ;
#1152=VERTEX_POINT ( 'NONE', #10180 ) ;
#1154=DIRECTION ( 'NONE',  ( -1.000000000000000000, -0.000000000000000000, 0.000000000000000000 ) ) ;
#1157=DIRECTION ( 'NONE',  ( -1.000000000000000000, 0.000000000000000000, 0.000000000000000000 ) ) ;
#1158=CARTESIAN_POINT ( 'NONE',  ( 10.00000000000000000, 45.00825343885067298, -33.95787273855199828 ) ) ;
#1168=AXIS2_PLACEMENT_3D ( 'NONE', #4885, #17740, #6311 ) ;
#1171=VERTEX_POINT ( 'NONE', #5806 ) ;
#1172=EDGE_CURVE ( 'NONE', #8441, #9928, #14502, .T. ) ;
#1177=CIRCLE ( 'NONE', #14554, 24.00000000002400213 ) ;
#1181=CARTESIAN_POINT ( 'NONE',  ( 0.000000000000000000, -41.62350880771888484, -47.29147401531999861 ) ) ;
#1184=DIRECTION ( 'NONE',  ( 0.000000000000000000, 0.000000000000000000, 1.000000000000000000 ) ) ;
#1185=ORIENTED_EDGE ( 'NONE', *, *, #8556, .F. ) ;
#1192=CIRCLE ( 'NONE', #4821, 56.24900000005627021 ) ;
#1194=ORIENTED_EDGE ( 'NONE', *, *, #5338, .F. ) ;
#1195=AXIS2_PLACEMENT_3D ( 'NONE', #7428, #1717, #9049 ) ;
#1198=DIRECTION ( 'NONE',  ( 0.000000000000000000, 0.000000000000000000, 1.000000000000000000 ) ) ;
#1202=AXIS2_PLACEMENT_3D ( 'NONE', #13414, #4550, #11790 ) ;
#1207=CARTESIAN_POINT ( 'NONE',  ( 0.000000000000000000, 55.33199130079798778, -10.11537145609316468 ) ) ;
#1209=CARTESIAN_POINT ( 'NONE',  ( 0.000000000000000000, -39.14194549634336084, -40.58063702438384013 ) ) ;
#1214=ORIENTED_EDGE ( 'NONE', *, *, #11893, .F. ) ;
#1215=DIRECTION ( 'NONE',  ( -1.000000000000000000, 0.000000000000000000, -0.000000000000000000 ) ) ;
#1216=AXIS2_PLACEMENT_3D ( 'NONE', #4208, #12675, #10009 ) ;
#1218=DIRECTION ( 'NONE',  ( -1.000000000000000000, 0.000000000000000000, 0.000000000000000000 ) ) ;
#1231=EDGE_CURVE ( 'NONE', #17073, #15243, #5440, .T. ) ;
#1235=CARTESIAN_POINT ( 'NONE',  ( 10.00000000000000000, -32.31183295104805353, 46.20417134726119457 ) ) ;
#1238=ORIENTED_EDGE ( 'NONE', *, *, #803, .T. ) ;
#1240=EDGE_CURVE ( 'NONE', #10707, #11571, #11166, .T. ) ;
#1244=EDGE_CURVE ( 'NONE', #16786, #7064, #13313, .T. ) ;
#1246=CIRCLE ( 'NONE', #11871, 63.00000000006298961 ) ;
#1247=ORIENTED_EDGE ( 'NONE', *, *, #111, .T. ) ;
#1254=CYLINDRICAL_SURFACE ( 'NONE', #12528, 24.00000000002400213 ) ;
#1259=AXIS2_PLACEMENT_3D ( 'NONE', #16482, #9231, #15049 ) ;
#1272=DIRECTION ( 'NONE',  ( -1.000000000000000000, -0.000000000000000000, -0.000000000000000000 ) ) ;
#1274=DIRECTION ( 'NONE',  ( -1.000000000000000000, -0.000000000000000000, -0.000000000000000000 ) ) ;
#1275=CARTESIAN_POINT ( 'NONE',  ( 10.00000000000000000, -38.81885513159959800, -40.70683587897998734 ) ) ;
#1284=DIRECTION ( 'NONE',  ( 0.000000000000000000, 0.000000000000000000, -1.000000000000000000 ) ) ;
#1292=CARTESIAN_POINT ( 'NONE',  ( 10.00000000000000000, 39.14194549634421350, -40.58063702438301590 ) ) ;
#1297=DIRECTION ( 'NONE',  ( -1.000000000000000000, -0.000000000000000000, -0.000000000000000000 ) ) ;
#1301=ORIENTED_EDGE ( 'NONE', *, *, #8671, .T. ) ;
#1305=EDGE_CURVE ( 'NONE', #2152, #16786, #7212, .T. ) ;
#1306=AXIS2_PLACEMENT_3D ( 'NONE', #17895, #2175, #10558 ) ;
#1310=AXIS2_PLACEMENT_3D ( 'NONE', #293, #10106, #7140 ) ;
#1313=CARTESIAN_POINT ( 'NONE',  ( 0.000000000000000000, 47.29147401532013362, -41.62350880771872852 ) ) ;
#1315=CARTESIAN_POINT ( 'NONE',  ( 0.000000000000000000, 1.335003989221626775, 56.23315539212690339 ) ) ;
#1317=CARTESIAN_POINT ( 'NONE',  ( 10.00000000000000000, -24.33982105418938602, 50.71018745830434682 ) ) ;
#1318=EDGE_LOOP ( 'NONE', ( #13015, #394, #16969, #60 ) ) ;
#1322=ORIENTED_EDGE ( 'NONE', *, *, #10175, .T. ) ;
#1325=DIRECTION ( 'NONE',  ( 1.000000000000000000, 0.000000000000000000, 0.000000000000000000 ) ) ;
#1326=CARTESIAN_POINT ( 'NONE',  ( 10.00000000000000000, 56.37237871411034007, 1.017308535512583711 ) ) ;
#1332=VERTEX_POINT ( 'NONE', #13983 ) ;
#1333=AXIS2_PLACEMENT_3D ( 'NONE', #10419, #8975, #3282 ) ;
#1341=CARTESIAN_POINT ( 'NONE',  ( 10.00000000000000000, -55.74967257055887870, 7.478235706488783663 ) ) ;
#1345=CARTESIAN_POINT ( 'NONE',  ( 10.00000000000000000, -49.49802920186242972, 26.71881558261712186 ) ) ;
#1346=EDGE_CURVE ( 'NONE', #6013, #15420, #9786, .T. ) ;
#1347=ORIENTED_EDGE ( 'NONE', *, *, #13438, .F. ) ;
#1351=VERTEX_POINT ( 'NONE', #15597 ) ;
#1354=CARTESIAN_POINT ( 'NONE',  ( 0.000000000000000000, -9.823366686500245137, -55.51919907100663920 ) ) ;
#1360=EDGE_CURVE ( 'NONE', #15153, #18313, #3177, .T. ) ;
#1361=CARTESIAN_POINT ( 'NONE',  ( 10.00000000000000000, -26.71881558261766898, 49.49802920186213129 ) ) ;
#1363=DIRECTION ( 'NONE',  ( 0.000000000000000000, 0.8090169943749444537, 0.5877852522924772449 ) ) ;
#1367=LINE ( 'NONE', #17181, #428 ) ;
#1368=DIRECTION ( 'NONE',  ( -1.000000000000000000, -0.000000000000000000, 0.000000000000000000 ) ) ;
#1369=ORIENTED_EDGE ( 'NONE', *, *, #11664, .F. ) ;
#1372=CIRCLE ( 'NONE', #18701, 2.649999999999997691 ) ;
#1373=CARTESIAN_POINT ( 'NONE',  ( 10.00000000000000000, 40.19788616105610402, 48.50907078259396599 ) ) ;
#1376=EDGE_CURVE ( 'NONE', #17330, #6436, #16651, .T. ) ;
#1379=VERTEX_POINT ( 'NONE', #1129 ) ;
#1380=DIRECTION ( 'NONE',  ( -1.000000000000000000, -0.000000000000000000, -0.000000000000000000 ) ) ;
#1383=ORIENTED_EDGE ( 'NONE', *, *, #3704, .T. ) ;
#1384=AXIS2_PLACEMENT_3D ( 'NONE', #7473, #17582, #15958 ) ;
#1386=AXIS2_PLACEMENT_3D ( 'NONE', #9079, #17661, #4177 ) ;
#1388=ORIENTED_EDGE ( 'NONE', *, *, #13436, .F. ) ;
#1389=EDGE_CURVE ( 'NONE', #7667, #10934, #11478, .T. ) ;
#1395=AXIS2_PLACEMENT_3D ( 'NONE', #4398, #8866, #7433 ) ;
#1396=EDGE_LOOP ( 'NONE', ( #2043, #17843, #11361, #6167 ) ) ;
#1408=FACE_OUTER_BOUND ( 'NONE', #10176, .T. ) ;
#1409=CIRCLE ( 'NONE', #5665, 63.00000000006298961 ) ;
#1412=AXIS2_PLACEMENT_3D ( 'NONE', #15854, #5483, #5761 ) ;
#1415=AXIS2_PLACEMENT_3D ( 'NONE', #12758, #15515, #11024 ) ;
#1416=ORIENTED_EDGE ( 'NONE', *, *, #8913, .T. ) ;
#1418=CIRCLE ( 'NONE', #12064, 24.00000000002399858 ) ;
#1421=AXIS2_PLACEMENT_3D ( 'NONE', #18577, #2952, #17151 ) ;
#1427=DIRECTION ( 'NONE',  ( 1.000000000000000000, -0.000000000000000000, 0.000000000000000000 ) ) ;
#1429=ORIENTED_EDGE ( 'NONE', *, *, #14244, .F. ) ;
#1431=EDGE_CURVE ( 'NONE', #1351, #1465, #1744, .T. ) ;
#1437=FACE_BOUND ( 'NONE', #12860, .T. ) ;
#1438=AXIS2_PLACEMENT_3D ( 'NONE', #10845, #12667, #875 ) ;
#1443=AXIS2_PLACEMENT_3D ( 'NONE', #14790, #8968, #7556 ) ;
#1444=ORIENTED_EDGE ( 'NONE', *, *, #17033, .F. ) ;
#1445=DIRECTION ( 'NONE',  ( 0.000000000000000000, 0.000000000000000000, 1.000000000000000000 ) ) ;
#1451=DIRECTION ( 'NONE',  ( 0.000000000000000000, 0.000000000000000000, -1.000000000000000000 ) ) ;
#1459=ORIENTED_EDGE ( 'NONE', *, *, #15588, .F. ) ;
#1463=DIRECTION ( 'NONE',  ( 0.000000000000000000, -0.5877852522924801315, 0.8090169943749421222 ) ) ;
#1465=VERTEX_POINT ( 'NONE', #14612 ) ;
#1469=EDGE_CURVE ( 'NONE', #14358, #11663, #5702, .T. ) ;
#1473=DIRECTION ( 'NONE',  ( 1.000000000000000000, 0.000000000000000000, 0.000000000000000000 ) ) ;
#1475=DIRECTION ( 'NONE',  ( -1.000000000000000000, -0.000000000000000000, -0.000000000000000000 ) ) ;
#1477=CIRCLE ( 'NONE', #13629, 63.00000000006298961 ) ;
#1478=CARTESIAN_POINT ( 'NONE',  ( 0.000000000000000000, -23.24033432160480217, 58.55669782892453412 ) ) ;
#1482=CARTESIAN_POINT ( 'NONE',  ( 10.00000000000000000, -38.81885513160016643, 40.70683587897944022 ) ) ;
#1484=CIRCLE ( 'NONE', #6347, 24.00000000002400213 ) ;
#1485=ORIENTED_EDGE ( 'NONE', *, *, #7965, .F. ) ;
#1488=CARTESIAN_POINT ( 'NONE',  ( 0.000000000000000000, -56.37237871411034718, 25.01730853553617351 ) ) ;
#1493=CYLINDRICAL_SURFACE ( 'NONE', #7446, 56.24900000005625600 ) ;
#1496=VERTEX_POINT ( 'NONE', #13828 ) ;
#1499=CARTESIAN_POINT ( 'NONE',  ( 10.00000000000000000, 62.72529079327805590, 5.876895005582662534 ) ) ;
#1500=ORIENTED_EDGE ( 'NONE', *, *, #14129, .F. ) ;
#1501=VERTEX_POINT ( 'NONE', #10599 ) ;
#1502=ADVANCED_FACE ( 'NONE', ( #10876 ), #16316, .F. ) ;
#1516=EDGE_LOOP ( 'NONE', ( #10443, #4352 ) ) ;
#1518=CARTESIAN_POINT ( 'NONE',  ( 10.00000000000000000, -24.68609584167194981, 50.69000562871634230 ) ) ;
#1519=FACE_OUTER_BOUND ( 'NONE', #1696, .T. ) ;
#1522=CARTESIAN_POINT ( 'NONE',  ( 0.000000000000000000, 0.000000000000000000, 0.000000000000000000 ) ) ;
#1526=ORIENTED_EDGE ( 'NONE', *, *, #15585, .F. ) ;
#1529=EDGE_LOOP ( 'NONE', ( #15960, #3595, #8090, #14721 ) ) ;
#1531=VECTOR ( 'NONE', #8156, 1000.000000000000000 ) ;
#1536=VERTEX_POINT ( 'NONE', #8018 ) ;
#1538=EDGE_CURVE ( 'NONE', #2152, #15880, #13469, .T. ) ;
#1539=DIRECTION ( 'NONE',  ( -1.000000000000000000, -0.000000000000000000, -0.000000000000000000 ) ) ;
#1542=AXIS2_PLACEMENT_3D ( 'NONE', #15260, #10682, #12403 ) ;
#1545=CARTESIAN_POINT ( 'NONE',  ( 10.00000000000000000, 40.70683587897958944, 38.81885513160003143 ) ) ;
#1546=CARTESIAN_POINT ( 'NONE',  ( 10.00000000000000000, 56.23315539212690339, 1.335003989221828835 ) ) ;
#1549=ORIENTED_EDGE ( 'NONE', *, *, #3017, .T. ) ;
#1552=ORIENTED_EDGE ( 'NONE', *, *, #8041, .T. ) ;
#1554=ORIENTED_EDGE ( 'NONE', *, *, #12394, .F. ) ;
#1555=EDGE_CURVE ( 'NONE', #16736, #17488, #9076, .T. ) ;
#1556=CIRCLE ( 'NONE', #2153, 56.24900000005625600 ) ;
#1557=EDGE_CURVE ( 'NONE', #7366, #1171, #10497, .T. ) ;
#1561=CARTESIAN_POINT ( 'NONE',  ( 0.000000000000000000, 38.81885513159988932, 40.70683587897971734 ) ) ;
#1564=CARTESIAN_POINT ( 'NONE',  ( 10.00000000000000000, 40.58063702438398224, -39.14194549634321163 ) ) ;
#1568=EDGE_CURVE ( 'NONE', #11050, #10381, #18115, .T. ) ;
#1573=ORIENTED_EDGE ( 'NONE', *, *, #8580, .T. ) ;
#1577=VECTOR ( 'NONE', #7534, 1000.000000000000000 ) ;
#1579=DIRECTION ( 'NONE',  ( -1.000000000000000000, 0.000000000000000000, 0.000000000000000000 ) ) ;
#1589=ORIENTED_EDGE ( 'NONE', *, *, #12739, .T. ) ;
#1596=CIRCLE ( 'NONE', #8884, 24.00000000002400213 ) ;
#1598=FACE_OUTER_BOUND ( 'NONE', #11351, .T. ) ;
#1599=AXIS2_PLACEMENT_3D ( 'NONE', #9692, #1130, #14274 ) ;
#1600=CARTESIAN_POINT ( 'NONE',  ( 0.000000000000000000, 55.83748330407408389, -7.813799127873475747 ) ) ;
#1601=ORIENTED_EDGE ( 'NONE', *, *, #16635, .F. ) ;
#1606=CARTESIAN_POINT ( 'NONE',  ( 0.000000000000000000, 1.017308535512385870, 56.37237871411034007 ) ) ;
#1608=DIRECTION ( 'NONE',  ( 0.000000000000000000, -0.5877852522924623679, -0.8090169943749552228 ) ) ;
#1610=AXIS2_PLACEMENT_3D ( 'NONE', #7959, #732, #14925 ) ;
#1612=CARTESIAN_POINT ( 'NONE',  ( 10.00000000000000000, 7.813799127874054840, -55.83748330407399152 ) ) ;
#1614=ORIENTED_EDGE ( 'NONE', *, *, #7145, .F. ) ;
#1633=EDGE_LOOP ( 'NONE', ( #4393, #14259, #6883, #4525 ) ) ;
#1634=AXIS2_PLACEMENT_3D ( 'NONE', #18799, #15751, #1463 ) ;
#1635=CARTESIAN_POINT ( 'NONE',  ( 0.000000000000000000, 0.000000000000000000, 30.00000000000000000 ) ) ;
#1644=CARTESIAN_POINT ( 'NONE',  ( 10.00000000000000000, 0.000000000000000000, 0.000000000000000000 ) ) ;
#1648=ORIENTED_EDGE ( 'NONE', *, *, #5400, .T. ) ;
#1653=VERTEX_POINT ( 'NONE', #8502 ) ;
#1655=ADVANCED_FACE ( 'NONE', ( #1077 ), #6982, .T. ) ;
#1657=CARTESIAN_POINT ( 'NONE',  ( 10.00000000000000000, 55.83748330407408389, 16.18620087215052195 ) ) ;
#1660=CARTESIAN_POINT ( 'NONE',  ( 10.00000000000000000, 0.000000000000000000, 0.000000000000000000 ) ) ;
#1661=EDGE_CURVE ( 'NONE', #16801, #16490, #12405, .T. ) ;
#1664=EDGE_CURVE ( 'NONE', #15420, #16109, #13016, .T. ) ;
#1673=ORIENTED_EDGE ( 'NONE', *, *, #14938, .F. ) ;
#1674=CARTESIAN_POINT ( 'NONE',  ( 0.000000000000000000, 40.70683587898012235, -38.81885513159945589 ) ) ;
#1678=CYLINDRICAL_SURFACE ( 'NONE', #5863, 56.24900000005625600 ) ;
#1680=EDGE_LOOP ( 'NONE', ( #2596, #9124, #12279, #78 ) ) ;
#1683=VERTEX_POINT ( 'NONE', #16885 ) ;
#1684=CARTESIAN_POINT ( 'NONE',  ( 10.00000000000000000, 0.000000000000000000, 0.000000000000000000 ) ) ;
#1688=DIRECTION ( 'NONE',  ( 0.000000000000000000, 0.3090169943749480619, -0.9510565162951533091 ) ) ;
#1690=CIRCLE ( 'NONE', #2305, 63.00000000006298961 ) ;
#1691=VERTEX_POINT ( 'NONE', #6788 ) ;
#1692=DIRECTION ( 'NONE',  ( 0.000000000000000000, 0.000000000000000000, -1.000000000000000000 ) ) ;
#1695=AXIS2_PLACEMENT_3D ( 'NONE', #1846, #13475, #418 ) ;
#1696=EDGE_LOOP ( 'NONE', ( #10398, #5674, #5841, #2401 ) ) ;
#1698=CARTESIAN_POINT ( 'NONE',  ( 0.000000000000000000, 0.000000000000000000, 0.000000000000000000 ) ) ;
#1699=DIRECTION ( 'NONE',  ( -1.000000000000000000, -0.000000000000000000, 0.000000000000000000 ) ) ;
#1702=CARTESIAN_POINT ( 'NONE',  ( 10.00000000000000000, -49.76630880786327538, 26.49895292617986797 ) ) ;
#1704=LINE ( 'NONE', #664, #14185 ) ;
#1705=ORIENTED_EDGE ( 'NONE', *, *, #18797, .T. ) ;
#1707=FACE_BOUND ( 'NONE', #9784, .T. ) ;
#1711=CIRCLE ( 'NONE', #14792, 63.00000000006298961 ) ;
#1713=ORIENTED_EDGE ( 'NONE', *, *, #5547, .T. ) ;
#1714=DIRECTION ( 'NONE',  ( -1.000000000000000000, 0.000000000000000000, 0.000000000000000000 ) ) ;
#1715=DIRECTION ( 'NONE',  ( -1.000000000000000000, 0.000000000000000000, 0.000000000000000000 ) ) ;
#1716=EDGE_LOOP ( 'NONE', ( #10886, #17650, #17205, #12206 ) ) ;
#1717=DIRECTION ( 'NONE',  ( -1.000000000000000000, -0.000000000000000000, -0.000000000000000000 ) ) ;
#1721=CIRCLE ( 'NONE', #5688, 56.24900000005625600 ) ;
#1723=VERTEX_POINT ( 'NONE', #5352 ) ;
#1725=ORIENTED_EDGE ( 'NONE', *, *, #6339, .F. ) ;
#1727=EDGE_CURVE ( 'NONE', #12710, #10680, #11505, .T. ) ;
#1730=CIRCLE ( 'NONE', #16338, 24.00000000002399503 ) ;
#1731=CIRCLE ( 'NONE', #6605, 24.00000000002399858 ) ;
#1734=VERTEX_POINT ( 'NONE', #15461 ) ;
#1744=LINE ( 'NONE', #136, #12073 ) ;
#1746=CARTESIAN_POINT ( 'NONE',  ( 10.00000000000000000, 0.000000000000000000, 0.000000000000000000 ) ) ;
#1749=FACE_OUTER_BOUND ( 'NONE', #11560, .T. ) ;
#1757=DIRECTION ( 'NONE',  ( 1.000000000000000000, 0.000000000000000000, -0.000000000000000000 ) ) ;
#1759=CIRCLE ( 'NONE', #11195, 24.00000000002399148 ) ;
#1777=EDGE_CURVE ( 'NONE', #3205, #1351, #18794, .T. ) ;
#1778=DIRECTION ( 'NONE',  ( -1.000000000000000000, -0.000000000000000000, 0.000000000000000000 ) ) ;
#1780=ORIENTED_EDGE ( 'NONE', *, *, #11249, .F. ) ;
#1781=CARTESIAN_POINT ( 'NONE',  ( 10.00000000000000000, 0.000000000000000000, 0.000000000000000000 ) ) ;
#1783=EDGE_CURVE ( 'NONE', #19, #11318, #4212, .T. ) ;
#1784=VERTEX_POINT ( 'NONE', #989 ) ;
#1790=CARTESIAN_POINT ( 'NONE',  ( 10.00000000000000000, -56.23315539212689629, -1.335003989222221410 ) ) ;
#1795=ORIENTED_EDGE ( 'NONE', *, *, #8008, .F. ) ;
#1803=DIRECTION ( 'NONE',  ( 0.000000000000000000, 0.000000000000000000, 1.000000000000000000 ) ) ;
#1805=VERTEX_POINT ( 'NONE', #16206 ) ;
#1807=EDGE_CURVE ( 'NONE', #15635, #9576, #6637, .T. ) ;
#1809=ORIENTED_EDGE ( 'NONE', *, *, #18302, .T. ) ;
#1810=DIRECTION ( 'NONE',  ( -1.000000000000000000, 0.000000000000000000, 0.000000000000000000 ) ) ;
#1812=AXIS2_PLACEMENT_3D ( 'NONE', #3869, #12083, #13518 ) ;
#1814=ORIENTED_EDGE ( 'NONE', *, *, #669, .F. ) ;
#1817=ORIENTED_EDGE ( 'NONE', *, *, #16635, .T. ) ;
#1825=DIRECTION ( 'NONE',  ( 0.000000000000000000, 0.000000000000000000, 1.000000000000000000 ) ) ;
#1827=EDGE_CURVE ( 'NONE', #8389, #18189, #16667, .T. ) ;
#1829=DIRECTION ( 'NONE',  ( 0.000000000000000000, -0.1564344650402382242, 0.9876883405951366601 ) ) ;
#1835=CIRCLE ( 'NONE', #3365, 24.00000000002399858 ) ;
#1838=CYLINDRICAL_SURFACE ( 'NONE', #14238, 2.649999999999999467 ) ;
#1839=CARTESIAN_POINT ( 'NONE',  ( 10.00000000000000000, 41.62350880771986539, -47.29147401531911754 ) ) ;
#1843=CARTESIAN_POINT ( 'NONE',  ( 10.00000000000000000, -40.19788616105573453, -48.50907078259425731 ) ) ;
#1844=ORIENTED_EDGE ( 'NONE', *, *, #15943, .F. ) ;
#1846=CARTESIAN_POINT ( 'NONE',  ( 10.00000000000000000, -46.20417134726108088, -32.31183295104820985 ) ) ;
#1848=CARTESIAN_POINT ( 'NONE',  ( 10.00000000000000000, 0.000000000000000000, 0.000000000000000000 ) ) ;
#1855=ORIENTED_EDGE ( 'NONE', *, *, #11917, .F. ) ;
#1857=DIRECTION ( 'NONE',  ( -1.000000000000000000, 0.000000000000000000, 0.000000000000000000 ) ) ;
#1861=CIRCLE ( 'NONE', #4307, 63.00000000006298961 ) ;
#1862=CARTESIAN_POINT ( 'NONE',  ( 10.00000000000000000, -50.71018745830427576, -24.33982105418956010 ) ) ;
#1864=VERTEX_POINT ( 'NONE', #14317 ) ;
#1869=FACE_OUTER_BOUND ( 'NONE', #5848, .T. ) ;
#1874=DIRECTION ( 'NONE',  ( 0.000000000000000000, 0.000000000000000000, 1.000000000000000000 ) ) ;
#1879=VERTEX_POINT ( 'NONE', #1361 ) ;
#1883=CYLINDRICAL_SURFACE ( 'NONE', #4798, 24.00000000002399858 ) ;
#1885=LINE ( 'NONE', #10735, #13920 ) ;
#1886=DIRECTION ( 'NONE',  ( 0.000000000000000000, -0.4539904997395351471, -0.8910065241883737830 ) ) ;
#1890=DIRECTION ( 'NONE',  ( 0.000000000000000000, 0.000000000000000000, 1.000000000000000000 ) ) ;
#1899=ADVANCED_FACE ( 'NONE', ( #5744 ), #13164, .T. ) ;
#1908=DIRECTION ( 'NONE',  ( 0.000000000000000000, 0.000000000000000000, -1.000000000000000000 ) ) ;
#1912=CARTESIAN_POINT ( 'NONE',  ( 10.00000000000000000, 16.10733642026559309, -53.89344778774794520 ) ) ;
#1921=CIRCLE ( 'NONE', #2522, 63.00000000006298961 ) ;
#1922=ORIENTED_EDGE ( 'NONE', *, *, #13802, .T. ) ;
#1925=EDGE_CURVE ( 'NONE', #9576, #1332, #11730, .T. ) ;
#1933=CARTESIAN_POINT ( 'NONE',  ( 10.00000000000000000, 53.06836994729258805, -18.64666490672316712 ) ) ;
#1940=VERTEX_POINT ( 'NONE', #10308 ) ;
#1941=ORIENTED_EDGE ( 'NONE', *, *, #8242, .T. ) ;
#1942=CARTESIAN_POINT ( 'NONE',  ( 0.000000000000000000, 1.017308535513159695, -56.37237871411032586 ) ) ;
#1946=EDGE_CURVE ( 'NONE', #5117, #18145, #14677, .T. ) ;
#1948=CARTESIAN_POINT ( 'NONE',  ( 0.000000000000000000, 0.000000000000000000, 0.000000000000000000 ) ) ;
#1949=DIRECTION ( 'NONE',  ( -1.000000000000000000, 0.000000000000000000, -0.000000000000000000 ) ) ;
#1960=VERTEX_POINT ( 'NONE', #18096 ) ;
#1961=EDGE_LOOP ( 'NONE', ( #2882, #3153, #16697, #4559 ) ) ;
#1962=ADVANCED_FACE ( 'NONE', ( #9052 ), #4953, .T. ) ;
#1969=CARTESIAN_POINT ( 'NONE',  ( -10.00000000000000000, -26.45033635316118747, 33.75576474687270689 ) ) ;
#1977=ORIENTED_EDGE ( 'NONE', *, *, #10728, .F. ) ;
#1980=DIRECTION ( 'NONE',  ( -1.000000000000000000, -0.000000000000000000, -0.000000000000000000 ) ) ;
#1982=ORIENTED_EDGE ( 'NONE', *, *, #15760, .F. ) ;
#1984=CARTESIAN_POINT ( 'NONE',  ( 10.00000000000000000, 0.000000000000000000, 0.000000000000000000 ) ) ;
#1986=ORIENTED_EDGE ( 'NONE', *, *, #11152, .F. ) ;
#1989=AXIS2_PLACEMENT_3D ( 'NONE', #13677, #7858, #6427 ) ;
#1990=AXIS2_PLACEMENT_3D ( 'NONE', #6317, #3744, #9645 ) ;
#1994=CARTESIAN_POINT ( 'NONE',  ( 10.00000000000000000, 38.81885513160045065, -40.70683587897917022 ) ) ;
#1998=AXIS2_PLACEMENT_3D ( 'NONE', #9837, #14222, #1184 ) ;
#1999=DIRECTION ( 'NONE',  ( 1.000000000000000000, 0.000000000000000000, -0.000000000000000000 ) ) ;
#2000=ADVANCED_FACE ( 'NONE', ( #13726 ), #10472, .T. ) ;
#2009=EDGE_LOOP ( 'NONE', ( #17323, #14040, #14167, #14688 ) ) ;
#2014=CIRCLE ( 'NONE', #14479, 24.00000000002399858 ) ;
#2015=VERTEX_POINT ( 'NONE', #4674 ) ;
#2020=ORIENTED_EDGE ( 'NONE', *, *, #16871, .F. ) ;
#2023=AXIS2_PLACEMENT_3D ( 'NONE', #11529, #10177, #14294 ) ;
#2025=DIRECTION ( 'NONE',  ( -1.000000000000000000, -0.000000000000000000, -0.000000000000000000 ) ) ;
#2026=CARTESIAN_POINT ( 'NONE',  ( 0.000000000000000000, 39.14194549634364506, 40.58063702438359144 ) ) ;
#2028=AXIS2_PLACEMENT_3D ( 'NONE', #7255, #13074, #10203 ) ;
#2029=DIRECTION ( 'NONE',  ( -1.000000000000000000, -0.000000000000000000, -0.000000000000000000 ) ) ;
#2035=ORIENTED_EDGE ( 'NONE', *, *, #747, .T. ) ;
#2040=CYLINDRICAL_SURFACE ( 'NONE', #7098, 24.00000000002399858 ) ;
#2041=CARTESIAN_POINT ( 'NONE',  ( 10.00000000000000000, -7.478235706488566059, -55.74967257055892134 ) ) ;
#2043=ORIENTED_EDGE ( 'NONE', *, *, #8293, .T. ) ;
#2048=ORIENTED_EDGE ( 'NONE', *, *, #10295, .T. ) ;
#2049=CIRCLE ( 'NONE', #11777, 56.24900000005625600 ) ;
#2053=DIRECTION ( 'NONE',  ( -1.000000000000000000, -0.000000000000000000, -0.000000000000000000 ) ) ;
#2054=DIRECTION ( 'NONE',  ( 0.000000000000000000, 0.000000000000000000, 1.000000000000000000 ) ) ;
#2060=CARTESIAN_POINT ( 'NONE',  ( 10.00000000000000000, 55.33199130079800199, -10.11537145609316646 ) ) ;
#2064=CARTESIAN_POINT ( 'NONE',  ( 10.00000000000000000, -46.20417134726153563, 32.31183295104756326 ) ) ;
#2066=ORIENTED_EDGE ( 'NONE', *, *, #12078, .T. ) ;
#2072=LINE ( 'NONE', #7877, #12145 ) ;
#2075=CARTESIAN_POINT ( 'NONE',  ( 0.000000000000000000, 0.000000000000000000, 0.000000000000000000 ) ) ;
#2078=ORIENTED_EDGE ( 'NONE', *, *, #14142, .T. ) ;
#2084=LINE ( 'NONE', #13330, #12691 ) ;
#2087=EDGE_CURVE ( 'NONE', #7622, #417, #4221, .T. ) ;
#2093=CARTESIAN_POINT ( 'NONE',  ( 0.000000000000000000, 0.000000000000000000, 0.000000000000000000 ) ) ;
#2094=ORIENTED_EDGE ( 'NONE', *, *, #1807, .F. ) ;
#2101=EDGE_LOOP ( 'NONE', ( #4438, #9725, #8083, #4707 ) ) ;
#2108=CARTESIAN_POINT ( 'NONE',  ( 10.00000000000000000, 0.000000000000000000, 0.000000000000000000 ) ) ;
#2109=DIRECTION ( 'NONE',  ( -1.000000000000000000, -0.000000000000000000, -0.000000000000000000 ) ) ;
#2111=ORIENTED_EDGE ( 'NONE', *, *, #8088, .T. ) ;
#2113=ORIENTED_EDGE ( 'NONE', *, *, #14019, .F. ) ;
#2114=ADVANCED_FACE ( 'NONE', ( #18480 ), #15624, .T. ) ;
#2118=CARTESIAN_POINT ( 'NONE',  ( 0.000000000000000000, -5.120903701083534543E-13, -45.00000000000000000 ) ) ;
#2120=AXIS2_PLACEMENT_3D ( 'NONE', #59, #8439, #7184 ) ;
#2122=CYLINDRICAL_SURFACE ( 'NONE', #3242, 56.24900000005625600 ) ;
#2125=CARTESIAN_POINT ( 'NONE',  ( 10.00000000000000000, -31.97297851452457351, 46.27827401617392411 ) ) ;
#2126=ORIENTED_EDGE ( 'NONE', *, *, #7213, .F. ) ;
#2127=CARTESIAN_POINT ( 'NONE',  ( 10.00000000000000000, -26.45033635316118747, 39.05576474687271116 ) ) ;
#2128=ORIENTED_EDGE ( 'NONE', *, *, #7354, .F. ) ;
#2129=ADVANCED_FACE ( 'NONE', ( #13810 ), #11335, .T. ) ;
#2137=ORIENTED_EDGE ( 'NONE', *, *, #14327, .T. ) ;
#2139=ADVANCED_FACE ( 'NONE', ( #3636 ), #17070, .F. ) ;
#2140=MECHANICAL_DESIGN_GEOMETRIC_PRESENTATION_REPRESENTATION('',(#622),#17654);
#2141=EDGE_CURVE ( 'NONE', #14103, #1152, #2566, .T. ) ;
#2145=DIRECTION ( 'NONE',  ( -1.000000000000000000, -0.000000000000000000, -0.000000000000000000 ) ) ;
#2147=ORIENTED_EDGE ( 'NONE', *, *, #11094, .F. ) ;
#2152=VERTEX_POINT ( 'NONE', #12384 ) ;
#2153=AXIS2_PLACEMENT_3D ( 'NONE', #4669, #7705, #4763 ) ;
#2156=DIRECTION ( 'NONE',  ( 1.000000000000000000, 0.000000000000000000, 0.000000000000000000 ) ) ;
#2157=VERTEX_POINT ( 'NONE', #12773 ) ;
#2159=DIRECTION ( 'NONE',  ( -1.000000000000000000, -0.000000000000000000, -0.000000000000000000 ) ) ;
#2160=ORIENTED_EDGE ( 'NONE', *, *, #2665, .T. ) ;
#2167=ORIENTED_EDGE ( 'NONE', *, *, #15982, .T. ) ;
#2175=DIRECTION ( 'NONE',  ( -1.000000000000000000, 0.000000000000000000, 0.000000000000000000 ) ) ;
#2178=CIRCLE ( 'NONE', #318, 63.00000000006298961 ) ;
#2182=DIRECTION ( 'NONE',  ( 1.000000000000000000, 0.000000000000000000, 0.000000000000000000 ) ) ;
#2183=AXIS2_PLACEMENT_3D ( 'NONE', #7432, #6107, #9053 ) ;
#2184=CIRCLE ( 'NONE', #4619, 24.00000000002399858 ) ;
#2185=EDGE_CURVE ( 'NONE', #16278, #4962, #6334, .T. ) ;
#2197=DIRECTION ( 'NONE',  ( -1.000000000000000000, 0.000000000000000000, 0.000000000000000000 ) ) ;
#2198=ORIENTED_EDGE ( 'NONE', *, *, #5386, .T. ) ;
#2199=EDGE_CURVE ( 'NONE', #10808, #1653, #6646, .T. ) ;
#2202=EDGE_CURVE ( 'NONE', #10253, #14080, #6024, .T. ) ;
#2203=AXIS2_PLACEMENT_3D ( 'NONE', #81, #7110, #5961 ) ;
#2204=ORIENTED_EDGE ( 'NONE', *, *, #4568, .F. ) ;
#2208=CARTESIAN_POINT ( 'NONE',  ( 0.000000000000000000, 56.37237871411034007, 1.017308535512583711 ) ) ;
#2213=DIRECTION ( 'NONE',  ( 0.000000000000000000, 0.000000000000000000, -1.000000000000000000 ) ) ;
#2214=DIRECTION ( 'NONE',  ( 0.000000000000000000, 0.000000000000000000, -1.000000000000000000 ) ) ;
#2215=ORIENTED_EDGE ( 'NONE', *, *, #10265, .T. ) ;
#2216=DIRECTION ( 'NONE',  ( 0.000000000000000000, 0.000000000000000000, 1.000000000000000000 ) ) ;
#2218=AXIS2_PLACEMENT_3D ( 'NONE', #9108, #9392, #12335 ) ;
#2222=VERTEX_POINT ( 'NONE', #3726 ) ;
#2226=DIRECTION ( 'NONE',  ( 0.000000000000000000, 0.000000000000000000, 1.000000000000000000 ) ) ;
#2227=ORIENTED_EDGE ( 'NONE', *, *, #3683, .T. ) ;
#2229=FACE_OUTER_BOUND ( 'NONE', #6165, .T. ) ;
#2234=ORIENTED_EDGE ( 'NONE', *, *, #6922, .F. ) ;
#2235=CARTESIAN_POINT ( 'NONE',  ( 0.000000000000000000, 26.49895292618076326, -49.76630880786279931 ) ) ;
#2236=ORIENTED_EDGE ( 'NONE', *, *, #7658, .F. ) ;
#2240=DIRECTION ( 'NONE',  ( 0.000000000000000000, -0.8090169943749531134, 0.5877852522924653655 ) ) ;
#2241=DIRECTION ( 'NONE',  ( 0.000000000000000000, 0.000000000000000000, 1.000000000000000000 ) ) ;
#2242=LINE ( 'NONE', #3971, #1531 ) ;
#2244=VERTEX_POINT ( 'NONE', #12574 ) ;
#2249=DIRECTION ( 'NONE',  ( -1.000000000000000000, -0.000000000000000000, 0.000000000000000000 ) ) ;
#2252=EDGE_CURVE ( 'NONE', #1940, #1723, #3606, .T. ) ;
#2254=ORIENTED_EDGE ( 'NONE', *, *, #10755, .T. ) ;
#2256=ORIENTED_EDGE ( 'NONE', *, *, #615, .F. ) ;
#2261=DIRECTION ( 'NONE',  ( 0.000000000000000000, 0.000000000000000000, -1.000000000000000000 ) ) ;
#2264=DIRECTION ( 'NONE',  ( 0.000000000000000000, 0.000000000000000000, 1.000000000000000000 ) ) ;
#2268=FACE_OUTER_BOUND ( 'NONE', #7540, .T. ) ;
#2272=EDGE_CURVE ( 'NONE', #3285, #14075, #11425, .T. ) ;
#2276=ORIENTED_EDGE ( 'NONE', *, *, #2354, .F. ) ;
#2279=LINE ( 'NONE', #6675, #17552 ) ;
#2281=EDGE_CURVE ( 'NONE', #1501, #12720, #5292, .T. ) ;
#2288=DIRECTION ( 'NONE',  ( -1.000000000000000000, 0.000000000000000000, 0.000000000000000000 ) ) ;
#2291=EDGE_LOOP ( 'NONE', ( #6867, #1141, #4399, #17646 ) ) ;
#2293=EDGE_LOOP ( 'NONE', ( #2111, #1500, #15355, #2594 ) ) ;
#2298=CARTESIAN_POINT ( 'NONE',  ( 10.00000000000000000, -24.68609584167124282, -50.69000562871667626 ) ) ;
#2300=CARTESIAN_POINT ( 'NONE',  ( 0.000000000000000000, 46.20417134726178432, -32.31183295104722220 ) ) ;
#2301=FACE_OUTER_BOUND ( 'NONE', #5097, .T. ) ;
#2305=AXIS2_PLACEMENT_3D ( 'NONE', #6729, #2159, #14151 ) ;
#2309=CIRCLE ( 'NONE', #15392, 63.00000000006298961 ) ;
#2312=AXIS2_PLACEMENT_3D ( 'NONE', #2026, #16502, #15180 ) ;
#2313=DIRECTION ( 'NONE',  ( 0.000000000000000000, 0.5877852522924685852, 0.8090169943749505599 ) ) ;
#2314=DIRECTION ( 'NONE',  ( -1.000000000000000000, 0.000000000000000000, 0.000000000000000000 ) ) ;
#2315=ORIENTED_EDGE ( 'NONE', *, *, #13326, .F. ) ;
#2317=AXIS2_PLACEMENT_3D ( 'NONE', #8342, #2901, #10050 ) ;
#2322=EDGE_LOOP ( 'NONE', ( #1922, #4258, #16781, #7012 ) ) ;
#2323=AXIS2_PLACEMENT_3D ( 'NONE', #16802, #12515, #8135 ) ;
#2327=AXIS2_PLACEMENT_3D ( 'NONE', #9831, #10021, #5550 ) ;
#2329=CARTESIAN_POINT ( 'NONE',  ( 0.000000000000000000, 32.11449294037196722, 54.20017844242522642 ) ) ;
#2331=VERTEX_POINT ( 'NONE', #8482 ) ;
#2332=FACE_OUTER_BOUND ( 'NONE', #8917, .T. ) ;
#2335=DIRECTION ( 'NONE',  ( -1.000000000000000000, -0.000000000000000000, -0.000000000000000000 ) ) ;
#2336=DIRECTION ( 'NONE',  ( -1.000000000000000000, -0.000000000000000000, -0.000000000000000000 ) ) ;
#2337=VECTOR ( 'NONE', #5230, 1000.000000000000000 ) ;
#2343=CARTESIAN_POINT ( 'NONE',  ( 10.00000000000000000, -49.49802920186203892, -26.71881558261783951 ) ) ;
#2345=AXIS2_PLACEMENT_3D ( 'NONE', #6456, #16546, #15131 ) ;
#2354=EDGE_CURVE ( 'NONE', #16064, #6188, #12953, .T. ) ;
#2357=DIRECTION ( 'NONE',  ( -1.000000000000000000, 0.000000000000000000, 0.000000000000000000 ) ) ;
#2359=VERTEX_POINT ( 'NONE', #5987 ) ;
#2361=ORIENTED_EDGE ( 'NONE', *, *, #4802, .T. ) ;
#2364=CARTESIAN_POINT ( 'NONE',  ( -10.00000000000000000, 0.000000000000000000, 0.000000000000000000 ) ) ;
#2369=LINE ( 'NONE', #13715, #17925 ) ;
#2370=CYLINDRICAL_SURFACE ( 'NONE', #11303, 56.24900000005625600 ) ;
#2372=AXIS2_PLACEMENT_3D ( 'NONE', #11920, #16407, #17729 ) ;
#2380=DIRECTION ( 'NONE',  ( -1.000000000000000000, 0.000000000000000000, 0.000000000000000000 ) ) ;
#2382=CARTESIAN_POINT ( 'NONE',  ( 10.00000000000000000, 9.823366686501460165, -55.51919907100641893 ) ) ;
#2391=ORIENTED_EDGE ( 'NONE', *, *, #50, .T. ) ;
#2394=DIRECTION ( 'NONE',  ( -1.000000000000000000, -0.000000000000000000, 0.000000000000000000 ) ) ;
#2396=EDGE_LOOP ( 'NONE', ( #4118, #12826, #1017, #6367 ) ) ;
#2398=EDGE_LOOP ( 'NONE', ( #3586, #10804, #12630, #2943 ) ) ;
#2401=ORIENTED_EDGE ( 'NONE', *, *, #12383, .T. ) ;
#2403=AXIS2_PLACEMENT_3D ( 'NONE', #1235, #80, #14441 ) ;
#2406=DIRECTION ( 'NONE',  ( -1.000000000000000000, 0.000000000000000000, -0.000000000000000000 ) ) ;
#2410=DIRECTION ( 'NONE',  ( 0.000000000000000000, 0.000000000000000000, 1.000000000000000000 ) ) ;
#2411=DIRECTION ( 'NONE',  ( 0.000000000000000000, 0.000000000000000000, -1.000000000000000000 ) ) ;
#2412=AXIS2_PLACEMENT_3D ( 'NONE', #9241, #7813, #6485 ) ;
#2413=CARTESIAN_POINT ( 'NONE',  ( 10.00000000000000000, -62.87238730325622527, 4.007856633823161374 ) ) ;
#2421=ORIENTED_EDGE ( 'NONE', *, *, #2141, .T. ) ;
#2427=CIRCLE ( 'NONE', #7884, 56.24900000005625600 ) ;
#2430=LINE ( 'NONE', #12905, #8813 ) ;
#2434=EDGE_LOOP ( 'NONE', ( #16013, #12350, #1725, #15793 ) ) ;
#2436=ORIENTED_EDGE ( 'NONE', *, *, #1360, .F. ) ;
#2437=CARTESIAN_POINT ( 'NONE',  ( 10.00000000000000000, 33.95787273855309252, -45.00825343884985585 ) ) ;
#2438=DIRECTION ( 'NONE',  ( -1.000000000000000000, 0.000000000000000000, 0.000000000000000000 ) ) ;
#2439=VECTOR ( 'NONE', #7371, 1000.000000000000000 ) ;
#2440=DIRECTION ( 'NONE',  ( -1.000000000000000000, 0.000000000000000000, 0.000000000000000000 ) ) ;
#2444=ORIENTED_EDGE ( 'NONE', *, *, #7325, .F. ) ;
#2446=ADVANCED_FACE ( 'NONE', ( #13709 ), #4848, .T. ) ;
#2451=CARTESIAN_POINT ( 'NONE',  ( 0.000000000000000000, 0.000000000000000000, 0.000000000000000000 ) ) ;
#2453=ORIENTED_EDGE ( 'NONE', *, *, #6974, .T. ) ;
#2454=DIRECTION ( 'NONE',  ( -1.000000000000000000, -0.000000000000000000, -0.000000000000000000 ) ) ;
#2455=DIRECTION ( 'NONE',  ( 0.000000000000000000, 0.000000000000000000, 1.000000000000000000 ) ) ;
#2459=EDGE_LOOP ( 'NONE', ( #8753, #6365, #5072, #5009 ) ) ;
#2466=ORIENTED_EDGE ( 'NONE', *, *, #4485, .T. ) ;
#2468=DIRECTION ( 'NONE',  ( -1.000000000000000000, 0.000000000000000000, 0.000000000000000000 ) ) ;
#2474=DIRECTION ( 'NONE',  ( 0.000000000000000000, -0.3090169943749547787, 0.9510565162951511997 ) ) ;
#2475=DIRECTION ( 'NONE',  ( 1.000000000000000000, 0.000000000000000000, 0.000000000000000000 ) ) ;
#2477=CARTESIAN_POINT ( 'NONE',  ( 10.00000000000000000, -55.51919907100660367, 9.823366686500467182 ) ) ;
#2484=DIRECTION ( 'NONE',  ( -1.000000000000000000, 0.000000000000000000, 0.000000000000000000 ) ) ;
#2488=DIRECTION ( 'NONE',  ( 0.000000000000000000, 0.000000000000000000, -1.000000000000000000 ) ) ;
#2491=EDGE_CURVE ( 'NONE', #17597, #2625, #3627, .T. ) ;
#2492=ORIENTED_EDGE ( 'NONE', *, *, #4160, .T. ) ;
#2493=ORIENTED_EDGE ( 'NONE', *, *, #8105, .F. ) ;
#2502=DIRECTION ( 'NONE',  ( 0.000000000000000000, -0.7071067811865389130, -0.7071067811865561215 ) ) ;
#2503=CARTESIAN_POINT ( 'NONE',  ( 0.000000000000000000, 44.70888270294162226, 34.13306034420202906 ) ) ;
#2506=ORIENTED_EDGE ( 'NONE', *, *, #619, .F. ) ;
#2508=DIRECTION ( 'NONE',  ( -1.000000000000000000, -0.000000000000000000, -0.000000000000000000 ) ) ;
#2509=DIRECTION ( 'NONE',  ( 0.000000000000000000, 0.3090169943749411785, 0.9510565162951556406 ) ) ;
#2510=ORIENTED_EDGE ( 'NONE', *, *, #1946, .T. ) ;
#2511=CYLINDRICAL_SURFACE ( 'NONE', #17239, 24.00000000002399858 ) ;
#2515=VERTEX_POINT ( 'NONE', #9308 ) ;
#2518=LINE ( 'NONE', #719, #14481 ) ;
#2520=CARTESIAN_POINT ( 'NONE',  ( 10.00000000000000000, -50.69000562871624993, -24.68609584167212745 ) ) ;
#2522=AXIS2_PLACEMENT_3D ( 'NONE', #3970, #14145, #14249 ) ;
#2523=CIRCLE ( 'NONE', #17715, 63.00000000006298961 ) ;
#2524=VECTOR ( 'NONE', #2288, 1000.000000000000000 ) ;
#2526=ORIENTED_EDGE ( 'NONE', *, *, #13067, .T. ) ;
#2527=CARTESIAN_POINT ( 'NONE',  ( 10.00000000000000000, 0.000000000000000000, 0.000000000000000000 ) ) ;
#2528=DIRECTION ( 'NONE',  ( 1.000000000000000000, 0.000000000000000000, 0.000000000000000000 ) ) ;
#2530=VERTEX_POINT ( 'NONE', #11978 ) ;
#2535=EDGE_CURVE ( 'NONE', #12076, #1784, #10557, .T. ) ;
#2537=DIRECTION ( 'NONE',  ( 1.000000000000000000, -0.000000000000000000, -0.000000000000000000 ) ) ;
#2538=CARTESIAN_POINT ( 'NONE',  ( 5.000000000000000000, 62.87238730325621106, 4.007856633823612569 ) ) ;
#2543=DIRECTION ( 'NONE',  ( -1.000000000000000000, -0.000000000000000000, -0.000000000000000000 ) ) ;
#2546=LINE ( 'NONE', #11220, #15742 ) ;
#2547=ORIENTED_EDGE ( 'NONE', *, *, #4709, .T. ) ;
#2550=CARTESIAN_POINT ( 'NONE',  ( 0.000000000000000000, 0.000000000000000000, 0.000000000000000000 ) ) ;
#2551=LINE ( 'NONE', #11117, #17123 ) ;
#2555=EDGE_CURVE ( 'NONE', #12447, #13033, #3324, .T. ) ;
#2556=ORIENTED_EDGE ( 'NONE', *, *, #13530, .T. ) ;
#2557=LINE ( 'NONE', #17233, #7575 ) ;
#2558=DIRECTION ( 'NONE',  ( -1.000000000000000000, -0.000000000000000000, 0.000000000000000000 ) ) ;
#2559=( GEOMETRIC_REPRESENTATION_CONTEXT ( 3 ) GLOBAL_UNCERTAINTY_ASSIGNED_CONTEXT ( ( #12436 ) ) GLOBAL_UNIT_ASSIGNED_CONTEXT ( ( #5426, #3996, #5518 ) ) REPRESENTATION_CONTEXT ( 'NONE', 'WORKASPACE' ) );
#2561=VERTEX_POINT ( 'NONE', #951 ) ;
#2562=DIRECTION ( 'NONE',  ( 0.000000000000000000, -0.4539904997395542430, 0.8910065241883641241 ) ) ;
#2564=DIRECTION ( 'NONE',  ( -1.000000000000000000, 0.000000000000000000, 0.000000000000000000 ) ) ;
#2566=LINE ( 'NONE', #9722, #15457 ) ;
#2569=ORIENTED_EDGE ( 'NONE', *, *, #8105, .T. ) ;
#2583=EDGE_CURVE ( 'NONE', #18126, #9305, #8169, .T. ) ;
#2586=ORIENTED_EDGE ( 'NONE', *, *, #1555, .T. ) ;
#2588=VECTOR ( 'NONE', #10689, 1000.000000000000000 ) ;
#2594=ORIENTED_EDGE ( 'NONE', *, *, #18748, .T. ) ;
#2596=ORIENTED_EDGE ( 'NONE', *, *, #16589, .T. ) ;
#2604=DIRECTION ( 'NONE',  ( -1.000000000000000000, 0.000000000000000000, 0.000000000000000000 ) ) ;
#2607=VECTOR ( 'NONE', #7345, 1000.000000000000000 ) ;
#2613=LINE ( 'NONE', #5188, #5408 ) ;
#2615=EDGE_CURVE ( 'NONE', #4819, #2625, #15231, .T. ) ;
#2616=AXIS2_PLACEMENT_3D ( 'NONE', #7357, #11281, #2892 ) ;
#2620=EDGE_CURVE ( 'NONE', #12166, #12513, #10304, .T. ) ;
#2622=DIRECTION ( 'NONE',  ( 0.000000000000000000, 0.000000000000000000, 1.000000000000000000 ) ) ;
#2625=VERTEX_POINT ( 'NONE', #13990 ) ;
#2628=EDGE_LOOP ( 'NONE', ( #5943, #3535, #15510, #6181 ) ) ;
#2629=FACE_OUTER_BOUND ( 'NONE', #18606, .T. ) ;
#2631=AXIS2_PLACEMENT_3D ( 'NONE', #7517, #12084, #373 ) ;
#2634=DIRECTION ( 'NONE',  ( 0.000000000000000000, 0.9510565162951543083, -0.3090169943749447312 ) ) ;
#2637=DIRECTION ( 'NONE',  ( 0.000000000000000000, 0.000000000000000000, -1.000000000000000000 ) ) ;
#2641=CARTESIAN_POINT ( 'NONE',  ( 0.000000000000000000, 0.000000000000000000, 0.000000000000000000 ) ) ;
#2645=CARTESIAN_POINT ( 'NONE',  ( 10.00000000000000000, -13.79392154159178219, 61.47135697633773788 ) ) ;
#2646=EDGE_CURVE ( 'NONE', #5108, #478, #9089, .T. ) ;
#2650=FACE_OUTER_BOUND ( 'NONE', #3807, .T. ) ;
#2652=VERTEX_POINT ( 'NONE', #13889 ) ;
#2653=ORIENTED_EDGE ( 'NONE', *, *, #4000, .F. ) ;
#2654=VECTOR ( 'NONE', #9756, 1000.000000000000000 ) ;
#2655=DIRECTION ( 'NONE',  ( -1.000000000000000000, 0.000000000000000000, 0.000000000000000000 ) ) ;
#2657=CARTESIAN_POINT ( 'NONE',  ( 10.00000000000000000, 0.000000000000000000, 0.000000000000000000 ) ) ;
#2658=CARTESIAN_POINT ( 'NONE',  ( 10.00000000000000000, 44.70888270294162226, 34.13306034420202906 ) ) ;
#2660=CIRCLE ( 'NONE', #4482, 24.00000000002399503 ) ;
#2662=AXIS2_PLACEMENT_3D ( 'NONE', #1007, #9762, #8037 ) ;
#2665=EDGE_CURVE ( 'NONE', #15635, #4270, #10931, .T. ) ;
#2683=VECTOR ( 'NONE', #17540, 1000.000000000000000 ) ;
#2684=ORIENTED_EDGE ( 'NONE', *, *, #13908, .T. ) ;
#2685=EDGE_CURVE ( 'NONE', #743, #16490, #9595, .T. ) ;
#2706=AXIS2_PLACEMENT_3D ( 'NONE', #7616, #13433, #8939 ) ;
#2707=CARTESIAN_POINT ( 'NONE',  ( 10.00000000000000000, 53.06836994729233936, 18.64666490672390964 ) ) ;
#2711=VECTOR ( 'NONE', #15694, 1000.000000000000000 ) ;
#2721=DIRECTION ( 'NONE',  ( -1.000000000000000000, -0.000000000000000000, -0.000000000000000000 ) ) ;
#2724=VERTEX_POINT ( 'NONE', #8636 ) ;
#2725=EDGE_LOOP ( 'NONE', ( #3624, #14962, #6912, #14335 ) ) ;
#2726=EDGE_CURVE ( 'NONE', #2157, #15536, #7207, .T. ) ;
#2727=DIRECTION ( 'NONE',  ( -1.000000000000000000, 0.000000000000000000, 0.000000000000000000 ) ) ;
#2729=ADVANCED_FACE ( 'NONE', ( #12845 ), #9883, .T. ) ;
#2732=DIRECTION ( 'NONE',  ( 0.000000000000000000, 0.000000000000000000, 1.000000000000000000 ) ) ;
#2738=EDGE_LOOP ( 'NONE', ( #9733, #12727, #5582, #3284 ) ) ;
#2739=CARTESIAN_POINT ( 'NONE',  ( 10.00000000000000000, 24.97244012287502102, 57.83923611457328207 ) ) ;
#2740=EDGE_CURVE ( 'NONE', #13520, #5686, #5697, .T. ) ;
#2741=VECTOR ( 'NONE', #9770, 1000.000000000000000 ) ;
#2745=ORIENTED_EDGE ( 'NONE', *, *, #16920, .F. ) ;
#2748=AXIS2_PLACEMENT_3D ( 'NONE', #225, #8696, #5927 ) ;
#2749=DIRECTION ( 'NONE',  ( -1.000000000000000000, -0.000000000000000000, 0.000000000000000000 ) ) ;
#2751=ORIENTED_EDGE ( 'NONE', *, *, #4432, .F. ) ;
#2752=ORIENTED_EDGE ( 'NONE', *, *, #938, .T. ) ;
#2756=CARTESIAN_POINT ( 'NONE',  ( 10.00000000000000000, 32.11449294037196012, 54.20017844242522642 ) ) ;
#2758=AXIS2_PLACEMENT_3D ( 'NONE', #12017, #16041, #13100 ) ;
#2763=ORIENTED_EDGE ( 'NONE', *, *, #14780, .F. ) ;
#2765=DIRECTION ( 'NONE',  ( 0.000000000000000000, 0.000000000000000000, 1.000000000000000000 ) ) ;
#2766=DIRECTION ( 'NONE',  ( -1.000000000000000000, 0.000000000000000000, -0.000000000000000000 ) ) ;
#2779=ADVANCED_FACE ( 'NONE', ( #11603 ), #15798, .T. ) ;
#2780=ORIENTED_EDGE ( 'NONE', *, *, #12189, .T. ) ;
#2791=FACE_OUTER_BOUND ( 'NONE', #2398, .T. ) ;
#2793=ADVANCED_FACE ( 'NONE', ( #15885 ), #10256, .T. ) ;
#2795=CARTESIAN_POINT ( 'NONE',  ( 10.00000000000000000, 0.000000000000000000, 0.000000000000000000 ) ) ;
#2796=ORIENTED_EDGE ( 'NONE', *, *, #13436, .T. ) ;
#2798=ADVANCED_FACE ( 'NONE', ( #18561 ), #14279, .T. ) ;
#2799=DIRECTION ( 'NONE',  ( 1.000000000000000000, 0.000000000000000000, 0.000000000000000000 ) ) ;
#2800=VERTEX_POINT ( 'NONE', #9981 ) ;
#2802=AXIS2_PLACEMENT_3D ( 'NONE', #11320, #18569, #11029 ) ;
#2806=DIRECTION ( 'NONE',  ( -1.000000000000000000, 0.000000000000000000, -0.000000000000000000 ) ) ;
#2807=CIRCLE ( 'NONE', #5228, 24.00000000002399858 ) ;
#2810=AXIS2_PLACEMENT_3D ( 'NONE', #16094, #10183, #1803 ) ;
#2823=VECTOR ( 'NONE', #17528, 1000.000000000000000 ) ;
#2828=EDGE_CURVE ( 'NONE', #8859, #15153, #14572, .T. ) ;
#2831=ORIENTED_EDGE ( 'NONE', *, *, #4665, .T. ) ;
#2832=DIRECTION ( 'NONE',  ( 0.000000000000000000, 0.000000000000000000, 1.000000000000000000 ) ) ;
#2835=CARTESIAN_POINT ( 'NONE',  ( 10.00000000000000000, 1.335003989221626997, 56.23315539212691050 ) ) ;
#2838=ORIENTED_EDGE ( 'NONE', *, *, #5867, .T. ) ;
#2839=CYLINDRICAL_SURFACE ( 'NONE', #5691, 24.00000000002399858 ) ;
#2840=( LENGTH_UNIT ( ) NAMED_UNIT ( * ) SI_UNIT ( .MILLI., .METRE. ) );
#2842=AXIS2_PLACEMENT_3D ( 'NONE', #638, #2156, #16353 ) ;
#2848=ORIENTED_EDGE ( 'NONE', *, *, #12889, .F. ) ;
#2849=EDGE_CURVE ( 'NONE', #18692, #2244, #16352, .T. ) ;
#2850=AXIS2_PLACEMENT_3D ( 'NONE', #10051, #5773, #14705 ) ;
#2852=ORIENTED_EDGE ( 'NONE', *, *, #16913, .T. ) ;
#2853=CYLINDRICAL_SURFACE ( 'NONE', #11146, 63.00000000006298961 ) ;
#2859=DIRECTION ( 'NONE',  ( -1.000000000000000000, 0.000000000000000000, 0.000000000000000000 ) ) ;
#2869=CIRCLE ( 'NONE', #17462, 24.00000000002399858 ) ;
#2872=CYLINDRICAL_SURFACE ( 'NONE', #6888, 63.00000000006298961 ) ;
#2879=CARTESIAN_POINT ( 'NONE',  ( 10.00000000000000000, -58.55669782892444175, -23.24033432160499757 ) ) ;
#2882=ORIENTED_EDGE ( 'NONE', *, *, #17547, .T. ) ;
#2884=FACE_OUTER_BOUND ( 'NONE', #6510, .T. ) ;
#2886=ORIENTED_EDGE ( 'NONE', *, *, #17266, .F. ) ;
#2889=CIRCLE ( 'NONE', #5317, 56.24900000005627021 ) ;
#2890=AXIS2_PLACEMENT_3D ( 'NONE', #11013, #9499, #3505 ) ;
#2892=DIRECTION ( 'NONE',  ( 0.000000000000000000, 0.000000000000000000, 1.000000000000000000 ) ) ;
#2893=DIRECTION ( 'NONE',  ( 0.000000000000000000, 0.000000000000000000, -1.000000000000000000 ) ) ;
#2900=AXIS2_PLACEMENT_3D ( 'NONE', #3477, #9373, #915 ) ;
#2901=DIRECTION ( 'NONE',  ( -1.000000000000000000, -0.000000000000000000, 0.000000000000000000 ) ) ;
#2905=VECTOR ( 'NONE', #17759, 1000.000000000000000 ) ;
#2908=CARTESIAN_POINT ( 'NONE',  ( 10.00000000000000000, 56.37237871411034007, 1.017308535512583711 ) ) ;
#2909=ORIENTED_EDGE ( 'NONE', *, *, #18022, .F. ) ;
#2910=VECTOR ( 'NONE', #11965, 1000.000000000000000 ) ;
#2915=AXIS2_PLACEMENT_3D ( 'NONE', #11642, #13079, #11913 ) ;
#2916=VERTEX_POINT ( 'NONE', #9194 ) ;
#2917=CARTESIAN_POINT ( 'NONE',  ( 0.000000000000000000, -24.68609584167194981, 50.69000562871634230 ) ) ;
#2920=ORIENTED_EDGE ( 'NONE', *, *, #9059, .F. ) ;
#2924=AXIS2_PLACEMENT_3D ( 'NONE', #6711, #3754, #18037 ) ;
#2926=ORIENTED_EDGE ( 'NONE', *, *, #17885, .F. ) ;
#2928=FACE_OUTER_BOUND ( 'NONE', #4526, .T. ) ;
#2931=EDGE_LOOP ( 'NONE', ( #11354, #3267, #8279, #6111 ) ) ;
#2936=ADVANCED_FACE ( 'NONE', ( #3116 ), #11961, .T. ) ;
#2937=ADVANCED_FACE ( 'NONE', ( #14727 ), #7487, .T. ) ;
#2938=APPLICATION_CONTEXT ( 'automotive_design' ) ;
#2943=ORIENTED_EDGE ( 'NONE', *, *, #9943, .T. ) ;
#2944=EDGE_CURVE ( 'NONE', #15698, #10240, #10229, .T. ) ;
#2945=AXIS2_PLACEMENT_3D ( 'NONE', #17447, #8680, #8948 ) ;
#2946=CIRCLE ( 'NONE', #3547, 2.649999999999999467 ) ;
#2952=DIRECTION ( 'NONE',  ( -1.000000000000000000, 0.000000000000000000, 0.000000000000000000 ) ) ;
#2956=CARTESIAN_POINT ( 'NONE',  ( 0.000000000000000000, 0.000000000000000000, 0.000000000000000000 ) ) ;
#2958=VERTEX_POINT ( 'NONE', #7584 ) ;
#2960=DIRECTION ( 'NONE',  ( 0.000000000000000000, 0.000000000000000000, 1.000000000000000000 ) ) ;
#2961=ORIENTED_EDGE ( 'NONE', *, *, #5295, .T. ) ;
#2963=FACE_BOUND ( 'NONE', #3551, .T. ) ;
#2964=VECTOR ( 'NONE', #9303, 1000.000000000000000 ) ;
#2967=ADVANCED_FACE ( 'NONE', ( #12053 ), #8154, .T. ) ;
#2971=EDGE_CURVE ( 'NONE', #17712, #12431, #4166, .T. ) ;
#2976=ORIENTED_EDGE ( 'NONE', *, *, #10641, .T. ) ;
#2982=CYLINDRICAL_SURFACE ( 'NONE', #7655, 2.649999999999999467 ) ;
#2985=VERTEX_POINT ( 'NONE', #11192 ) ;
#2995=AXIS2_PLACEMENT_3D ( 'NONE', #6407, #13467, #504 ) ;
#2998=FACE_OUTER_BOUND ( 'NONE', #18263, .T. ) ;
#2999=FACE_OUTER_BOUND ( 'NONE', #10741, .T. ) ;
#3007=CARTESIAN_POINT ( 'NONE',  ( 10.00000000000000178, 3.673940397442059178E-15, -30.00000000000000000 ) ) ;
#3010=VECTOR ( 'NONE', #5639, 1000.000000000000000 ) ;
#3016=AXIS2_PLACEMENT_3D ( 'NONE', #12218, #993, #8022 ) ;
#3017=EDGE_CURVE ( 'NONE', #9182, #10921, #3548, .T. ) ;
#3024=CARTESIAN_POINT ( 'NONE',  ( 0.000000000000000000, 9.823366686500662581, 55.51919907100656104 ) ) ;
#3030=DIRECTION ( 'NONE',  ( -1.000000000000000000, 0.000000000000000000, 0.000000000000000000 ) ) ;
#3034=CARTESIAN_POINT ( 'NONE',  ( 10.00000000000000000, 0.000000000000000000, 0.000000000000000000 ) ) ;
#3041=CIRCLE ( 'NONE', #5481, 24.00000000002399858 ) ;
#3043=AXIS2_PLACEMENT_3D ( 'NONE', #16223, #7277, #47 ) ;
#3047=LINE ( 'NONE', #5894, #5084 ) ;
#3048=VERTEX_POINT ( 'NONE', #13772 ) ;
#3054=CARTESIAN_POINT ( 'NONE',  ( 0.000000000000000000, -49.49802920186242261, 26.71881558261711831 ) ) ;
#3058=CARTESIAN_POINT ( 'NONE',  ( 10.00000000000000000, 31.97297851452492168, -46.27827401617368963 ) ) ;
#3060=CIRCLE ( 'NONE', #10663, 24.00000000002400569 ) ;
#3061=EDGE_CURVE ( 'NONE', #6013, #17928, #14779, .T. ) ;
#3065=ORIENTED_EDGE ( 'NONE', *, *, #14566, .F. ) ;
#3066=CARTESIAN_POINT ( 'NONE',  ( 10.00000000000000000, 46.27827401617449965, -31.97297851452373507 ) ) ;
#3067=EDGE_CURVE ( 'NONE', #12641, #10237, #8048, .T. ) ;
#3068=CARTESIAN_POINT ( 'NONE',  ( 5.000000000000000000, -58.55669782892444886, -23.24033432160501178 ) ) ;
#3069=EDGE_CURVE ( 'NONE', #5083, #18009, #8702, .T. ) ;
#3073=CARTESIAN_POINT ( 'NONE',  ( -10.00000000000000000, 26.45033635316149301, 36.40576474687247099 ) ) ;
#3084=AXIS2_PLACEMENT_3D ( 'NONE', #7754, #7951, #15109 ) ;
#3088=CYLINDRICAL_SURFACE ( 'NONE', #13932, 63.00000000006298961 ) ;
#3091=DIRECTION ( 'NONE',  ( -1.000000000000000000, 0.000000000000000000, 0.000000000000000000 ) ) ;
#3092=CARTESIAN_POINT ( 'NONE',  ( 0.000000000000000000, -40.70683587897930522, -38.81885513160031564 ) ) ;
#3093=DIRECTION ( 'NONE',  ( 0.000000000000000000, 0.000000000000000000, -1.000000000000000000 ) ) ;
#3097=LINE ( 'NONE', #1482, #113 ) ;
#3099=EDGE_LOOP ( 'NONE', ( #3131, #12412, #7674, #13034 ) ) ;
#3100=VERTEX_POINT ( 'NONE', #12529 ) ;
#3102=DIRECTION ( 'NONE',  ( 0.000000000000000000, 0.000000000000000000, 1.000000000000000000 ) ) ;
#3105=FACE_OUTER_BOUND ( 'NONE', #16753, .T. ) ;
#3106=VERTEX_POINT ( 'NONE', #5671 ) ;
#3108=DIRECTION ( 'NONE',  ( 0.000000000000000000, 0.000000000000000000, 1.000000000000000000 ) ) ;
#3109=AXIS2_PLACEMENT_3D ( 'NONE', #17950, #15475, #8032 ) ;
#3113=VERTEX_POINT ( 'NONE', #8706 ) ;
#3114=CARTESIAN_POINT ( 'NONE',  ( 10.00000000000000000, -54.20017844242534011, 32.11449294037175406 ) ) ;
#3116=FACE_OUTER_BOUND ( 'NONE', #3709, .T. ) ;
#3123=VERTEX_POINT ( 'NONE', #13007 ) ;
#3124=CARTESIAN_POINT ( 'NONE',  ( 0.000000000000000000, -24.97244012287460535, -57.83923611457346681 ) ) ;
#3131=ORIENTED_EDGE ( 'NONE', *, *, #11068, .T. ) ;
#3134=DIRECTION ( 'NONE',  ( -1.000000000000000000, -0.000000000000000000, 0.000000000000000000 ) ) ;
#3140=DIRECTION ( 'NONE',  ( 0.000000000000000000, -0.9510565162951565288, 0.3090169943749383474 ) ) ;
#3141=CARTESIAN_POINT ( 'NONE',  ( 0.000000000000000000, 45.00825343885067298, -33.95787273855199828 ) ) ;
#3152=CARTESIAN_POINT ( 'NONE',  ( 10.00000000000000000, -16.10733642026522006, 53.89344778774807310 ) ) ;
#3153=ORIENTED_EDGE ( 'NONE', *, *, #2185, .T. ) ;
#3160=VERTEX_POINT ( 'NONE', #14516 ) ;
#3164=ORIENTED_EDGE ( 'NONE', *, *, #9412, .F. ) ;
#3166=EDGE_CURVE ( 'NONE', #4962, #11121, #8096, .T. ) ;
#3167=ADVANCED_FACE ( 'NONE', ( #8617 ), #14144, .T. ) ;
#3168=ORIENTED_EDGE ( 'NONE', *, *, #16807, .F. ) ;
#3174=DIRECTION ( 'NONE',  ( 0.000000000000000000, 0.000000000000000000, 1.000000000000000000 ) ) ;
#3176=ADVANCED_FACE ( 'NONE', ( #4254 ), #15863, .T. ) ;
#3177=LINE ( 'NONE', #8356, #12393 ) ;
#3180=DIRECTION ( 'NONE',  ( -1.000000000000000000, -0.000000000000000000, -0.000000000000000000 ) ) ;
#3181=ORIENTED_EDGE ( 'NONE', *, *, #7944, .T. ) ;
#3182=FACE_OUTER_BOUND ( 'NONE', #12508, .T. ) ;
#3183=EDGE_CURVE ( 'NONE', #6177, #10381, #12970, .T. ) ;
#3184=CARTESIAN_POINT ( 'NONE',  ( 10.00000000000000000, -49.76630880786289879, -26.49895292618059273 ) ) ;
#3189=LINE ( 'NONE', #13287, #9606 ) ;
#3192=CARTESIAN_POINT ( 'NONE',  ( 10.00000000000000000, -53.22058882792220658, 33.71303790549256263 ) ) ;
#3193=VERTEX_POINT ( 'NONE', #1207 ) ;
#3194=VECTOR ( 'NONE', #17698, 1000.000000000000000 ) ;
#3198=EDGE_CURVE ( 'NONE', #16109, #6670, #4429, .T. ) ;
#3200=CARTESIAN_POINT ( 'NONE',  ( 10.00000000000000000, -53.92768374110902840, 16.45250512421837641 ) ) ;
#3201=ADVANCED_FACE ( 'NONE', ( #9859 ), #14337, .T. ) ;
#3205=VERTEX_POINT ( 'NONE', #12820 ) ;
#3210=FACE_OUTER_BOUND ( 'NONE', #1680, .T. ) ;
#3212=ORIENTED_EDGE ( 'NONE', *, *, #896, .T. ) ;
#3213=LINE ( 'NONE', #9010, #2910 ) ;
#3217=AXIS2_PLACEMENT_3D ( 'NONE', #10704, #6234, #14814 ) ;
#3220=EDGE_CURVE ( 'NONE', #17928, #1108, #18438, .T. ) ;
#3223=DIRECTION ( 'NONE',  ( 0.000000000000000000, 0.000000000000000000, 1.000000000000000000 ) ) ;
#3224=DIRECTION ( 'NONE',  ( 0.000000000000000000, 0.000000000000000000, 1.000000000000000000 ) ) ;
#3226=AXIS2_PLACEMENT_3D ( 'NONE', #6860, #4018, #9819 ) ;
#3232=AXIS2_PLACEMENT_3D ( 'NONE', #12714, #4988, #9378 ) ;
#3234=VERTEX_POINT ( 'NONE', #15773 ) ;
#3241=EDGE_CURVE ( 'NONE', #16413, #16577, #5359, .T. ) ;
#3242=AXIS2_PLACEMENT_3D ( 'NONE', #8015, #12119, #13555 ) ;
#3244=AXIS2_PLACEMENT_3D ( 'NONE', #2382, #6575, #12381 ) ;
#3249=DIRECTION ( 'NONE',  ( -1.000000000000000000, -0.000000000000000000, -0.000000000000000000 ) ) ;
#3252=CIRCLE ( 'NONE', #8425, 24.00000000002399858 ) ;
#3255=DIRECTION ( 'NONE',  ( -1.000000000000000000, -0.000000000000000000, 0.000000000000000000 ) ) ;
#3256=ORIENTED_EDGE ( 'NONE', *, *, #13395, .T. ) ;
#3258=DIRECTION ( 'NONE',  ( 0.000000000000000000, 0.000000000000000000, 1.000000000000000000 ) ) ;
#3262=EDGE_CURVE ( 'NONE', #3665, #8441, #14904, .T. ) ;
#3263=ORIENTED_EDGE ( 'NONE', *, *, #17390, .T. ) ;
#3267=ORIENTED_EDGE ( 'NONE', *, *, #14108, .T. ) ;
#3272=AXIS2_PLACEMENT_3D ( 'NONE', #11356, #14219, #9744 ) ;
#3273=FACE_OUTER_BOUND ( 'NONE', #7411, .T. ) ;
#3274=DIRECTION ( 'NONE',  ( -1.000000000000000000, -0.000000000000000000, -0.000000000000000000 ) ) ;
#3282=DIRECTION ( 'NONE',  ( 0.000000000000000000, 0.000000000000000000, 1.000000000000000000 ) ) ;
#3283=FACE_OUTER_BOUND ( 'NONE', #15647, .T. ) ;
#3284=ORIENTED_EDGE ( 'NONE', *, *, #9923, .T. ) ;
#3285=VERTEX_POINT ( 'NONE', #3007 ) ;
#3292=AXIS2_PLACEMENT_3D ( 'NONE', #794, #18505, #6600 ) ;
#3297=CARTESIAN_POINT ( 'NONE',  ( 5.000000000000000000, 61.03368945066435458, 15.61693798565518065 ) ) ;
#3298=ORIENTED_EDGE ( 'NONE', *, *, #18213, .T. ) ;
#3309=EDGE_CURVE ( 'NONE', #9576, #3525, #10215, .T. ) ;
#3312=CYLINDRICAL_SURFACE ( 'NONE', #3435, 63.00000000006298961 ) ;
#3315=DIRECTION ( 'NONE',  ( -1.000000000000000000, -0.000000000000000000, 0.000000000000000000 ) ) ;
#3318=ORIENTED_EDGE ( 'NONE', *, *, #5395, .T. ) ;
#3319=DIRECTION ( 'NONE',  ( 0.000000000000000000, 0.000000000000000000, 1.000000000000000000 ) ) ;
#3321=VECTOR ( 'NONE', #10379, 1000.000000000000000 ) ;
#3322=AXIS2_PLACEMENT_3D ( 'NONE', #10512, #16332, #149 ) ;
#3324=CIRCLE ( 'NONE', #5448, 56.24900000005626310 ) ;
#3327=EDGE_LOOP ( 'NONE', ( #1416, #15430, #9342, #5545 ) ) ;
#3328=AXIS2_PLACEMENT_3D ( 'NONE', #18509, #5470, #11360 ) ;
#3331=DIRECTION ( 'NONE',  ( 0.000000000000000000, 0.000000000000000000, 1.000000000000000000 ) ) ;
#3332=CARTESIAN_POINT ( 'NONE',  ( 10.00000000000000000, -26.49895292617967257, -49.76630880786338196 ) ) ;
#3335=ADVANCED_FACE ( 'NONE', ( #3182 ), #11851, .T. ) ;
#3337=DIRECTION ( 'NONE',  ( -1.000000000000000000, 0.000000000000000000, -0.000000000000000000 ) ) ;
#3344=CARTESIAN_POINT ( 'NONE',  ( 0.000000000000000000, 61.03368945066435458, 15.61693798565518421 ) ) ;
#3349=ORIENTED_EDGE ( 'NONE', *, *, #7624, .T. ) ;
#3351=ORIENTED_EDGE ( 'NONE', *, *, #12168, .T. ) ;
#3352=CARTESIAN_POINT ( 'NONE',  ( 0.000000000000000000, -53.92768374110902840, 16.45250512421837641 ) ) ;
#3353=DIRECTION ( 'NONE',  ( 0.000000000000000000, 0.000000000000000000, 1.000000000000000000 ) ) ;
#3355=CARTESIAN_POINT ( 'NONE',  ( 5.000000000000000000, 41.62350880771921169, 47.29147401531970019 ) ) ;
#3356=ORIENTED_EDGE ( 'NONE', *, *, #6693, .T. ) ;
#3358=ORIENTED_EDGE ( 'NONE', *, *, #7325, .T. ) ;
#3359=DIRECTION ( 'NONE',  ( 0.000000000000000000, -0.5877852522924622569, -0.8090169943749552228 ) ) ;
#3360=VERTEX_POINT ( 'NONE', #14799 ) ;
#3361=ADVANCED_FACE ( 'NONE', ( #1749 ), #13384, .T. ) ;
#3362=ORIENTED_EDGE ( 'NONE', *, *, #11569, .F. ) ;
#3364=ORIENTED_EDGE ( 'NONE', *, *, #5872, .T. ) ;
#3365=AXIS2_PLACEMENT_3D ( 'NONE', #2298, #18684, #12886 ) ;
#3367=CARTESIAN_POINT ( 'NONE',  ( 10.00000000000000000, -24.68609584167194981, 50.69000562871634230 ) ) ;
#3370=CARTESIAN_POINT ( 'NONE',  ( 5.000000000000000000, -41.62350880771888484, -47.29147401531999861 ) ) ;
#3375=EDGE_LOOP ( 'NONE', ( #6819, #11602, #8987, #13775 ) ) ;
#3386=EDGE_LOOP ( 'NONE', ( #16072, #1648, #4851, #3697 ) ) ;
#3392=AXIS2_PLACEMENT_3D ( 'NONE', #4713, #347, #13400 ) ;
#3393=VERTEX_POINT ( 'NONE', #8489 ) ;
#3401=ORIENTED_EDGE ( 'NONE', *, *, #12, .F. ) ;
#3404=ORIENTED_EDGE ( 'NONE', *, *, #17059, .T. ) ;
#3406=AXIS2_PLACEMENT_3D ( 'NONE', #5082, #4984, #11071 ) ;
#3407=EDGE_CURVE ( 'NONE', #17793, #14080, #4739, .T. ) ;
#3409=AXIS2_PLACEMENT_3D ( 'NONE', #14852, #11536, #17429 ) ;
#3411=ADVANCED_FACE ( 'NONE', ( #11250 ), #15443, .T. ) ;
#3413=ADVANCED_FACE ( 'NONE', ( #14099 ), #1060, .T. ) ;
#3426=CARTESIAN_POINT ( 'NONE',  ( 10.00000000000000000, -7.478235706489372525, 55.74967257055880054 ) ) ;
#3427=AXIS2_PLACEMENT_3D ( 'NONE', #8658, #1699, #14 ) ;
#3432=ADVANCED_FACE ( 'NONE', ( #13663 ), #10694, .T. ) ;
#3435=AXIS2_PLACEMENT_3D ( 'NONE', #13689, #18052, #10806 ) ;
#3447=DIRECTION ( 'NONE',  ( -1.000000000000000000, -0.000000000000000000, 0.000000000000000000 ) ) ;
#3450=DIRECTION ( 'NONE',  ( -1.000000000000000000, -0.000000000000000000, -0.000000000000000000 ) ) ;
#3455=ORIENTED_EDGE ( 'NONE', *, *, #16189, .T. ) ;
#3456=ORIENTED_EDGE ( 'NONE', *, *, #1827, .F. ) ;
#3459=CARTESIAN_POINT ( 'NONE',  ( 10.00000000000000000, -49.76630880786289879, -26.49895292618059273 ) ) ;
#3460=EDGE_CURVE ( 'NONE', #1496, #7847, #2309, .T. ) ;
#3464=DIRECTION ( 'NONE',  ( 1.000000000000000000, -0.000000000000000000, 0.000000000000000000 ) ) ;
#3467=VERTEX_POINT ( 'NONE', #4977 ) ;
#3471=FACE_OUTER_BOUND ( 'NONE', #10173, .T. ) ;
#3472=CARTESIAN_POINT ( 'NONE',  ( 10.00000000000000000, -53.92768374110879392, -16.45250512421912603 ) ) ;
#3474=ORIENTED_EDGE ( 'NONE', *, *, #10728, .T. ) ;
#3475=CARTESIAN_POINT ( 'NONE',  ( 10.00000000000000000, 0.000000000000000000, 0.000000000000000000 ) ) ;
#3477=CARTESIAN_POINT ( 'NONE',  ( 10.00000000000000000, 0.000000000000000000, 0.000000000000000000 ) ) ;
#3479=EDGE_CURVE ( 'NONE', #2331, #7064, #14303, .T. ) ;
#3480=EDGE_CURVE ( 'NONE', #3687, #5915, #7800, .T. ) ;
#3483=CYLINDRICAL_SURFACE ( 'NONE', #8141, 2.649999999999999467 ) ;
#3491=CYLINDRICAL_SURFACE ( 'NONE', #2218, 63.00000000006298961 ) ;
#3492=VERTEX_POINT ( 'NONE', #16603 ) ;
#3494=AXIS2_PLACEMENT_3D ( 'NONE', #9807, #17150, #13049 ) ;
#3500=VECTOR ( 'NONE', #16543, 1000.000000000000000 ) ;
#3502=ORIENTED_EDGE ( 'NONE', *, *, #4839, .T. ) ;
#3505=DIRECTION ( 'NONE',  ( 0.000000000000000000, 0.8090169943749444537, 0.5877852522924772449 ) ) ;
#3512=EDGE_LOOP ( 'NONE', ( #12651, #7480, #13628, #17404 ) ) ;
#3516=EDGE_CURVE ( 'NONE', #7464, #15934, #5050, .T. ) ;
#3519=FACE_OUTER_BOUND ( 'NONE', #14329, .T. ) ;
#3524=VECTOR ( 'NONE', #16046, 1000.000000000000000 ) ;
#3525=VERTEX_POINT ( 'NONE', #1345 ) ;
#3535=ORIENTED_EDGE ( 'NONE', *, *, #18177, .F. ) ;
#3536=CARTESIAN_POINT ( 'NONE',  ( 4.999999999999999112, -62.87238730325623948, 4.007856633823172032 ) ) ;
#3540=DIRECTION ( 'NONE',  ( -1.000000000000000000, 0.000000000000000000, -0.000000000000000000 ) ) ;
#3541=EDGE_LOOP ( 'NONE', ( #13369, #12246, #7203, #16130 ) ) ;
#3542=AXIS2_PLACEMENT_3D ( 'NONE', #3849, #12226, #10888 ) ;
#3545=EDGE_CURVE ( 'NONE', #4094, #15091, #5815, .T. ) ;
#3547=AXIS2_PLACEMENT_3D ( 'NONE', #2118, #693, #12297 ) ;
#3548=CIRCLE ( 'NONE', #16620, 63.00000000006298961 ) ;
#3551=EDGE_LOOP ( 'NONE', ( #12645, #15066 ) ) ;
#3554=DIRECTION ( 'NONE',  ( 0.000000000000000000, -0.3090169943749547787, 0.9510565162951511997 ) ) ;
#3555=CIRCLE ( 'NONE', #1438, 56.24900000005626310 ) ;
#3557=DIRECTION ( 'NONE',  ( 0.000000000000000000, 0.5877852522924685852, 0.8090169943749507819 ) ) ;
#3562=LINE ( 'NONE', #6217, #4642 ) ;
#3563=CIRCLE ( 'NONE', #7209, 24.00000000002400569 ) ;
#3569=CARTESIAN_POINT ( 'NONE',  ( -10.00000000000000000, 0.000000000000000000, 0.000000000000000000 ) ) ;
#3573=ORIENTED_EDGE ( 'NONE', *, *, #3753, .T. ) ;
#3574=CYLINDRICAL_SURFACE ( 'NONE', #4756, 63.00000000006298961 ) ;
#3576=FACE_OUTER_BOUND ( 'NONE', #7469, .T. ) ;
#3579=EDGE_CURVE ( 'NONE', #13137, #2157, #12661, .T. ) ;
#3580=AXIS2_PLACEMENT_3D ( 'NONE', #10279, #16091, #8843 ) ;
#3583=DIRECTION ( 'NONE',  ( -1.000000000000000000, -0.000000000000000000, -0.000000000000000000 ) ) ;
#3586=ORIENTED_EDGE ( 'NONE', *, *, #13463, .F. ) ;
#3590=DIRECTION ( 'NONE',  ( 0.000000000000000000, 0.000000000000000000, 1.000000000000000000 ) ) ;
#3594=CIRCLE ( 'NONE', #2995, 56.24900000005625600 ) ;
#3595=ORIENTED_EDGE ( 'NONE', *, *, #17059, .F. ) ;
#3596=EDGE_LOOP ( 'NONE', ( #3401, #14385, #5873, #4656 ) ) ;
#3598=FACE_OUTER_BOUND ( 'NONE', #5239, .T. ) ;
#3602=AXIS2_PLACEMENT_3D ( 'NONE', #2235, #5096, #6523 ) ;
#3606=CIRCLE ( 'NONE', #16988, 56.24900000005627732 ) ;
#3607=ORIENTED_EDGE ( 'NONE', *, *, #12237, .T. ) ;
#3610=CARTESIAN_POINT ( 'NONE',  ( 10.00000000000000000, -4.007856633822949988, -62.87238730325625369 ) ) ;
#3612=EDGE_CURVE ( 'NONE', #3711, #12567, #503, .T. ) ;
#3619=ORIENTED_EDGE ( 'NONE', *, *, #6778, .F. ) ;
#3620=CARTESIAN_POINT ( 'NONE',  ( 0.000000000000000000, -56.23315539212689629, -1.335003989222221410 ) ) ;
#3624=ORIENTED_EDGE ( 'NONE', *, *, #2685, .T. ) ;
#3627=CIRCLE ( 'NONE', #14873, 56.24900000005625600 ) ;
#3630=VECTOR ( 'NONE', #17416, 1000.000000000000000 ) ;
#3636=FACE_OUTER_BOUND ( 'NONE', #17621, .T. ) ;
#3637=LINE ( 'NONE', #16777, #15094 ) ;
#3638=ORIENTED_EDGE ( 'NONE', *, *, #7805, .F. ) ;
#3645=VERTEX_POINT ( 'NONE', #17795 ) ;
#3647=ADVANCED_FACE ( 'NONE', ( #13713 ), #568, .T. ) ;
#3651=AXIS2_PLACEMENT_3D ( 'NONE', #8344, #10657, #16472 ) ;
#3655=EDGE_CURVE ( 'NONE', #12204, #4722, #1704, .T. ) ;
#3657=DIRECTION ( 'NONE',  ( -1.000000000000000000, -0.000000000000000000, -0.000000000000000000 ) ) ;
#3661=ORIENTED_EDGE ( 'NONE', *, *, #16329, .F. ) ;
#3662=CARTESIAN_POINT ( 'NONE',  ( 0.000000000000000000, 10.11537145609375443, 55.33199130079787409 ) ) ;
#3665=VERTEX_POINT ( 'NONE', #9035 ) ;
#3669=VERTEX_POINT ( 'NONE', #3426 ) ;
#3671=AXIS2_PLACEMENT_3D ( 'NONE', #1644, #3274, #7361 ) ;
#3674=DIRECTION ( 'NONE',  ( 0.000000000000000000, 0.000000000000000000, 1.000000000000000000 ) ) ;
#3678=DIRECTION ( 'NONE',  ( -1.000000000000000000, -0.000000000000000000, -0.000000000000000000 ) ) ;
#3681=DIRECTION ( 'NONE',  ( -1.000000000000000000, 0.000000000000000000, 0.000000000000000000 ) ) ;
#3683=EDGE_CURVE ( 'NONE', #12720, #8736, #12354, .T. ) ;
#3684=AXIS2_PLACEMENT_3D ( 'NONE', #13441, #13876, #16838 ) ;
#3687=VERTEX_POINT ( 'NONE', #7793 ) ;
#3688=VERTEX_POINT ( 'NONE', #3620 ) ;
#3689=DIRECTION ( 'NONE',  ( 0.000000000000000000, -1.000000000000000000, -1.047444401652940007E-14 ) ) ;
#3696=CARTESIAN_POINT ( 'NONE',  ( 0.000000000000000000, 33.71303790549351476, -53.22058882792159551 ) ) ;
#3697=ORIENTED_EDGE ( 'NONE', *, *, #11094, .T. ) ;
#3701=DIRECTION ( 'NONE',  ( 0.000000000000000000, 0.8910065241883688980, -0.4539904997395446951 ) ) ;
#3704=EDGE_CURVE ( 'NONE', #8362, #11459, #16475, .T. ) ;
#3706=CARTESIAN_POINT ( 'NONE',  ( 0.000000000000000000, 0.000000000000000000, 0.000000000000000000 ) ) ;
#3708=VERTEX_POINT ( 'NONE', #4941 ) ;
#3709=EDGE_LOOP ( 'NONE', ( #8045, #7943, #2126, #3181 ) ) ;
#3711=VERTEX_POINT ( 'NONE', #16556 ) ;
#3718=ADVANCED_FACE ( 'NONE', ( #2268 ), #15608, .T. ) ;
#3724=CYLINDRICAL_SURFACE ( 'NONE', #13903, 24.00000000002399858 ) ;
#3726=CARTESIAN_POINT ( 'NONE',  ( 0.000000000000000000, 42.79754323328179311, -16.55576474687299537 ) ) ;
#3727=CARTESIAN_POINT ( 'NONE',  ( 0.000000000000000000, -34.13306034420217827, 44.70888270294149436 ) ) ;
#3728=EDGE_LOOP ( 'NONE', ( #5591, #5202, #10031, #15195 ) ) ;
#3729=LINE ( 'NONE', #3536, #13656 ) ;
#3732=VERTEX_POINT ( 'NONE', #6556 ) ;
#3734=ORIENTED_EDGE ( 'NONE', *, *, #16685, .F. ) ;
#3736=VECTOR ( 'NONE', #7421, 1000.000000000000000 ) ;
#3744=DIRECTION ( 'NONE',  ( -1.000000000000000000, 0.000000000000000000, 0.000000000000000000 ) ) ;
#3746=LINE ( 'NONE', #18399, #9996 ) ;
#3752=AXIS2_PLACEMENT_3D ( 'NONE', #13716, #11986, #16559 ) ;
#3753=EDGE_CURVE ( 'NONE', #18350, #4490, #9626, .T. ) ;
#3754=DIRECTION ( 'NONE',  ( 1.000000000000000000, 0.000000000000000000, 0.000000000000000000 ) ) ;
#3756=DIRECTION ( 'NONE',  ( 0.000000000000000000, 0.000000000000000000, -1.000000000000000000 ) ) ;
#3768=ORIENTED_EDGE ( 'NONE', *, *, #4807, .T. ) ;
#3772=DIRECTION ( 'NONE',  ( -1.000000000000000000, 0.000000000000000000, 0.000000000000000000 ) ) ;
#3774=ORIENTED_EDGE ( 'NONE', *, *, #2555, .T. ) ;
#3777=CARTESIAN_POINT ( 'NONE',  ( 10.00000000000000000, 46.20417134726132247, 32.31183295104789011 ) ) ;
#3784=CARTESIAN_POINT ( 'NONE',  ( 0.000000000000000000, 32.31183295104839459, -46.20417134726096009 ) ) ;
#3792=CARTESIAN_POINT ( 'NONE',  ( 10.00000000000000000, 50.71018745830478736, -24.33982105418846942 ) ) ;
#3794=DIRECTION ( 'NONE',  ( -1.000000000000000000, -0.000000000000000000, 0.000000000000000000 ) ) ;
#3795=DIRECTION ( 'NONE',  ( 0.000000000000000000, 0.000000000000000000, 1.000000000000000000 ) ) ;
#3796=ORIENTED_EDGE ( 'NONE', *, *, #12383, .F. ) ;
#3797=ORIENTED_EDGE ( 'NONE', *, *, #7458, .F. ) ;
#3798=ORIENTED_EDGE ( 'NONE', *, *, #2685, .F. ) ;
#3804=EDGE_CURVE ( 'NONE', #16545, #11178, #1132, .T. ) ;
#3807=EDGE_LOOP ( 'NONE', ( #8476, #5920, #10354, #6113 ) ) ;
#3808=DIRECTION ( 'NONE',  ( 1.000000000000000000, -0.000000000000000000, 0.000000000000000000 ) ) ;
#3810=FACE_OUTER_BOUND ( 'NONE', #14253, .T. ) ;
#3811=DIRECTION ( 'NONE',  ( -1.000000000000000000, 0.000000000000000000, 0.000000000000000000 ) ) ;
#3814=DIRECTION ( 'NONE',  ( -1.000000000000000000, 0.000000000000000000, 0.000000000000000000 ) ) ;
#3815=AXIS2_PLACEMENT_3D ( 'NONE', #7500, #17693, #4643 ) ;
#3816=CYLINDRICAL_SURFACE ( 'NONE', #7792, 24.00000000002399858 ) ;
#3818=LINE ( 'NONE', #11045, #5135 ) ;
#3819=AXIS2_PLACEMENT_3D ( 'NONE', #1746, #14357, #9168 ) ;
#3822=ORIENTED_EDGE ( 'NONE', *, *, #2944, .T. ) ;
#3824=EDGE_CURVE ( 'NONE', #14293, #5713, #15322, .T. ) ;
#3831=DIRECTION ( 'NONE',  ( 1.000000000000000000, 0.000000000000000000, 0.000000000000000000 ) ) ;
#3832=CYLINDRICAL_SURFACE ( 'NONE', #5153, 24.00000000002399858 ) ;
#3833=CARTESIAN_POINT ( 'NONE',  ( 0.000000000000000000, -32.31183295104739273, -46.20417134726167063 ) ) ;
#3834=CARTESIAN_POINT ( 'NONE',  ( 10.00000000000000000, -53.29895248911688554, 18.38754094778222026 ) ) ;
#3836=CARTESIAN_POINT ( 'NONE',  ( 10.00000000000000000, 49.76630880786309064, 26.49895292618021614 ) ) ;
#3841=EDGE_CURVE ( 'NONE', #980, #15243, #18152, .T. ) ;
#3842=CIRCLE ( 'NONE', #16304, 24.00000000002400213 ) ;
#3843=FACE_OUTER_BOUND ( 'NONE', #17898, .T. ) ;
#3847=ORIENTED_EDGE ( 'NONE', *, *, #17063, .T. ) ;
#3848=VECTOR ( 'NONE', #12673, 1000.000000000000000 ) ;
#3849=CARTESIAN_POINT ( 'NONE',  ( 10.00000000000000000, 53.92768374110892893, -16.45250512421876010 ) ) ;
#3851=ADVANCED_FACE ( 'NONE', ( #2928 ), #8735, .T. ) ;
#3853=ORIENTED_EDGE ( 'NONE', *, *, #1557, .F. ) ;
#3854=AXIS2_PLACEMENT_3D ( 'NONE', #1518, #8566, #5530 ) ;
#3857=CARTESIAN_POINT ( 'NONE',  ( 10.00000000000000000, 56.37237871411034007, 25.01730853553658207 ) ) ;
#3858=CARTESIAN_POINT ( 'NONE',  ( 0.000000000000000000, 61.47135697633798657, -13.79392154159068262 ) ) ;
#3861=DIRECTION ( 'NONE',  ( 0.000000000000000000, 0.000000000000000000, 1.000000000000000000 ) ) ;
#3865=DIRECTION ( 'NONE',  ( -1.000000000000000000, -0.000000000000000000, -0.000000000000000000 ) ) ;
#3866=ORIENTED_EDGE ( 'NONE', *, *, #12739, .F. ) ;
#3867=CARTESIAN_POINT ( 'NONE',  ( 10.00000000000000000, 0.000000000000000000, 0.000000000000000000 ) ) ;
#3868=DIRECTION ( 'NONE',  ( -1.000000000000000000, 0.000000000000000000, 0.000000000000000000 ) ) ;
#3869=CARTESIAN_POINT ( 'NONE',  ( 10.00000000000000000, 0.000000000000000000, 0.000000000000000000 ) ) ;
#3870=AXIS2_PLACEMENT_3D ( 'NONE', #11885, #6458, #13612 ) ;
#3871=ORIENTED_EDGE ( 'NONE', *, *, #14108, .F. ) ;
#3872=ORIENTED_EDGE ( 'NONE', *, *, #6706, .T. ) ;
#3879=AXIS2_PLACEMENT_3D ( 'NONE', #16179, #3134, #6786 ) ;
#3881=EDGE_CURVE ( 'NONE', #445, #12447, #5882, .T. ) ;
#3882=EDGE_LOOP ( 'NONE', ( #17815, #1589, #7518, #2048 ) ) ;
#3887=VECTOR ( 'NONE', #11680, 1000.000000000000000 ) ;
#3892=CARTESIAN_POINT ( 'NONE',  ( 10.00000000000000000, 31.97297851452424311, 46.27827401617415148 ) ) ;
#3893=VERTEX_POINT ( 'NONE', #17229 ) ;
#3906=CARTESIAN_POINT ( 'NONE',  ( 10.00000000000000000, 0.000000000000000000, 0.000000000000000000 ) ) ;
#3910=AXIS2_PLACEMENT_3D ( 'NONE', #9951, #17193, #5663 ) ;
#3912=ORIENTED_EDGE ( 'NONE', *, *, #4023, .T. ) ;
#3914=CIRCLE ( 'NONE', #7546, 24.00000000002399858 ) ;
#3918=CARTESIAN_POINT ( 'NONE',  ( 10.00000000000000000, 45.00825343885067298, -33.95787273855199828 ) ) ;
#3919=DIRECTION ( 'NONE',  ( -1.000000000000000000, -0.000000000000000000, -0.000000000000000000 ) ) ;
#3926=VECTOR ( 'NONE', #18361, 1000.000000000000000 ) ;
#3928=ADVANCED_FACE ( 'NONE', ( #1408 ), #2839, .T. ) ;
#3929=DIRECTION ( 'NONE',  ( -1.000000000000000000, -0.000000000000000000, -0.000000000000000000 ) ) ;
#3930=DIRECTION ( 'NONE',  ( -1.000000000000000000, 0.000000000000000000, -0.000000000000000000 ) ) ;
#3936=ORIENTED_EDGE ( 'NONE', *, *, #18440, .F. ) ;
#3937=AXIS2_PLACEMENT_3D ( 'NONE', #15097, #812, #13574 ) ;
#3938=AXIS2_PLACEMENT_3D ( 'NONE', #5140, #876, #15434 ) ;
#3943=DIRECTION ( 'NONE',  ( 0.000000000000000000, 0.000000000000000000, 1.000000000000000000 ) ) ;
#3948=ORIENTED_EDGE ( 'NONE', *, *, #16216, .T. ) ;
#3949=LINE ( 'NONE', #15084, #17906 ) ;
#3951=EDGE_CURVE ( 'NONE', #9406, #3665, #16632, .T. ) ;
#3952=AXIS2_PLACEMENT_3D ( 'NONE', #6731, #1215, #4069 ) ;
#3953=DIRECTION ( 'NONE',  ( -1.000000000000000000, 0.000000000000000000, 0.000000000000000000 ) ) ;
#3955=ORIENTED_EDGE ( 'NONE', *, *, #5499, .T. ) ;
#3957=DIRECTION ( 'NONE',  ( -1.000000000000000000, 0.000000000000000000, -0.000000000000000000 ) ) ;
#3959=CARTESIAN_POINT ( 'NONE',  ( 0.000000000000000000, -56.37237871411034718, 1.017308535512174261 ) ) ;
#3960=VERTEX_POINT ( 'NONE', #13216 ) ;
#3962=DIRECTION ( 'NONE',  ( -1.000000000000000000, 0.000000000000000000, -0.000000000000000000 ) ) ;
#3965=DIRECTION ( 'NONE',  ( 0.000000000000000000, 0.000000000000000000, 1.000000000000000000 ) ) ;
#3970=CARTESIAN_POINT ( 'NONE',  ( 0.000000000000000000, 0.000000000000000000, 0.000000000000000000 ) ) ;
#3971=CARTESIAN_POINT ( 'NONE',  ( 5.000000000000000000, 48.50907078259382388, 40.19788616105627455 ) ) ;
#3972=ORIENTED_EDGE ( 'NONE', *, *, #9995, .T. ) ;
#3979=CARTESIAN_POINT ( 'NONE',  ( 10.00000000000000000, 0.000000000000000000, 0.000000000000000000 ) ) ;
#3980=LINE ( 'NONE', #2538, #8124 ) ;
#3981=ORIENTED_EDGE ( 'NONE', *, *, #10266, .F. ) ;
#3984=ORIENTED_EDGE ( 'NONE', *, *, #6193, .F. ) ;
#3986=LINE ( 'NONE', #18554, #12561 ) ;
#3990=EDGE_LOOP ( 'NONE', ( #314, #6403, #15120, #15749 ) ) ;
#3993=VERTEX_POINT ( 'NONE', #6250 ) ;
#3996=( NAMED_UNIT ( * ) PLANE_ANGLE_UNIT ( ) SI_UNIT ( $, .RADIAN. ) );
#3999=CARTESIAN_POINT ( 'NONE',  ( 10.00000000000000000, -62.87238730325617553, -4.007856633824042447 ) ) ;
#4000=EDGE_CURVE ( 'NONE', #3993, #16544, #9199, .T. ) ;
#4001=AXIS2_PLACEMENT_3D ( 'NONE', #12977, #11636, #8675 ) ;
#4003=EDGE_CURVE ( 'NONE', #5560, #7581, #18722, .T. ) ;
#4005=EDGE_CURVE ( 'NONE', #5290, #9292, #17877, .T. ) ;
#4007=CYLINDRICAL_SURFACE ( 'NONE', #6593, 24.00000000002399858 ) ;
#4010=CARTESIAN_POINT ( 'NONE',  ( 5.000000000000000000, 15.61693798565582547, -61.03368945066419826 ) ) ;
#4012=ADVANCED_FACE ( 'NONE', ( #13596 ), #4833, .T. ) ;
#4013=DIRECTION ( 'NONE',  ( 0.000000000000000000, -0.8910065241883626808, -0.4539904997395568520 ) ) ;
#4015=CARTESIAN_POINT ( 'NONE',  ( 5.000000000000000000, 58.55669782892461939, 23.24033432160458545 ) ) ;
#4018=DIRECTION ( 'NONE',  ( -1.000000000000000000, 0.000000000000000000, -0.000000000000000000 ) ) ;
#4021=DIRECTION ( 'NONE',  ( -1.000000000000000000, 0.000000000000000000, 0.000000000000000000 ) ) ;
#4023=EDGE_CURVE ( 'NONE', #6557, #1864, #9020, .T. ) ;
#4032=VECTOR ( 'NONE', #1427, 1000.000000000000000 ) ;
#4033=DIRECTION ( 'NONE',  ( -1.000000000000000000, -0.000000000000000000, -0.000000000000000000 ) ) ;
#4035=CARTESIAN_POINT ( 'NONE',  ( 50.00005079999999680, 0.000000000000000000, 30.00000000000000000 ) ) ;
#4041=CARTESIAN_POINT ( 'NONE',  ( 0.000000000000000000, -46.20417134726108088, -32.31183295104820985 ) ) ;
#4049=AXIS2_PLACEMENT_3D ( 'NONE', #2956, #8750, #14568 ) ;
#4057=AXIS2_PLACEMENT_3D ( 'NONE', #4062, #5491, #2622 ) ;
#4058=AXIS2_PLACEMENT_3D ( 'NONE', #11343, #9822, #18589 ) ;
#4060=VERTEX_POINT ( 'NONE', #16359 ) ;
#4061=DIRECTION ( 'NONE',  ( 0.000000000000000000, 0.7071067811865485719, -0.7071067811865463515 ) ) ;
#4062=CARTESIAN_POINT ( 'NONE',  ( 10.00000000000000000, 0.000000000000000000, 0.000000000000000000 ) ) ;
#4063=DIRECTION ( 'NONE',  ( -1.000000000000000000, 0.000000000000000000, -0.000000000000000000 ) ) ;
#4067=EDGE_CURVE ( 'NONE', #4463, #13753, #7164, .T. ) ;
#4069=DIRECTION ( 'NONE',  ( 0.000000000000000000, 0.8910065241883688980, -0.4539904997395446951 ) ) ;
#4071=DIRECTION ( 'NONE',  ( -1.000000000000000000, -0.000000000000000000, -0.000000000000000000 ) ) ;
#4079=ORIENTED_EDGE ( 'NONE', *, *, #4757, .T. ) ;
#4086=EDGE_CURVE ( 'NONE', #9292, #18350, #10516, .T. ) ;
#4089=EDGE_CURVE ( 'NONE', #10426, #3123, #3213, .T. ) ;
#4094=VERTEX_POINT ( 'NONE', #17773 ) ;
#4095=EDGE_LOOP ( 'NONE', ( #3065, #4196, #12387, #7301 ) ) ;
#4096=FACE_OUTER_BOUND ( 'NONE', #14033, .T. ) ;
#4099=DIRECTION ( 'NONE',  ( 0.000000000000000000, -0.8090169943749530024, 0.5877852522924653655 ) ) ;
#4102=DIRECTION ( 'NONE',  ( -1.000000000000000000, 0.000000000000000000, 0.000000000000000000 ) ) ;
#4104=CARTESIAN_POINT ( 'NONE',  ( 4.999999999999999112, 57.83923611457355918, -24.97244012287440285 ) ) ;
#4107=DIRECTION ( 'NONE',  ( -1.000000000000000000, -0.000000000000000000, -0.000000000000000000 ) ) ;
#4108=DIRECTION ( 'NONE',  ( -1.000000000000000000, -0.000000000000000000, 0.000000000000000000 ) ) ;
#4111=ORIENTED_EDGE ( 'NONE', *, *, #6339, .T. ) ;
#4114=DIRECTION ( 'NONE',  ( -1.000000000000000000, -0.000000000000000000, 0.000000000000000000 ) ) ;
#4116=DIRECTION ( 'NONE',  ( 0.000000000000000000, 0.000000000000000000, 1.000000000000000000 ) ) ;
#4117=CIRCLE ( 'NONE', #13844, 63.00000000006298961 ) ;
#4118=ORIENTED_EDGE ( 'NONE', *, *, #12722, .T. ) ;
#4122=EDGE_CURVE ( 'NONE', #3732, #8023, #8257, .T. ) ;
#4133=DIRECTION ( 'NONE',  ( -1.000000000000000000, 0.000000000000000000, 0.000000000000000000 ) ) ;
#4137=DIRECTION ( 'NONE',  ( -1.000000000000000000, -0.000000000000000000, 0.000000000000000000 ) ) ;
#4139=CYLINDRICAL_SURFACE ( 'NONE', #12376, 63.00000000006298961 ) ;
#4142=CIRCLE ( 'NONE', #1093, 24.00000000002400213 ) ;
#4143=EDGE_CURVE ( 'NONE', #6887, #17793, #8989, .T. ) ;
#4144=CARTESIAN_POINT ( 'NONE',  ( 0.000000000000000000, 4.007856633823394077, 62.87238730325622527 ) ) ;
#4149=EDGE_CURVE ( 'NONE', #11786, #14902, #1690, .T. ) ;
#4150=CIRCLE ( 'NONE', #7475, 56.24900000005625600 ) ;
#4151=AXIS2_PLACEMENT_3D ( 'NONE', #2437, #15114, #11087 ) ;
#4155=DIRECTION ( 'NONE',  ( 0.000000000000000000, 0.7071067811865485719, -0.7071067811865463515 ) ) ;
#4156=DIRECTION ( 'NONE',  ( 0.000000000000000000, 0.4539904997395479147, -0.8910065241883673437 ) ) ;
#4158=VERTEX_POINT ( 'NONE', #6914 ) ;
#4160=EDGE_CURVE ( 'NONE', #2985, #11786, #14457, .T. ) ;
#4163=FACE_OUTER_BOUND ( 'NONE', #10157, .T. ) ;
#4164=CIRCLE ( 'NONE', #5354, 56.24900000005625600 ) ;
#4166=CIRCLE ( 'NONE', #17236, 24.00000000002399858 ) ;
#4171=DIRECTION ( 'NONE',  ( 0.000000000000000000, 0.000000000000000000, 1.000000000000000000 ) ) ;
#4177=DIRECTION ( 'NONE',  ( 0.000000000000000000, 0.000000000000000000, 1.000000000000000000 ) ) ;
#4178=VERTEX_POINT ( 'NONE', #11200 ) ;
#4180=DIRECTION ( 'NONE',  ( 0.000000000000000000, 0.000000000000000000, 1.000000000000000000 ) ) ;
#4181=DIRECTION ( 'NONE',  ( -1.000000000000000000, 0.000000000000000000, 0.000000000000000000 ) ) ;
#4187=ORIENTED_EDGE ( 'NONE', *, *, #2620, .T. ) ;
#4189=CARTESIAN_POINT ( 'NONE',  ( 10.00000000000000000, 49.49802920186223076, 26.71881558261748069 ) ) ;
#4195=ADVANCED_FACE ( 'NONE', ( #3598 ), #12628, .T. ) ;
#4196=ORIENTED_EDGE ( 'NONE', *, *, #14850, .F. ) ;
#4201=FACE_OUTER_BOUND ( 'NONE', #6624, .T. ) ;
#4208=CARTESIAN_POINT ( 'NONE',  ( 10.00000000000000000, 55.51919907100653973, 9.823366686500859757 ) ) ;
#4210=CARTESIAN_POINT ( 'NONE',  ( 0.000000000000000000, -23.24033432160398860, -58.55669782892485387 ) ) ;
#4211=CARTESIAN_POINT ( 'NONE',  ( 5.000000000000000000, -33.71303790549235657, -53.22058882792234158 ) ) ;
#4212=CIRCLE ( 'NONE', #14842, 63.00000000006298961 ) ;
#4215=EDGE_LOOP ( 'NONE', ( #8073, #13068, #14235, #14500 ) ) ;
#4216=AXIS2_PLACEMENT_3D ( 'NONE', #11563, #4133, #5475 ) ;
#4221=CIRCLE ( 'NONE', #18807, 63.00000000006298961 ) ;
#4223=CYLINDRICAL_SURFACE ( 'NONE', #14188, 24.00000000002399858 ) ;
#4228=ORIENTED_EDGE ( 'NONE', *, *, #15943, .T. ) ;
#4229=CARTESIAN_POINT ( 'NONE',  ( 10.00000000000000000, -31.97297851452390915, -46.27827401617439307 ) ) ;
#4235=AXIS2_PLACEMENT_3D ( 'NONE', #9037, #1810, #11898 ) ;
#4236=DIRECTION ( 'NONE',  ( 0.000000000000000000, 0.000000000000000000, 1.000000000000000000 ) ) ;
#4237=ORIENTED_EDGE ( 'NONE', *, *, #10084, .F. ) ;
#4238=CIRCLE ( 'NONE', #9086, 56.24900000005625600 ) ;
#4240=EDGE_CURVE ( 'NONE', #8632, #5801, #5661, .T. ) ;
#4241=EDGE_CURVE ( 'NONE', #4178, #2244, #13560, .T. ) ;
#4244=CARTESIAN_POINT ( 'NONE',  ( 0.000000000000000000, 3.673940397442059178E-15, -30.00000000000000000 ) ) ;
#4248=DIRECTION ( 'NONE',  ( -1.000000000000000000, -0.000000000000000000, 0.000000000000000000 ) ) ;
#4249=LINE ( 'NONE', #11577, #17990 ) ;
#4250=VECTOR ( 'NONE', #2249, 1000.000000000000000 ) ;
#4254=FACE_OUTER_BOUND ( 'NONE', #8728, .T. ) ;
#4255=ADVANCED_FACE ( 'NONE', ( #5583 ), #11671, .T. ) ;
#4257=DIRECTION ( 'NONE',  ( -1.000000000000000000, 0.000000000000000000, 0.000000000000000000 ) ) ;
#4258=ORIENTED_EDGE ( 'NONE', *, *, #5027, .T. ) ;
#4260=CARTESIAN_POINT ( 'NONE',  ( 10.00000000000000000, 54.20017844242511273, 32.11449294037215196 ) ) ;
#4262=ORIENTED_EDGE ( 'NONE', *, *, #6787, .F. ) ;
#4263=EDGE_CURVE ( 'NONE', #14803, #8173, #1100, .T. ) ;
#4265=LINE ( 'NONE', #17401, #9966 ) ;
#4270=VERTEX_POINT ( 'NONE', #1488 ) ;
#4276=DIRECTION ( 'NONE',  ( -1.000000000000000000, -0.000000000000000000, -0.000000000000000000 ) ) ;
#4279=ORIENTED_EDGE ( 'NONE', *, *, #15124, .F. ) ;
#4282=CARTESIAN_POINT ( 'NONE',  ( 10.00000000000000000, -46.27827401617379621, -31.97297851452475470 ) ) ;
#4285=DIRECTION ( 'NONE',  ( -1.000000000000000000, 0.000000000000000000, -0.000000000000000000 ) ) ;
#4286=EDGE_CURVE ( 'NONE', #701, #13284, #15081, .T. ) ;
#4289=CARTESIAN_POINT ( 'NONE',  ( 10.00000000000000000, 26.71881558261799228, -49.49802920186195365 ) ) ;
#4294=CYLINDRICAL_SURFACE ( 'NONE', #3427, 24.00000000002399503 ) ;
#4297=DIRECTION ( 'NONE',  ( -1.000000000000000000, 0.000000000000000000, 0.000000000000000000 ) ) ;
#4298=CIRCLE ( 'NONE', #14934, 63.00000000006298961 ) ;
#4300=ORIENTED_EDGE ( 'NONE', *, *, #13770, .F. ) ;
#4301=LINE ( 'NONE', #7139, #6037 ) ;
#4302=LINE ( 'NONE', #3058, #2823 ) ;
#4307=AXIS2_PLACEMENT_3D ( 'NONE', #6520, #3678, #12327 ) ;
#4309=CARTESIAN_POINT ( 'NONE',  ( 10.00000000000000000, -53.06836994729219725, -18.64666490672428623 ) ) ;
#4310=ORIENTED_EDGE ( 'NONE', *, *, #3220, .T. ) ;
#4312=CARTESIAN_POINT ( 'NONE',  ( 0.000000000000000000, 0.000000000000000000, 0.000000000000000000 ) ) ;
#4316=LINE ( 'NONE', #8505, #8391 ) ;
#4317=VERTEX_POINT ( 'NONE', #4260 ) ;
#4320=CARTESIAN_POINT ( 'NONE',  ( 10.00000000000000000, 0.000000000000000000, 0.000000000000000000 ) ) ;
#4326=CARTESIAN_POINT ( 'NONE',  ( 0.000000000000000000, -26.49895292618039377, 49.76630880786299826 ) ) ;
#4327=DIRECTION ( 'NONE',  ( -1.000000000000000000, 0.000000000000000000, 0.000000000000000000 ) ) ;
#4329=DIRECTION ( 'NONE',  ( 0.000000000000000000, -6.982962677686266711E-15, 1.000000000000000000 ) ) ;
#4332=ORIENTED_EDGE ( 'NONE', *, *, #8841, .F. ) ;
#4335=DIRECTION ( 'NONE',  ( 0.000000000000000000, -0.8910065241883626808, -0.4539904997395568520 ) ) ;
#4337=CARTESIAN_POINT ( 'NONE',  ( 10.00000000000000000, 56.37237871411034007, 1.017308535512583711 ) ) ;
#4339=ORIENTED_EDGE ( 'NONE', *, *, #10749, .F. ) ;
#4340=DIRECTION ( 'NONE',  ( -1.000000000000000000, 0.000000000000000000, 0.000000000000000000 ) ) ;
#4349=AXIS2_PLACEMENT_3D ( 'NONE', #12020, #327, #4889 ) ;
#4352=ORIENTED_EDGE ( 'NONE', *, *, #4665, .F. ) ;
#4354=EDGE_LOOP ( 'NONE', ( #1855, #16404, #15887, #11580 ) ) ;
#4356=VERTEX_POINT ( 'NONE', #5856 ) ;
#4359=ADVANCED_FACE ( 'NONE', ( #15677 ), #8443, .T. ) ;
#4364=CARTESIAN_POINT ( 'NONE',  ( 10.00000000000000000, 44.70888270294162226, 34.13306034420202906 ) ) ;
#4369=EDGE_CURVE ( 'NONE', #11814, #3234, #7776, .T. ) ;
#4374=DIRECTION ( 'NONE',  ( -1.000000000000000000, 0.000000000000000000, -0.000000000000000000 ) ) ;
#4375=LINE ( 'NONE', #10178, #10005 ) ;
#4376=DIRECTION ( 'NONE',  ( -1.000000000000000000, -0.000000000000000000, 0.000000000000000000 ) ) ;
#4381=DIRECTION ( 'NONE',  ( 0.000000000000000000, 0.000000000000000000, 1.000000000000000000 ) ) ;
#4382=ORIENTED_EDGE ( 'NONE', *, *, #8659, .T. ) ;
#4383=DIRECTION ( 'NONE',  ( -1.000000000000000000, 0.000000000000000000, 0.000000000000000000 ) ) ;
#4384=DIRECTION ( 'NONE',  ( -1.000000000000000000, -0.000000000000000000, -0.000000000000000000 ) ) ;
#4385=VERTEX_POINT ( 'NONE', #13389 ) ;
#4386=DIRECTION ( 'NONE',  ( -1.000000000000000000, -0.000000000000000000, 0.000000000000000000 ) ) ;
#4390=VERTEX_POINT ( 'NONE', #9090 ) ;
#4393=ORIENTED_EDGE ( 'NONE', *, *, #6732, .F. ) ;
#4398=CARTESIAN_POINT ( 'NONE',  ( 10.00000000000000000, 0.000000000000000000, 0.000000000000000000 ) ) ;
#4399=ORIENTED_EDGE ( 'NONE', *, *, #11819, .T. ) ;
#4400=FACE_OUTER_BOUND ( 'NONE', #15739, .T. ) ;
#4408=ORIENTED_EDGE ( 'NONE', *, *, #15757, .T. ) ;
#4409=DIRECTION ( 'NONE',  ( -1.000000000000000000, 0.000000000000000000, 0.000000000000000000 ) ) ;
#4413=DIRECTION ( 'NONE',  ( 1.000000000000000000, 0.000000000000000000, 0.000000000000000000 ) ) ;
#4415=CARTESIAN_POINT ( 'NONE',  ( 10.00000000000000000, -24.33982105418865061, -50.71018745830470920 ) ) ;
#4422=CARTESIAN_POINT ( 'NONE',  ( -10.00000000000000000, -26.45033635316118747, 39.05576474687271116 ) ) ;
#4426=CARTESIAN_POINT ( 'NONE',  ( 10.00000000000000000, -55.51919907100660367, 9.823366686500467182 ) ) ;
#4428=ORIENTED_EDGE ( 'NONE', *, *, #10607, .T. ) ;
#4429=CIRCLE ( 'NONE', #8990, 24.00000000002399858 ) ;
#4431=CARTESIAN_POINT ( 'NONE',  ( 10.00000000000000000, -47.29147401531925965, -41.62350880771970196 ) ) ;
#4432=EDGE_CURVE ( 'NONE', #8867, #7847, #3189, .T. ) ;
#4435=LINE ( 'NONE', #8907, #14208 ) ;
#4438=ORIENTED_EDGE ( 'NONE', *, *, #17189, .F. ) ;
#4442=DIRECTION ( 'NONE',  ( 0.000000000000000000, 0.000000000000000000, 1.000000000000000000 ) ) ;
#4445=VERTEX_POINT ( 'NONE', #1657 ) ;
#4450=CIRCLE ( 'NONE', #2945, 24.00000000002399503 ) ;
#4451=EDGE_LOOP ( 'NONE', ( #13837, #7550, #10937, #14970 ) ) ;
#4458=EDGE_CURVE ( 'NONE', #9593, #14358, #12660, .T. ) ;
#4460=ORIENTED_EDGE ( 'NONE', *, *, #7857, .T. ) ;
#4461=CIRCLE ( 'NONE', #15119, 56.24900000005625600 ) ;
#4463=VERTEX_POINT ( 'NONE', #12032 ) ;
#4467=CARTESIAN_POINT ( 'NONE',  ( 5.000000000000000000, -40.19788616105644508, 48.50907078259368888 ) ) ;
#4472=CARTESIAN_POINT ( 'NONE',  ( 5.000000000000000000, -53.22058882792220658, 33.71303790549256263 ) ) ;
#4473=CARTESIAN_POINT ( 'NONE',  ( 0.000000000000000000, 46.27827401617403780, 31.97297851452440653 ) ) ;
#4477=ADVANCED_FACE ( 'NONE', ( #10613 ), #16519, .T. ) ;
#4478=ORIENTED_EDGE ( 'NONE', *, *, #67, .T. ) ;
#4480=DIRECTION ( 'NONE',  ( -1.000000000000000000, -0.000000000000000000, -0.000000000000000000 ) ) ;
#4481=VECTOR ( 'NONE', #16653, 1000.000000000000000 ) ;
#4482=AXIS2_PLACEMENT_3D ( 'NONE', #17344, #13229, #14463 ) ;
#4483=VECTOR ( 'NONE', #9098, 1000.000000000000000 ) ;
#4485=EDGE_CURVE ( 'NONE', #5915, #18103, #6878, .T. ) ;
#4490=VERTEX_POINT ( 'NONE', #11764 ) ;
#4506=ORIENTED_EDGE ( 'NONE', *, *, #9915, .T. ) ;
#4513=DIRECTION ( 'NONE',  ( -1.000000000000000000, -0.000000000000000000, 0.000000000000000000 ) ) ;
#4514=ADVANCED_FACE ( 'NONE', ( #17669 ), #336, .T. ) ;
#4515=DIRECTION ( 'NONE',  ( 0.000000000000000000, 0.000000000000000000, 1.000000000000000000 ) ) ;
#4520=ORIENTED_EDGE ( 'NONE', *, *, #15588, .T. ) ;
#4525=ORIENTED_EDGE ( 'NONE', *, *, #7230, .F. ) ;
#4526=EDGE_LOOP ( 'NONE', ( #1388, #8069, #17436, #13082 ) ) ;
#4528=DIRECTION ( 'NONE',  ( -1.000000000000000000, 0.000000000000000000, 0.000000000000000000 ) ) ;
#4531=ADVANCED_FACE ( 'NONE', ( #6799 ), #3574, .T. ) ;
#4534=DIRECTION ( 'NONE',  ( -1.000000000000000000, 0.000000000000000000, -0.000000000000000000 ) ) ;
#4537=ORIENTED_EDGE ( 'NONE', *, *, #8008, .T. ) ;
#4541=ORIENTED_EDGE ( 'NONE', *, *, #1389, .T. ) ;
#4543=CARTESIAN_POINT ( 'NONE',  ( 10.00000000000000000, 40.70683587897958944, 38.81885513160003143 ) ) ;
#4545=ORIENTED_EDGE ( 'NONE', *, *, #10984, .F. ) ;
#4547=CARTESIAN_POINT ( 'NONE',  ( 10.00000000000000000, 55.74967257055883607, 7.478235706489176238 ) ) ;
#4550=DIRECTION ( 'NONE',  ( -1.000000000000000000, -0.000000000000000000, 0.000000000000000000 ) ) ;
#4552=AXIS2_PLACEMENT_3D ( 'NONE', #9959, #11761, #10235 ) ;
#4554=CIRCLE ( 'NONE', #3043, 2.649999999999999467 ) ;
#4559=ORIENTED_EDGE ( 'NONE', *, *, #12967, .T. ) ;
#4562=CARTESIAN_POINT ( 'NONE',  ( 5.000000000000000000, 32.11449294037271329, -54.20017844242479299 ) ) ;
#4568=EDGE_CURVE ( 'NONE', #3665, #4445, #5049, .T. ) ;
#4569=ORIENTED_EDGE ( 'NONE', *, *, #14938, .T. ) ;
#4570=LINE ( 'NONE', #5994, #3321 ) ;
#4571=DIRECTION ( 'NONE',  ( -1.000000000000000000, 0.000000000000000000, -0.000000000000000000 ) ) ;
#4576=ORIENTED_EDGE ( 'NONE', *, *, #8347, .F. ) ;
#4577=DIRECTION ( 'NONE',  ( -1.000000000000000000, 0.000000000000000000, 0.000000000000000000 ) ) ;
#4582=DIRECTION ( 'NONE',  ( 0.000000000000000000, 0.000000000000000000, 1.000000000000000000 ) ) ;
#4589=ORIENTED_EDGE ( 'NONE', *, *, #8242, .F. ) ;
#4590=EDGE_CURVE ( 'NONE', #16471, #3732, #489, .T. ) ;
#4596=ORIENTED_EDGE ( 'NONE', *, *, #8367, .F. ) ;
#4601=LINE ( 'NONE', #5763, #13394 ) ;
#4608=ORIENTED_EDGE ( 'NONE', *, *, #1240, .T. ) ;
#4609=CIRCLE ( 'NONE', #3671, 63.00000000006298961 ) ;
#4611=DIRECTION ( 'NONE',  ( -1.000000000000000000, 0.000000000000000000, -0.000000000000000000 ) ) ;
#4612=FACE_OUTER_BOUND ( 'NONE', #11902, .T. ) ;
#4616=VECTOR ( 'NONE', #13165, 1000.000000000000000 ) ;
#4619=AXIS2_PLACEMENT_3D ( 'NONE', #9800, #2558, #1146 ) ;
#4620=ADVANCED_FACE ( 'NONE', ( #15272 ), #14041, .T. ) ;
#4623=DIRECTION ( 'NONE',  ( -1.000000000000000000, -0.000000000000000000, -0.000000000000000000 ) ) ;
#4629=ORIENTED_EDGE ( 'NONE', *, *, #9515, .F. ) ;
#4631=EDGE_CURVE ( 'NONE', #5290, #5739, #12349, .T. ) ;
#4632=DIRECTION ( 'NONE',  ( -1.000000000000000000, -0.000000000000000000, 0.000000000000000000 ) ) ;
#4635=ORIENTED_EDGE ( 'NONE', *, *, #15519, .F. ) ;
#4636=CARTESIAN_POINT ( 'NONE',  ( 0.000000000000000000, 53.92768374110892893, -16.45250512421876010 ) ) ;
#4640=DIRECTION ( 'NONE',  ( 0.000000000000000000, 0.000000000000000000, 1.000000000000000000 ) ) ;
#4642=VECTOR ( 'NONE', #16317, 1000.000000000000000 ) ;
#4643=DIRECTION ( 'NONE',  ( 0.000000000000000000, 0.000000000000000000, 1.000000000000000000 ) ) ;
#4645=ORIENTED_EDGE ( 'NONE', *, *, #13090, .F. ) ;
#4648=CARTESIAN_POINT ( 'NONE',  ( 0.000000000000000000, 7.478235706489786416, -55.74967257055873660 ) ) ;
#4649=EDGE_CURVE ( 'NONE', #9984, #16064, #4164, .T. ) ;
#4651=CARTESIAN_POINT ( 'NONE',  ( 10.00000000000000000, 0.000000000000000000, 0.000000000000000000 ) ) ;
#4652=CIRCLE ( 'NONE', #8306, 24.00000000002400213 ) ;
#4654=CARTESIAN_POINT ( 'NONE',  ( 10.00000000000000000, -39.14194549634393638, 40.58063702438330722 ) ) ;
#4656=ORIENTED_EDGE ( 'NONE', *, *, #10520, .T. ) ;
#4663=DIRECTION ( 'NONE',  ( 0.000000000000000000, 0.000000000000000000, 1.000000000000000000 ) ) ;
#4664=CIRCLE ( 'NONE', #18360, 56.24900000005626310 ) ;
#4665=EDGE_CURVE ( 'NONE', #14075, #7866, #17832, .T. ) ;
#4668=EDGE_CURVE ( 'NONE', #5686, #14039, #16614, .T. ) ;
#4669=CARTESIAN_POINT ( 'NONE',  ( 10.00000000000000000, 0.000000000000000000, 0.000000000000000000 ) ) ;
#4670=ORIENTED_EDGE ( 'NONE', *, *, #6303, .T. ) ;
#4672=CARTESIAN_POINT ( 'NONE',  ( 0.000000000000000000, 46.27827401617449965, -31.97297851452373507 ) ) ;
#4674=CARTESIAN_POINT ( 'NONE',  ( 0.000000000000000000, 16.10733642026559309, -53.89344778774794520 ) ) ;
#4675=LINE ( 'NONE', #15056, #11302 ) ;
#4676=ORIENTED_EDGE ( 'NONE', *, *, #8560, .T. ) ;
#4683=ADVANCED_FACE ( 'NONE', ( #12804 ), #2511, .T. ) ;
#4684=ORIENTED_EDGE ( 'NONE', *, *, #10641, .F. ) ;
#4691=CARTESIAN_POINT ( 'NONE',  ( 10.00000000000000000, -26.45033635316118747, 33.75576474687270689 ) ) ;
#4697=ORIENTED_EDGE ( 'NONE', *, *, #16389, .F. ) ;
#4699=DIRECTION ( 'NONE',  ( -1.000000000000000000, 0.000000000000000000, 0.000000000000000000 ) ) ;
#4700=ORIENTED_EDGE ( 'NONE', *, *, #5385, .T. ) ;
#4701=ORIENTED_EDGE ( 'NONE', *, *, #15404, .T. ) ;
#4707=ORIENTED_EDGE ( 'NONE', *, *, #3241, .T. ) ;
#4708=CIRCLE ( 'NONE', #151, 2.649999999999999467 ) ;
#4709=EDGE_CURVE ( 'NONE', #445, #5103, #3555, .T. ) ;
#4710=CARTESIAN_POINT ( 'NONE',  ( 0.000000000000000000, 62.72529079327815538, -5.876895005581757481 ) ) ;
#4711=LINE ( 'NONE', #3297, #4483 ) ;
#4713=CARTESIAN_POINT ( 'NONE',  ( 10.00000000000000000, 32.31183295104839459, -46.20417134726096009 ) ) ;
#4715=AXIS2_PLACEMENT_3D ( 'NONE', #10150, #6053, #13488 ) ;
#4719=ADVANCED_FACE ( 'NONE', ( #12379 ), #4007, .T. ) ;
#4722=VERTEX_POINT ( 'NONE', #10944 ) ;
#4723=ORIENTED_EDGE ( 'NONE', *, *, #15191, .F. ) ;
#4730=CIRCLE ( 'NONE', #6561, 56.24900000005627732 ) ;
#4738=DIRECTION ( 'NONE',  ( 1.000000000000000000, 0.000000000000000000, 0.000000000000000000 ) ) ;
#4739=CIRCLE ( 'NONE', #9294, 63.00000000006298961 ) ;
#4740=ORIENTED_EDGE ( 'NONE', *, *, #11222, .F. ) ;
#4743=VECTOR ( 'NONE', #15741, 1000.000000000000000 ) ;
#4745=CYLINDRICAL_SURFACE ( 'NONE', #1306, 24.00000000002399503 ) ;
#4746=CIRCLE ( 'NONE', #12973, 24.00000000002399858 ) ;
#4747=CARTESIAN_POINT ( 'NONE',  ( 10.00000000000000000, -53.06836994729246726, 18.64666490672351529 ) ) ;
#4753=EDGE_LOOP ( 'NONE', ( #15600, #9398, #8943, #15189 ) ) ;
#4756=AXIS2_PLACEMENT_3D ( 'NONE', #4982, #16719, #712 ) ;
#4757=EDGE_CURVE ( 'NONE', #8925, #3393, #15618, .T. ) ;
#4758=CIRCLE ( 'NONE', #16943, 24.00000000002399858 ) ;
#4759=AXIS2_PLACEMENT_3D ( 'NONE', #6871, #12690, #17168 ) ;
#4761=ORIENTED_EDGE ( 'NONE', *, *, #4839, .F. ) ;
#4763=DIRECTION ( 'NONE',  ( 0.000000000000000000, 0.8090169943749445647, 0.5877852522924770229 ) ) ;
#4765=CARTESIAN_POINT ( 'NONE',  ( 50.00005079999999680, 0.000000000000000000, 0.000000000000000000 ) ) ;
#4766=CARTESIAN_POINT ( 'NONE',  ( 0.000000000000000000, -55.83748330407401284, -7.813799127873885197 ) ) ;
#4767=DIRECTION ( 'NONE',  ( -1.000000000000000000, -0.000000000000000000, 0.000000000000000000 ) ) ;
#4768=CARTESIAN_POINT ( 'NONE',  ( 10.00000000000000000, -23.24033432160479862, 58.55669782892453412 ) ) ;
#4770=DIRECTION ( 'NONE',  ( 1.000000000000000000, 0.000000000000000000, -0.000000000000000000 ) ) ;
#4773=VERTEX_POINT ( 'NONE', #1050 ) ;
#4778=VECTOR ( 'NONE', #844, 1000.000000000000000 ) ;
#4790=DIRECTION ( 'NONE',  ( -1.000000000000000000, -0.000000000000000000, 0.000000000000000000 ) ) ;
#4792=FACE_OUTER_BOUND ( 'NONE', #14817, .T. ) ;
#4798=AXIS2_PLACEMENT_3D ( 'NONE', #7685, #13511, #455 ) ;
#4800=VERTEX_POINT ( 'NONE', #16770 ) ;
#4802=EDGE_CURVE ( 'NONE', #12513, #8692, #9019, .T. ) ;
#4805=CIRCLE ( 'NONE', #15454, 24.00000000002400569 ) ;
#4806=DIRECTION ( 'NONE',  ( 0.000000000000000000, 0.000000000000000000, -1.000000000000000000 ) ) ;
#4807=EDGE_CURVE ( 'NONE', #3732, #16471, #5062, .T. ) ;
#4809=VECTOR ( 'NONE', #4513, 1000.000000000000000 ) ;
#4811=EDGE_CURVE ( 'NONE', #10374, #9128, #18772, .T. ) ;
#4813=EDGE_CURVE ( 'NONE', #3285, #9916, #12067, .T. ) ;
#4814=FACE_OUTER_BOUND ( 'NONE', #6738, .T. ) ;
#4818=DIRECTION ( 'NONE',  ( 0.000000000000000000, -0.1564344650402382242, 0.9876883405951364381 ) ) ;
#4819=VERTEX_POINT ( 'NONE', #9612 ) ;
#4821=AXIS2_PLACEMENT_3D ( 'NONE', #6753, #8084, #15043 ) ;
#4822=EDGE_CURVE ( 'NONE', #3525, #7103, #8095, .T. ) ;
#4823=AXIS2_PLACEMENT_3D ( 'NONE', #17657, #14894, #3174 ) ;
#4824=ORIENTED_EDGE ( 'NONE', *, *, #1946, .F. ) ;
#4826=DIRECTION ( 'NONE',  ( 0.000000000000000000, 0.1564344650402243464, 0.9876883405951388806 ) ) ;
#4832=EDGE_CURVE ( 'NONE', #7722, #17686, #3252, .T. ) ;
#4833=CYLINDRICAL_SURFACE ( 'NONE', #173, 24.00000000002399858 ) ;
#4839=EDGE_CURVE ( 'NONE', #4158, #6075, #1721, .T. ) ;
#4841=ORIENTED_EDGE ( 'NONE', *, *, #6732, .T. ) ;
#4846=ORIENTED_EDGE ( 'NONE', *, *, #14014, .T. ) ;
#4847=CARTESIAN_POINT ( 'NONE',  ( 0.000000000000000000, 24.33982105418971642, -50.71018745830419050 ) ) ;
#4848=CYLINDRICAL_SURFACE ( 'NONE', #16082, 63.00000000006298961 ) ;
#4851=ORIENTED_EDGE ( 'NONE', *, *, #5520, .T. ) ;
#4852=CARTESIAN_POINT ( 'NONE',  ( 10.00000000000000000, -32.31183295104739273, -46.20417134726167063 ) ) ;
#4856=AXIS2_PLACEMENT_3D ( 'NONE', #5492, #15491, #6814 ) ;
#4862=DIRECTION ( 'NONE',  ( 0.000000000000000000, 0.000000000000000000, 1.000000000000000000 ) ) ;
#4863=CARTESIAN_POINT ( 'NONE',  ( 10.00000000000000000, -24.68609584167124282, -50.69000562871667626 ) ) ;
#4865=CARTESIAN_POINT ( 'NONE',  ( 0.000000000000000000, 53.22058882792197210, 33.71303790549294632 ) ) ;
#4872=CARTESIAN_POINT ( 'NONE',  ( -10.00000000000000000, -5.120903701083534543E-13, -45.00000000000000000 ) ) ;
#4873=EDGE_LOOP ( 'NONE', ( #13316, #6301, #13695, #17941 ) ) ;
#4880=EDGE_LOOP ( 'NONE', ( #3661, #8453, #14774, #3168 ) ) ;
#4882=FACE_OUTER_BOUND ( 'NONE', #16146, .T. ) ;
#4885=CARTESIAN_POINT ( 'NONE',  ( 0.000000000000000000, 0.000000000000000000, 0.000000000000000000 ) ) ;
#4889=DIRECTION ( 'NONE',  ( 0.000000000000000000, 0.000000000000000000, -1.000000000000000000 ) ) ;
#4894=CARTESIAN_POINT ( 'NONE',  ( 0.000000000000000000, 0.000000000000000000, 0.000000000000000000 ) ) ;
#4898=ORIENTED_EDGE ( 'NONE', *, *, #15760, .T. ) ;
#4904=CYLINDRICAL_SURFACE ( 'NONE', #9903, 24.00000000002399858 ) ;
#4906=CARTESIAN_POINT ( 'NONE',  ( 0.000000000000000000, 0.000000000000000000, 56.24900000005625600 ) ) ;
#4907=ORIENTED_EDGE ( 'NONE', *, *, #1568, .T. ) ;
#4908=EDGE_CURVE ( 'NONE', #3106, #7239, #11472, .T. ) ;
#4910=CYLINDRICAL_SURFACE ( 'NONE', #5821, 63.00000000006298961 ) ;
#4912=ORIENTED_EDGE ( 'NONE', *, *, #11595, .T. ) ;
#4914=ORIENTED_EDGE ( 'NONE', *, *, #6303, .F. ) ;
#4915=AXIS2_PLACEMENT_3D ( 'NONE', #3834, #15462, #11556 ) ;
#4920=DIRECTION ( 'NONE',  ( 0.000000000000000000, 0.1564344650402312575, -0.9876883405951376593 ) ) ;
#4924=AXIS2_PLACEMENT_3D ( 'NONE', #12575, #5617, #6962 ) ;
#4925=FACE_OUTER_BOUND ( 'NONE', #15110, .T. ) ;
#4927=EDGE_CURVE ( 'NONE', #8010, #11814, #12055, .T. ) ;
#4928=ADVANCED_FACE ( 'NONE', ( #4096 ), #6956, .T. ) ;
#4930=CARTESIAN_POINT ( 'NONE',  ( 0.000000000000000000, 34.13306034420251223, -44.70888270294124567 ) ) ;
#4935=ADVANCED_FACE ( 'NONE', ( #11329 ), #15815, .T. ) ;
#4939=ORIENTED_EDGE ( 'NONE', *, *, #14323, .F. ) ;
#4940=ADVANCED_FACE ( 'NONE', ( #15716 ), #2853, .T. ) ;
#4941=CARTESIAN_POINT ( 'NONE',  ( 10.00000000000000000, 47.29147401532012651, -41.62350880771872141 ) ) ;
#4942=ORIENTED_EDGE ( 'NONE', *, *, #9430, .T. ) ;
#4945=EDGE_CURVE ( 'NONE', #8362, #5290, #8713, .T. ) ;
#4947=AXIS2_PLACEMENT_3D ( 'NONE', #17112, #14056, #13857 ) ;
#4949=ORIENTED_EDGE ( 'NONE', *, *, #7257, .F. ) ;
#4951=DIRECTION ( 'NONE',  ( 0.000000000000000000, 0.000000000000000000, 1.000000000000000000 ) ) ;
#4953=CYLINDRICAL_SURFACE ( 'NONE', #15150, 56.24900000005625600 ) ;
#4958=PRODUCT_DEFINITION_SHAPE ( 'NONE', 'NONE',  #15382 ) ;
#4962=VERTEX_POINT ( 'NONE', #4289 ) ;
#4964=DIRECTION ( 'NONE',  ( -1.000000000000000000, 0.000000000000000000, -0.000000000000000000 ) ) ;
#4974=CARTESIAN_POINT ( 'NONE',  ( 10.00000000000000000, 18.64666490672447097, -53.06836994729213330 ) ) ;
#4977=CARTESIAN_POINT ( 'NONE',  ( 0.000000000000000000, 44.70888270294211253, -34.13306034420136825 ) ) ;
#4982=CARTESIAN_POINT ( 'NONE',  ( -10.00000000000000000, 0.000000000000000000, 0.000000000000000000 ) ) ;
#4984=DIRECTION ( 'NONE',  ( -1.000000000000000000, 0.000000000000000000, 0.000000000000000000 ) ) ;
#4988=DIRECTION ( 'NONE',  ( -1.000000000000000000, -0.000000000000000000, -0.000000000000000000 ) ) ;
#4990=DIRECTION ( 'NONE',  ( -1.000000000000000000, -0.000000000000000000, 0.000000000000000000 ) ) ;
#4991=ORIENTED_EDGE ( 'NONE', *, *, #13123, .F. ) ;
#4994=ORIENTED_EDGE ( 'NONE', *, *, #15173, .T. ) ;
#4997=FACE_OUTER_BOUND ( 'NONE', #4354, .T. ) ;
#5001=DIRECTION ( 'NONE',  ( 0.000000000000000000, 0.7071067811865440200, 0.7071067811865511255 ) ) ;
#5003=FACE_OUTER_BOUND ( 'NONE', #2434, .T. ) ;
#5005=CYLINDRICAL_SURFACE ( 'NONE', #3815, 24.00000000002400213 ) ;
#5008=CIRCLE ( 'NONE', #14452, 24.00000000002400213 ) ;
#5009=ORIENTED_EDGE ( 'NONE', *, *, #8767, .F. ) ;
#5010=VERTEX_POINT ( 'NONE', #557 ) ;
#5020=EDGE_LOOP ( 'NONE', ( #12957, #11394, #2547, #4111 ) ) ;
#5025=CIRCLE ( 'NONE', #1395, 63.00000000006298961 ) ;
#5026=EDGE_CURVE ( 'NONE', #2515, #18313, #16019, .T. ) ;
#5027=EDGE_CURVE ( 'NONE', #11971, #6793, #12680, .T. ) ;
#5036=CARTESIAN_POINT ( 'NONE',  ( 4.999999999999999112, 4.007856633824268044, -62.87238730325617553 ) ) ;
#5038=CIRCLE ( 'NONE', #194, 24.00000000002400213 ) ;
#5039=DIRECTION ( 'NONE',  ( -1.000000000000000000, 0.000000000000000000, -0.000000000000000000 ) ) ;
#5040=CARTESIAN_POINT ( 'NONE',  ( 0.000000000000000000, 13.79392154159224404, -61.47135697633764551 ) ) ;
#5043=CARTESIAN_POINT ( 'NONE',  ( 10.00000000000000000, -55.83748330407401284, 16.18620087215011338 ) ) ;
#5044=VERTEX_POINT ( 'NONE', #17889 ) ;
#5048=ORIENTED_EDGE ( 'NONE', *, *, #8699, .F. ) ;
#5049=CIRCLE ( 'NONE', #5678, 24.00000000002400569 ) ;
#5050=CIRCLE ( 'NONE', #10823, 56.24900000005626310 ) ;
#5055=CIRCLE ( 'NONE', #4759, 56.24900000005627021 ) ;
#5059=ORIENTED_EDGE ( 'NONE', *, *, #13913, .T. ) ;
#5062=CIRCLE ( 'NONE', #13901, 2.649999999999999467 ) ;
#5063=AXIS2_PLACEMENT_3D ( 'NONE', #1781, #16167, #12162 ) ;
#5066=VECTOR ( 'NONE', #14195, 1000.000000000000000 ) ;
#5067=DIRECTION ( 'NONE',  ( -1.000000000000000000, 0.000000000000000000, 0.000000000000000000 ) ) ;
#5072=ORIENTED_EDGE ( 'NONE', *, *, #13101, .F. ) ;
#5073=AXIS2_PLACEMENT_3D ( 'NONE', #5324, #15530, #2474 ) ;
#5074=DIRECTION ( 'NONE',  ( -1.000000000000000000, 0.000000000000000000, 0.000000000000000000 ) ) ;
#5082=CARTESIAN_POINT ( 'NONE',  ( 0.000000000000000000, 0.000000000000000000, 0.000000000000000000 ) ) ;
#5083=VERTEX_POINT ( 'NONE', #4930 ) ;
#5084=VECTOR ( 'NONE', #5463, 1000.000000000000000 ) ;
#5086=AXIS2_PLACEMENT_3D ( 'NONE', #10988, #11079, #3861 ) ;
#5089=DIRECTION ( 'NONE',  ( 1.000000000000000000, 0.000000000000000000, -0.000000000000000000 ) ) ;
#5092=EDGE_LOOP ( 'NONE', ( #3936, #11960, #11590, #12581 ) ) ;
#5096=DIRECTION ( 'NONE',  ( -1.000000000000000000, -0.000000000000000000, 0.000000000000000000 ) ) ;
#5097=EDGE_LOOP ( 'NONE', ( #10435, #3349, #4676, #5802 ) ) ;
#5099=DIRECTION ( 'NONE',  ( 0.000000000000000000, -0.8090169943749402348, -0.5877852522924829071 ) ) ;
#5101=CIRCLE ( 'NONE', #18185, 24.00000000002399858 ) ;
#5102=ORIENTED_EDGE ( 'NONE', *, *, #12606, .F. ) ;
#5103=VERTEX_POINT ( 'NONE', #7602 ) ;
#5104=AXIS2_PLACEMENT_3D ( 'NONE', #15838, #13251, #8779 ) ;
#5108=VERTEX_POINT ( 'NONE', #14845 ) ;
#5110=EDGE_CURVE ( 'NONE', #18521, #12641, #14214, .T. ) ;
#5112=AXIS2_PLACEMENT_3D ( 'NONE', #313, #6112, #1829 ) ;
#5117=VERTEX_POINT ( 'NONE', #16177 ) ;
#5125=CIRCLE ( 'NONE', #15783, 63.00000000006298961 ) ;
#5131=LINE ( 'NONE', #18366, #16692 ) ;
#5132=DIRECTION ( 'NONE',  ( -1.000000000000000000, 0.000000000000000000, -0.000000000000000000 ) ) ;
#5135=VECTOR ( 'NONE', #3447, 1000.000000000000000 ) ;
#5136=ORIENTED_EDGE ( 'NONE', *, *, #9335, .F. ) ;
#5137=AXIS2_PLACEMENT_3D ( 'NONE', #1684, #5886, #10541 ) ;
#5140=CARTESIAN_POINT ( 'NONE',  ( 10.00000000000000000, 0.000000000000000000, 0.000000000000000000 ) ) ;
#5144=ADVANCED_FACE ( 'NONE', ( #8926 ), #14740, .T. ) ;
#5145=CARTESIAN_POINT ( 'NONE',  ( -10.00000000000000000, 42.79754323328179311, -13.90576474687299680 ) ) ;
#5146=DIRECTION ( 'NONE',  ( 0.000000000000000000, 0.000000000000000000, 1.000000000000000000 ) ) ;
#5148=DIRECTION ( 'NONE',  ( 1.000000000000000000, 0.000000000000000000, 0.000000000000000000 ) ) ;
#5153=AXIS2_PLACEMENT_3D ( 'NONE', #6699, #5067, #12501 ) ;
#5155=ORIENTED_EDGE ( 'NONE', *, *, #15404, .F. ) ;
#5156=EDGE_LOOP ( 'NONE', ( #12761, #17461, #17148, #4382 ) ) ;
#5158=EDGE_LOOP ( 'NONE', ( #14022, #15387, #13424, #16248 ) ) ;
#5163=DIRECTION ( 'NONE',  ( -1.000000000000000000, -0.000000000000000000, 0.000000000000000000 ) ) ;
#5165=AXIS2_PLACEMENT_3D ( 'NONE', #9379, #1099, #14135 ) ;
#5166=CARTESIAN_POINT ( 'NONE',  ( 10.00000000000000000, 34.13306034420185853, 44.70888270294173594 ) ) ;
#5167=EDGE_CURVE ( 'NONE', #8307, #8867, #10250, .T. ) ;
#5170=CARTESIAN_POINT ( 'NONE',  ( 10.00000000000000000, 24.33982105418901298, 50.71018745830453156 ) ) ;
#5172=DIRECTION ( 'NONE',  ( -1.000000000000000000, -0.000000000000000000, 0.000000000000000000 ) ) ;
#5173=ORIENTED_EDGE ( 'NONE', *, *, #3198, .T. ) ;
#5180=DIRECTION ( 'NONE',  ( 0.000000000000000000, 0.3090169943749480619, -0.9510565162951533091 ) ) ;
#5186=CARTESIAN_POINT ( 'NONE',  ( 10.00000000000000000, -55.83748330407401284, -7.813799127873885197 ) ) ;
#5188=CARTESIAN_POINT ( 'NONE',  ( 4.999999999999999112, 62.72529079327807011, 5.876895005582658982 ) ) ;
#5189=ORIENTED_EDGE ( 'NONE', *, *, #2583, .F. ) ;
#5191=EDGE_LOOP ( 'NONE', ( #12397, #11295, #13327, #3847 ) ) ;
#5193=ORIENTED_EDGE ( 'NONE', *, *, #17293, .F. ) ;
#5196=CARTESIAN_POINT ( 'NONE',  ( 10.00000000000000000, -38.81885513159959800, -40.70683587897998734 ) ) ;
#5202=ORIENTED_EDGE ( 'NONE', *, *, #3545, .T. ) ;
#5206=CARTESIAN_POINT ( 'NONE',  ( 0.000000000000000000, -53.29895248911662264, -18.38754094778296277 ) ) ;
#5218=ORIENTED_EDGE ( 'NONE', *, *, #12446, .T. ) ;
#5221=ORIENTED_EDGE ( 'NONE', *, *, #11983, .T. ) ;
#5222=DIRECTION ( 'NONE',  ( 0.000000000000000000, 0.000000000000000000, 1.000000000000000000 ) ) ;
#5223=DIRECTION ( 'NONE',  ( -1.000000000000000000, 0.000000000000000000, 0.000000000000000000 ) ) ;
#5228=AXIS2_PLACEMENT_3D ( 'NONE', #1326, #8901, #16432 ) ;
#5230=DIRECTION ( 'NONE',  ( -1.000000000000000000, 0.000000000000000000, 0.000000000000000000 ) ) ;
#5233=DIRECTION ( 'NONE',  ( 0.000000000000000000, 0.000000000000000000, -1.000000000000000000 ) ) ;
#5234=EDGE_CURVE ( 'NONE', #9593, #5722, #11707, .T. ) ;
#5239=EDGE_LOOP ( 'NONE', ( #9497, #12150, #1383, #11987 ) ) ;
#5241=CARTESIAN_POINT ( 'NONE',  ( 0.000000000000000000, 32.11449294037271329, -54.20017844242479299 ) ) ;
#5244=ORIENTED_EDGE ( 'NONE', *, *, #6974, .F. ) ;
#5245=CIRCLE ( 'NONE', #18013, 56.24900000005625600 ) ;
#5246=EDGE_CURVE ( 'NONE', #1734, #4317, #3047, .T. ) ;
#5248=CIRCLE ( 'NONE', #8894, 24.00000000002399858 ) ;
#5249=CIRCLE ( 'NONE', #4058, 56.24900000005625600 ) ;
#5251=CARTESIAN_POINT ( 'NONE',  ( 10.00000000000000000, 0.000000000000000000, 0.000000000000000000 ) ) ;
#5252=FACE_OUTER_BOUND ( 'NONE', #2009, .T. ) ;
#5253=CARTESIAN_POINT ( 'NONE',  ( 10.00000000000000000, -1.017308535511979972, -56.37237871411034718 ) ) ;
#5254=CARTESIAN_POINT ( 'NONE',  ( 10.00000000000000000, 62.87238730325621106, 4.007856633823605463 ) ) ;
#5256=DIRECTION ( 'NONE',  ( 0.000000000000000000, 0.7071067811865486830, -0.7071067811865463515 ) ) ;
#5258=DIRECTION ( 'NONE',  ( 1.000000000000000000, 0.000000000000000000, 0.000000000000000000 ) ) ;
#5266=ORIENTED_EDGE ( 'NONE', *, *, #15758, .T. ) ;
#5268=DIRECTION ( 'NONE',  ( 0.000000000000000000, -0.3090169943749548898, 0.9510565162951511997 ) ) ;
#5272=EDGE_CURVE ( 'NONE', #10680, #14902, #987, .T. ) ;
#5277=EDGE_CURVE ( 'NONE', #7753, #12641, #13916, .T. ) ;
#5278=CARTESIAN_POINT ( 'NONE',  ( 10.00000000000000000, 31.97297851452492168, -46.27827401617368963 ) ) ;
#5279=CARTESIAN_POINT ( 'NONE',  ( 10.00000000000000000, 26.71881558261730660, 49.49802920186232313 ) ) ;
#5281=EDGE_CURVE ( 'NONE', #13753, #15698, #5708, .T. ) ;
#5283=DIRECTION ( 'NONE',  ( -1.000000000000000000, -0.000000000000000000, -0.000000000000000000 ) ) ;
#5284=ORIENTED_EDGE ( 'NONE', *, *, #16542, .F. ) ;
#5287=CARTESIAN_POINT ( 'NONE',  ( 10.00000000000000000, -34.13306034420217827, 44.70888270294149436 ) ) ;
#5290=VERTEX_POINT ( 'NONE', #11160 ) ;
#5292=CIRCLE ( 'NONE', #6498, 24.00000000002399858 ) ;
#5293=ORIENTED_EDGE ( 'NONE', *, *, #4813, .F. ) ;
#5294=CARTESIAN_POINT ( 'NONE',  ( 10.00000000000000000, 55.83748330407408389, -7.813799127873475747 ) ) ;
#5295=EDGE_CURVE ( 'NONE', #13893, #484, #2049, .T. ) ;
#5296=DIRECTION ( 'NONE',  ( 0.000000000000000000, 0.000000000000000000, 1.000000000000000000 ) ) ;
#5297=DIRECTION ( 'NONE',  ( 1.000000000000000000, -0.000000000000000000, -0.000000000000000000 ) ) ;
#5302=DIRECTION ( 'NONE',  ( 0.000000000000000000, 0.000000000000000000, 1.000000000000000000 ) ) ;
#5311=ORIENTED_EDGE ( 'NONE', *, *, #12606, .T. ) ;
#5317=AXIS2_PLACEMENT_3D ( 'NONE', #9493, #5500, #17034 ) ;
#5320=ORIENTED_EDGE ( 'NONE', *, *, #11687, .T. ) ;
#5322=CARTESIAN_POINT ( 'NONE',  ( 0.000000000000000000, 0.000000000000000000, 0.000000000000000000 ) ) ;
#5324=CARTESIAN_POINT ( 'NONE',  ( 10.00000000000000000, -40.58063702438316511, -39.14194549634407139 ) ) ;
#5327=CIRCLE ( 'NONE', #3109, 63.00000000006298961 ) ;
#5328=DIRECTION ( 'NONE',  ( 0.000000000000000000, 0.000000000000000000, 1.000000000000000000 ) ) ;
#5329=CARTESIAN_POINT ( 'NONE',  ( 10.00000000000000000, 18.38754094778314752, -53.29895248911656580 ) ) ;
#5334=AXIS2_PLACEMENT_3D ( 'NONE', #12216, #18025, #9358 ) ;
#5338=EDGE_CURVE ( 'NONE', #14293, #3106, #15438, .T. ) ;
#5340=ORIENTED_EDGE ( 'NONE', *, *, #16920, .T. ) ;
#5342=EDGE_CURVE ( 'NONE', #13131, #15635, #6292, .T. ) ;
#5343=ORIENTED_EDGE ( 'NONE', *, *, #2646, .T. ) ;
#5344=AXIS2_PLACEMENT_3D ( 'NONE', #12610, #3962, #3674 ) ;
#5349=LINE ( 'NONE', #10873, #14251 ) ;
#5350=DIRECTION ( 'NONE',  ( -1.000000000000000000, 0.000000000000000000, -0.000000000000000000 ) ) ;
#5352=CARTESIAN_POINT ( 'NONE',  ( 10.00000000000000000, 18.64666490672371424, 53.06836994729241042 ) ) ;
#5354=AXIS2_PLACEMENT_3D ( 'NONE', #10980, #18318, #5268 ) ;
#5355=CARTESIAN_POINT ( 'NONE',  ( 0.000000000000000000, -40.19788616105574164, -48.50907078259425731 ) ) ;
#5357=ORIENTED_EDGE ( 'NONE', *, *, #9641, .F. ) ;
#5359=CIRCLE ( 'NONE', #8089, 63.00000000006298961 ) ;
#5361=AXIS2_PLACEMENT_3D ( 'NONE', #18687, #985, #9834 ) ;
#5362=CARTESIAN_POINT ( 'NONE',  ( -10.00000000000000000, 26.45033635316149301, 33.75576474687247241 ) ) ;
#5364=ORIENTED_EDGE ( 'NONE', *, *, #13913, .F. ) ;
#5372=EDGE_LOOP ( 'NONE', ( #12348, #5568, #17442, #3351 ) ) ;
#5380=FACE_OUTER_BOUND ( 'NONE', #7190, .T. ) ;
#5385=EDGE_CURVE ( 'NONE', #17330, #7275, #559, .T. ) ;
#5386=EDGE_CURVE ( 'NONE', #9315, #2222, #2084, .T. ) ;
#5389=LINE ( 'NONE', #14057, #17353 ) ;
#5395=EDGE_CURVE ( 'NONE', #13122, #1501, #13423, .T. ) ;
#5398=CIRCLE ( 'NONE', #7503, 24.00000000002400213 ) ;
#5399=AXIS2_PLACEMENT_3D ( 'NONE', #15311, #7886, #5302 ) ;
#5400=EDGE_CURVE ( 'NONE', #10719, #6939, #15126, .T. ) ;
#5404=CARTESIAN_POINT ( 'NONE',  ( 10.00000000000000000, -40.19788616105643797, 48.50907078259367466 ) ) ;
#5407=CIRCLE ( 'NONE', #10566, 56.24900000005626310 ) ;
#5408=VECTOR ( 'NONE', #18140, 1000.000000000000000 ) ;
#5409=ORIENTED_EDGE ( 'NONE', *, *, #5272, .F. ) ;
#5418=VERTEX_POINT ( 'NONE', #4648 ) ;
#5423=ORIENTED_EDGE ( 'NONE', *, *, #14064, .F. ) ;
#5426=( LENGTH_UNIT ( ) NAMED_UNIT ( * ) SI_UNIT ( .MILLI., .METRE. ) );
#5427=VERTEX_POINT ( 'NONE', #6170 ) ;
#5431=EDGE_CURVE ( 'NONE', #4385, #17139, #18161, .T. ) ;
#5432=VECTOR ( 'NONE', #3540, 1000.000000000000000 ) ;
#5437=ORIENTED_EDGE ( 'NONE', *, *, #8880, .T. ) ;
#5438=DIRECTION ( 'NONE',  ( 1.000000000000000000, 0.000000000000000000, 0.000000000000000000 ) ) ;
#5439=CYLINDRICAL_SURFACE ( 'NONE', #15661, 63.00000000006298961 ) ;
#5440=LINE ( 'NONE', #18665, #16339 ) ;
#5448=AXIS2_PLACEMENT_3D ( 'NONE', #2550, #18173, #6550 ) ;
#5450=CARTESIAN_POINT ( 'NONE',  ( -10.00000000000000000, 0.000000000000000000, 0.000000000000000000 ) ) ;
#5452=LINE ( 'NONE', #11253, #3736 ) ;
#5453=ADVANCED_FACE ( 'NONE', ( #14942 ), #1883, .T. ) ;
#5457=EDGE_LOOP ( 'NONE', ( #5343, #5797, #4237, #13548 ) ) ;
#5458=AXIS2_PLACEMENT_3D ( 'NONE', #7109, #12933, #17136 ) ;
#5461=DIRECTION ( 'NONE',  ( -1.000000000000000000, 0.000000000000000000, 0.000000000000000000 ) ) ;
#5462=DIRECTION ( 'NONE',  ( 0.000000000000000000, 0.000000000000000000, -1.000000000000000000 ) ) ;
#5463=DIRECTION ( 'NONE',  ( 1.000000000000000000, -0.000000000000000000, -0.000000000000000000 ) ) ;
#5466=AXIS2_PLACEMENT_3D ( 'NONE', #15441, #16779, #8104 ) ;
#5469=ORIENTED_EDGE ( 'NONE', *, *, #16754, .T. ) ;
#5470=DIRECTION ( 'NONE',  ( -1.000000000000000000, 0.000000000000000000, 0.000000000000000000 ) ) ;
#5475=DIRECTION ( 'NONE',  ( 0.000000000000000000, 0.8910065241883654563, 0.4539904997395512454 ) ) ;
#5481=AXIS2_PLACEMENT_3D ( 'NONE', #1702, #6088, #371 ) ;
#5483=DIRECTION ( 'NONE',  ( -1.000000000000000000, -0.000000000000000000, 0.000000000000000000 ) ) ;
#5490=DIRECTION ( 'NONE',  ( -1.000000000000000000, 0.000000000000000000, -0.000000000000000000 ) ) ;
#5491=DIRECTION ( 'NONE',  ( -1.000000000000000000, -0.000000000000000000, -0.000000000000000000 ) ) ;
#5492=CARTESIAN_POINT ( 'NONE',  ( 10.00000000000000000, 0.000000000000000000, 0.000000000000000000 ) ) ;
#5499=EDGE_CURVE ( 'NONE', #11085, #3960, #6652, .T. ) ;
#5500=DIRECTION ( 'NONE',  ( -1.000000000000000000, 0.000000000000000000, 0.000000000000000000 ) ) ;
#5505=LINE ( 'NONE', #15686, #17075 ) ;
#5508=FACE_OUTER_BOUND ( 'NONE', #16654, .T. ) ;
#5510=ORIENTED_EDGE ( 'NONE', *, *, #9189, .F. ) ;
#5516=ORIENTED_EDGE ( 'NONE', *, *, #5431, .F. ) ;
#5518=( NAMED_UNIT ( * ) SI_UNIT ( $, .STERADIAN. ) SOLID_ANGLE_UNIT ( ) );
#5520=EDGE_CURVE ( 'NONE', #6939, #12056, #13788, .T. ) ;
#5521=CARTESIAN_POINT ( 'NONE',  ( 0.000000000000000000, -57.83923611457337444, 24.97244012287480430 ) ) ;
#5523=AXIS2_PLACEMENT_3D ( 'NONE', #8339, #18707, #4329 ) ;
#5526=CIRCLE ( 'NONE', #12542, 24.00000000002399858 ) ;
#5530=DIRECTION ( 'NONE',  ( 0.000000000000000000, 0.000000000000000000, 1.000000000000000000 ) ) ;
#5531=DIRECTION ( 'NONE',  ( -1.000000000000000000, -0.000000000000000000, -0.000000000000000000 ) ) ;
#5534=FACE_BOUND ( 'NONE', #1516, .T. ) ;
#5536=DIRECTION ( 'NONE',  ( 0.000000000000000000, 0.5877852522924685852, 0.8090169943749507819 ) ) ;
#5545=ORIENTED_EDGE ( 'NONE', *, *, #1094, .T. ) ;
#5547=EDGE_CURVE ( 'NONE', #7753, #18363, #10267, .T. ) ;
#5548=ORIENTED_EDGE ( 'NONE', *, *, #8671, .F. ) ;
#5550=DIRECTION ( 'NONE',  ( 0.000000000000000000, -0.9510565162951502005, -0.3090169943749579984 ) ) ;
#5551=CARTESIAN_POINT ( 'NONE',  ( 10.00000000000000000, 56.37237871411035428, -1.017308535511785683 ) ) ;
#5556=DIRECTION ( 'NONE',  ( -1.000000000000000000, -0.000000000000000000, 0.000000000000000000 ) ) ;
#5559=CARTESIAN_POINT ( 'NONE',  ( 0.000000000000000000, 40.19788616105680035, -48.50907078259338334 ) ) ;
#5560=VERTEX_POINT ( 'NONE', #3892 ) ;
#5564=EDGE_LOOP ( 'NONE', ( #11897, #15488, #11051, #4310 ) ) ;
#5565=CARTESIAN_POINT ( 'NONE',  ( 0.000000000000000000, 0.000000000000000000, 0.000000000000000000 ) ) ;
#5568=ORIENTED_EDGE ( 'NONE', *, *, #8841, .T. ) ;
#5569=CARTESIAN_POINT ( 'NONE',  ( 5.000000000000000000, 53.22058882792197210, 33.71303790549294632 ) ) ;
#5571=CARTESIAN_POINT ( 'NONE',  ( 0.000000000000000000, 40.58063702438398224, -39.14194549634321163 ) ) ;
#5573=CARTESIAN_POINT ( 'NONE',  ( 0.000000000000000000, -40.19788616105644508, 48.50907078259368177 ) ) ;
#5577=EDGE_LOOP ( 'NONE', ( #14488, #15831, #12360, #16395 ) ) ;
#5582=ORIENTED_EDGE ( 'NONE', *, *, #17398, .T. ) ;
#5583=FACE_OUTER_BOUND ( 'NONE', #14821, .T. ) ;
#5584=ORIENTED_EDGE ( 'NONE', *, *, #14665, .T. ) ;
#5585=CYLINDRICAL_SURFACE ( 'NONE', #11238, 56.24900000005625600 ) ;
#5587=CIRCLE ( 'NONE', #1037, 24.00000000002399858 ) ;
#5589=DIRECTION ( 'NONE',  ( -1.000000000000000000, 0.000000000000000000, 0.000000000000000000 ) ) ;
#5590=CARTESIAN_POINT ( 'NONE',  ( 10.00000000000000000, 0.000000000000000000, 0.000000000000000000 ) ) ;
#5591=ORIENTED_EDGE ( 'NONE', *, *, #18543, .T. ) ;
#5592=DIRECTION ( 'NONE',  ( -1.000000000000000000, -0.000000000000000000, -0.000000000000000000 ) ) ;
#5599=ORIENTED_EDGE ( 'NONE', *, *, #10061, .F. ) ;
#5600=CARTESIAN_POINT ( 'NONE',  ( 10.00000000000000000, -32.31183295104739273, -46.20417134726167063 ) ) ;
#5603=ORIENTED_EDGE ( 'NONE', *, *, #4945, .F. ) ;
#5606=CYLINDRICAL_SURFACE ( 'NONE', #12128, 56.24900000005625600 ) ;
#5607=DIRECTION ( 'NONE',  ( -1.000000000000000000, 0.000000000000000000, -0.000000000000000000 ) ) ;
#5610=ORIENTED_EDGE ( 'NONE', *, *, #4241, .T. ) ;
#5612=DIRECTION ( 'NONE',  ( -1.000000000000000000, -0.000000000000000000, 0.000000000000000000 ) ) ;
#5616=DIRECTION ( 'NONE',  ( 0.000000000000000000, 0.9510565162951543083, -0.3090169943749447312 ) ) ;
#5617=DIRECTION ( 'NONE',  ( -1.000000000000000000, -0.000000000000000000, -0.000000000000000000 ) ) ;
#5619=ORIENTED_EDGE ( 'NONE', *, *, #11326, .T. ) ;
#5623=CARTESIAN_POINT ( 'NONE',  ( 10.00000000000000000, 0.000000000000000000, 56.24900000005625600 ) ) ;
#5628=CIRCLE ( 'NONE', #11397, 24.00000000002399858 ) ;
#5634=FACE_OUTER_BOUND ( 'NONE', #3596, .T. ) ;
#5639=DIRECTION ( 'NONE',  ( -1.000000000000000000, 0.000000000000000000, 0.000000000000000000 ) ) ;
#5640=VECTOR ( 'NONE', #17840, 1000.000000000000000 ) ;
#5641=CARTESIAN_POINT ( 'NONE',  ( 0.000000000000000000, -26.49895292617967257, -49.76630880786338196 ) ) ;
#5643=DIRECTION ( 'NONE',  ( 0.000000000000000000, 0.000000000000000000, 1.000000000000000000 ) ) ;
#5648=ADVANCED_FACE ( 'NONE', ( #11779 ), #14275, .T. ) ;
#5651=ORIENTED_EDGE ( 'NONE', *, *, #11346, .T. ) ;
#5654=LINE ( 'NONE', #2707, #2654 ) ;
#5661=CIRCLE ( 'NONE', #17802, 56.24900000005625600 ) ;
#5663=DIRECTION ( 'NONE',  ( 0.000000000000000000, 0.000000000000000000, 1.000000000000000000 ) ) ;
#5665=AXIS2_PLACEMENT_3D ( 'NONE', #18393, #1272, #12792 ) ;
#5666=AXIS2_PLACEMENT_3D ( 'NONE', #4326, #15940, #9852 ) ;
#5667=CARTESIAN_POINT ( 'NONE',  ( 10.00000000000000000, 38.81885513159988932, 40.70683587897971734 ) ) ;
#5670=SHAPE_REPRESENTATION ( 'spur gear 1_iso_ISO - Spur gear 3M 40T 20PA 10FW ---S40A75H50L60.0N', ( #8017 ), #2559 ) ;
#5671=CARTESIAN_POINT ( 'NONE',  ( 10.00000000000000000, 7.478235706489787304, -55.74967257055874370 ) ) ;
#5674=ORIENTED_EDGE ( 'NONE', *, *, #16442, .F. ) ;
#5676=DIRECTION ( 'NONE',  ( 0.000000000000000000, 0.000000000000000000, 1.000000000000000000 ) ) ;
#5678=AXIS2_PLACEMENT_3D ( 'NONE', #17005, #3957, #5180 ) ;
#5684=CARTESIAN_POINT ( 'NONE',  ( -10.00000000000000000, -5.117658387065794099E-13, -47.64999999999999858 ) ) ;
#5686=VERTEX_POINT ( 'NONE', #1315 ) ;
#5688=AXIS2_PLACEMENT_3D ( 'NONE', #5322, #11132, #16960 ) ;
#5689=EDGE_LOOP ( 'NONE', ( #8808, #5364, #1673, #15411 ) ) ;
#5691=AXIS2_PLACEMENT_3D ( 'NONE', #14445, #13035, #8830 ) ;
#5694=VERTEX_POINT ( 'NONE', #15690 ) ;
#5697=LINE ( 'NONE', #2835, #8059 ) ;
#5702=CIRCLE ( 'NONE', #10860, 24.00000000002400213 ) ;
#5708=CIRCLE ( 'NONE', #3879, 56.24900000005627021 ) ;
#5710=CIRCLE ( 'NONE', #12090, 56.24900000005625600 ) ;
#5713=VERTEX_POINT ( 'NONE', #11600 ) ;
#5722=VERTEX_POINT ( 'NONE', #12841 ) ;
#5730=AXIS2_PLACEMENT_3D ( 'NONE', #2477, #9431, #14006 ) ;
#5737=DIRECTION ( 'NONE',  ( 0.000000000000000000, 0.000000000000000000, 1.000000000000000000 ) ) ;
#5738=CIRCLE ( 'NONE', #12113, 56.24900000005624889 ) ;
#5739=VERTEX_POINT ( 'NONE', #1499 ) ;
#5740=VECTOR ( 'NONE', #4102, 1000.000000000000000 ) ;
#5742=CARTESIAN_POINT ( 'NONE',  ( 0.000000000000000000, -32.31183295104805353, 46.20417134726119457 ) ) ;
#5744=FACE_OUTER_BOUND ( 'NONE', #8305, .T. ) ;
#5746=CARTESIAN_POINT ( 'NONE',  ( 5.000000000000000000, 58.55669782892493203, -23.24033432160376478 ) ) ;
#5758=CIRCLE ( 'NONE', #3937, 24.00000000002399858 ) ;
#5761=DIRECTION ( 'NONE',  ( 0.000000000000000000, -0.7071067811865388020, -0.7071067811865562325 ) ) ;
#5763=CARTESIAN_POINT ( 'NONE',  ( 5.000000000000000000, 5.876895005582427167, 62.72529079327809853 ) ) ;
#5769=CYLINDRICAL_SURFACE ( 'NONE', #12122, 56.24900000005625600 ) ;
#5770=VERTEX_POINT ( 'NONE', #10434 ) ;
#5771=EDGE_CURVE ( 'NONE', #9920, #3160, #6948, .T. ) ;
#5773=DIRECTION ( 'NONE',  ( -1.000000000000000000, 0.000000000000000000, 0.000000000000000000 ) ) ;
#5774=CARTESIAN_POINT ( 'NONE',  ( 10.00000000000000000, -58.55669782892479702, 23.24033432160415913 ) ) ;
#5778=ORIENTED_EDGE ( 'NONE', *, *, #7458, .T. ) ;
#5779=CIRCLE ( 'NONE', #14893, 24.00000000002399858 ) ;
#5785=CIRCLE ( 'NONE', #10643, 24.00000000002399148 ) ;
#5790=EDGE_CURVE ( 'NONE', #5694, #16829, #11808, .T. ) ;
#5795=VERTEX_POINT ( 'NONE', #3114 ) ;
#5797=ORIENTED_EDGE ( 'NONE', *, *, #13595, .T. ) ;
#5799=AXIS2_PLACEMENT_3D ( 'NONE', #10493, #9073, #14892 ) ;
#5801=VERTEX_POINT ( 'NONE', #17960 ) ;
#5802=ORIENTED_EDGE ( 'NONE', *, *, #8423, .T. ) ;
#5806=CARTESIAN_POINT ( 'NONE',  ( 10.00000000000000000, 23.24033432160521429, -58.55669782892436359 ) ) ;
#5808=ADVANCED_FACE ( 'NONE', ( #11869 ), #13685, .T. ) ;
#5814=VECTOR ( 'NONE', #16934, 1000.000000000000000 ) ;
#5815=LINE ( 'NONE', #5623, #14495 ) ;
#5816=ORIENTED_EDGE ( 'NONE', *, *, #1305, .F. ) ;
#5817=DIRECTION ( 'NONE',  ( -1.000000000000000000, 0.000000000000000000, 0.000000000000000000 ) ) ;
#5821=AXIS2_PLACEMENT_3D ( 'NONE', #629, #13763, #13586 ) ;
#5822=EDGE_CURVE ( 'NONE', #5560, #11258, #13588, .T. ) ;
#5824=ORIENTED_EDGE ( 'NONE', *, *, #16677, .F. ) ;
#5833=VERTEX_POINT ( 'NONE', #1674 ) ;
#5835=CARTESIAN_POINT ( 'NONE',  ( 10.00000000000000000, -16.10733642026445978, -53.89344778774828626 ) ) ;
#5840=CIRCLE ( 'NONE', #16486, 24.00000000002399503 ) ;
#5841=ORIENTED_EDGE ( 'NONE', *, *, #3655, .F. ) ;
#5842=DIRECTION ( 'NONE',  ( 0.000000000000000000, 0.000000000000000000, -1.000000000000000000 ) ) ;
#5846=CARTESIAN_POINT ( 'NONE',  ( 10.00000000000000000, 24.68609584167159454, 50.69000562871650573 ) ) ;
#5848=EDGE_LOOP ( 'NONE', ( #11681, #17521, #4898, #7495 ) ) ;
#5854=EDGE_CURVE ( 'NONE', #15698, #3193, #15015, .T. ) ;
#5856=CARTESIAN_POINT ( 'NONE',  ( 0.000000000000000000, -41.62350880771954564, 47.29147401531940886 ) ) ;
#5863=AXIS2_PLACEMENT_3D ( 'NONE', #14361, #12934, #10164 ) ;
#5864=DIRECTION ( 'NONE',  ( 0.000000000000000000, 0.000000000000000000, 1.000000000000000000 ) ) ;
#5865=CARTESIAN_POINT ( 'NONE',  ( 10.00000000000000000, -46.27827401617427228, 31.97297851452409034 ) ) ;
#5867=EDGE_CURVE ( 'NONE', #3467, #1784, #13040, .T. ) ;
#5868=CIRCLE ( 'NONE', #8310, 2.649999999999997691 ) ;
#5872=EDGE_CURVE ( 'NONE', #5739, #11098, #1477, .T. ) ;
#5873=ORIENTED_EDGE ( 'NONE', *, *, #8293, .F. ) ;
#5875=VERTEX_POINT ( 'NONE', #12331 ) ;
#5876=ORIENTED_EDGE ( 'NONE', *, *, #10525, .T. ) ;
#5879=VERTEX_POINT ( 'NONE', #827 ) ;
#5882=LINE ( 'NONE', #4364, #13291 ) ;
#5885=VERTEX_POINT ( 'NONE', #11189 ) ;
#5886=DIRECTION ( 'NONE',  ( -1.000000000000000000, 0.000000000000000000, 0.000000000000000000 ) ) ;
#5889=ORIENTED_EDGE ( 'NONE', *, *, #10342, .F. ) ;
#5893=DIRECTION ( 'NONE',  ( -1.000000000000000000, 0.000000000000000000, 0.000000000000000000 ) ) ;
#5894=CARTESIAN_POINT ( 'NONE',  ( 5.000000000000000000, 54.20017844242511273, 32.11449294037214486 ) ) ;
#5898=LINE ( 'NONE', #4472, #8601 ) ;
#5901=DIRECTION ( 'NONE',  ( -1.000000000000000000, 0.000000000000000000, 0.000000000000000000 ) ) ;
#5907=ORIENTED_EDGE ( 'NONE', *, *, #456, .F. ) ;
#5910=ORIENTED_EDGE ( 'NONE', *, *, #18159, .T. ) ;
#5915=VERTEX_POINT ( 'NONE', #12526 ) ;
#5916=DIRECTION ( 'NONE',  ( 0.000000000000000000, 0.000000000000000000, 1.000000000000000000 ) ) ;
#5920=ORIENTED_EDGE ( 'NONE', *, *, #9888, .F. ) ;
#5923=EDGE_LOOP ( 'NONE', ( #18774, #15797, #8179, #5221 ) ) ;
#5927=DIRECTION ( 'NONE',  ( 0.000000000000000000, -0.9510565162951565288, 0.3090169943749384029 ) ) ;
#5930=DIRECTION ( 'NONE',  ( 0.000000000000000000, -0.3090169943749350723, -0.9510565162951576390 ) ) ;
#5932=CARTESIAN_POINT ( 'NONE',  ( 0.000000000000000000, 39.14194549634421350, -40.58063702438301590 ) ) ;
#5935=CARTESIAN_POINT ( 'NONE',  ( 0.000000000000000000, 62.87238730325621106, -4.007856633823609016 ) ) ;
#5937=ORIENTED_EDGE ( 'NONE', *, *, #291, .F. ) ;
#5938=CIRCLE ( 'NONE', #7463, 24.00000000002400569 ) ;
#5940=CIRCLE ( 'NONE', #10509, 56.24900000005625600 ) ;
#5943=ORIENTED_EDGE ( 'NONE', *, *, #5246, .F. ) ;
#5944=VECTOR ( 'NONE', #10913, 1000.000000000000000 ) ;
#5945=AXIS2_PLACEMENT_3D ( 'NONE', #14201, #2394, #8209 ) ;
#5949=FACE_OUTER_BOUND ( 'NONE', #13108, .T. ) ;
#5950=CIRCLE ( 'NONE', #8399, 63.00000000006298961 ) ;
#5951=ORIENTED_EDGE ( 'NONE', *, *, #3704, .F. ) ;
#5952=ADVANCED_FACE ( 'NONE', ( #2332 ), #12241, .F. ) ;
#5953=DIRECTION ( 'NONE',  ( 0.000000000000000000, 0.000000000000000000, 1.000000000000000000 ) ) ;
#5957=ORIENTED_EDGE ( 'NONE', *, *, #619, .T. ) ;
#5961=DIRECTION ( 'NONE',  ( 0.000000000000000000, 0.9876883405951382144, -0.1564344650402274828 ) ) ;
#5965=AXIS2_PLACEMENT_3D ( 'NONE', #2093, #14951, #17707 ) ;
#5967=EDGE_CURVE ( 'NONE', #10934, #11971, #9989, .T. ) ;
#5976=EDGE_CURVE ( 'NONE', #18009, #14803, #3914, .T. ) ;
#5978=ADVANCED_FACE ( 'NONE', ( #15291 ), #13853, .F. ) ;
#5981=CARTESIAN_POINT ( 'NONE',  ( 0.000000000000000000, 50.69000562871642046, -24.68609584167177218 ) ) ;
#5984=VERTEX_POINT ( 'NONE', #18245 ) ;
#5987=CARTESIAN_POINT ( 'NONE',  ( 10.00000000000000000, -53.89344778774823652, 16.10733642026462675 ) ) ;
#5988=CYLINDRICAL_SURFACE ( 'NONE', #9180, 56.24900000005625600 ) ;
#5990=ORIENTED_EDGE ( 'NONE', *, *, #9335, .T. ) ;
#5994=CARTESIAN_POINT ( 'NONE',  ( 10.00000000000000000, 16.10733642026482570, 53.89344778774818678 ) ) ;
#5995=FACE_BOUND ( 'NONE', #10950, .T. ) ;
#5999=ORIENTED_EDGE ( 'NONE', *, *, #9203, .T. ) ;
#6001=DIRECTION ( 'NONE',  ( -1.000000000000000000, 0.000000000000000000, 0.000000000000000000 ) ) ;
#6005=DIRECTION ( 'NONE',  ( 1.000000000000000000, 0.000000000000000000, 0.000000000000000000 ) ) ;
#6006=CIRCLE ( 'NONE', #9051, 24.00000000002399858 ) ;
#6011=AXIS2_PLACEMENT_3D ( 'NONE', #12503, #11161, #2411 ) ;
#6013=VERTEX_POINT ( 'NONE', #5667 ) ;
#6017=VERTEX_POINT ( 'NONE', #1478 ) ;
#6020=AXIS2_PLACEMENT_3D ( 'NONE', #9104, #16160, #4826 ) ;
#6021=AXIS2_PLACEMENT_3D ( 'NONE', #683, #2109, #8210 ) ;
#6024=CIRCLE ( 'NONE', #8764, 24.00000000002399503 ) ;
#6026=CARTESIAN_POINT ( 'NONE',  ( 0.000000000000000000, 0.000000000000000000, 0.000000000000000000 ) ) ;
#6028=FACE_OUTER_BOUND ( 'NONE', #14859, .T. ) ;
#6029=FACE_OUTER_BOUND ( 'NONE', #13420, .T. ) ;
#6033=CYLINDRICAL_SURFACE ( 'NONE', #1599, 24.00000000002400213 ) ;
#6035=DIRECTION ( 'NONE',  ( 1.000000000000000000, 0.000000000000000000, 0.000000000000000000 ) ) ;
#6037=VECTOR ( 'NONE', #12779, 1000.000000000000000 ) ;
#6039=CARTESIAN_POINT ( 'NONE',  ( 10.00000000000000000, -53.92768374110879392, -16.45250512421912603 ) ) ;
#6051=CIRCLE ( 'NONE', #13066, 24.00000000002399858 ) ;
#6053=DIRECTION ( 'NONE',  ( -1.000000000000000000, -0.000000000000000000, -0.000000000000000000 ) ) ;
#6068=SURFACE_SIDE_STYLE ('',( #7400 ) ) ;
#6070=LINE ( 'NONE', #18809, #3630 ) ;
#6075=VERTEX_POINT ( 'NONE', #14614 ) ;
#6081=ORIENTED_EDGE ( 'NONE', *, *, #11280, .T. ) ;
#6084=CARTESIAN_POINT ( 'NONE',  ( -10.00000000000000000, 0.000000000000000000, 0.000000000000000000 ) ) ;
#6085=CARTESIAN_POINT ( 'NONE',  ( 0.000000000000000000, 50.71018745830478736, -24.33982105418846942 ) ) ;
#6086=DIRECTION ( 'NONE',  ( 1.000000000000000000, -0.000000000000000000, -0.000000000000000000 ) ) ;
#6087=ORIENTED_EDGE ( 'NONE', *, *, #18201, .F. ) ;
#6088=DIRECTION ( 'NONE',  ( -1.000000000000000000, 0.000000000000000000, 0.000000000000000000 ) ) ;
#6098=ORIENTED_EDGE ( 'NONE', *, *, #18368, .T. ) ;
#6104=LINE ( 'NONE', #17364, #17242 ) ;
#6105=ADVANCED_FACE ( 'NONE', ( #16044 ), #5769, .T. ) ;
#6107=DIRECTION ( 'NONE',  ( -1.000000000000000000, 0.000000000000000000, 0.000000000000000000 ) ) ;
#6110=CARTESIAN_POINT ( 'NONE',  ( 0.000000000000000000, 0.000000000000000000, 0.000000000000000000 ) ) ;
#6111=ORIENTED_EDGE ( 'NONE', *, *, #18132, .F. ) ;
#6112=DIRECTION ( 'NONE',  ( -1.000000000000000000, 0.000000000000000000, 0.000000000000000000 ) ) ;
#6113=ORIENTED_EDGE ( 'NONE', *, *, #57, .T. ) ;
#6116=ORIENTED_EDGE ( 'NONE', *, *, #4263, .T. ) ;
#6118=ORIENTED_EDGE ( 'NONE', *, *, #9581, .F. ) ;
#6121=DIRECTION ( 'NONE',  ( 0.000000000000000000, 0.000000000000000000, 1.000000000000000000 ) ) ;
#6124=DIRECTION ( 'NONE',  ( -1.000000000000000000, -0.000000000000000000, 0.000000000000000000 ) ) ;
#6131=CARTESIAN_POINT ( 'NONE',  ( 10.00000000000000000, 46.27827401617449965, -31.97297851452373507 ) ) ;
#6142=CARTESIAN_POINT ( 'NONE',  ( 10.00000000000000000, 56.37237871411034007, 1.017308535512583711 ) ) ;
#6144=CYLINDRICAL_SURFACE ( 'NONE', #9041, 24.00000000002399858 ) ;
#6160=ADVANCED_FACE ( 'NONE', ( #6319 ), #16231, .T. ) ;
#6165=EDGE_LOOP ( 'NONE', ( #7775, #7846, #9694, #17374 ) ) ;
#6167=ORIENTED_EDGE ( 'NONE', *, *, #15585, .T. ) ;
#6170=CARTESIAN_POINT ( 'NONE',  ( 10.00000000000000000, -61.47135697633768814, -13.79392154159200068 ) ) ;
#6175=CARTESIAN_POINT ( 'NONE',  ( 0.000000000000000000, -61.47135697633788709, 13.79392154159114448 ) ) ;
#6177=VERTEX_POINT ( 'NONE', #1843 ) ;
#6181=ORIENTED_EDGE ( 'NONE', *, *, #10749, .T. ) ;
#6185=AXIS2_PLACEMENT_3D ( 'NONE', #1084, #16891, #12309 ) ;
#6188=VERTEX_POINT ( 'NONE', #7365 ) ;
#6191=DIRECTION ( 'NONE',  ( 1.000000000000000000, 0.000000000000000000, 0.000000000000000000 ) ) ;
#6193=EDGE_CURVE ( 'NONE', #3113, #7366, #7266, .T. ) ;
#6197=ORIENTED_EDGE ( 'NONE', *, *, #2971, .F. ) ;
#6198=CARTESIAN_POINT ( 'NONE',  ( 10.00000000000000000, -33.95787273855213328, -45.00825343885058061 ) ) ;
#6202=LINE ( 'NONE', #10585, #7850 ) ;
#6203=ORIENTED_EDGE ( 'NONE', *, *, #4631, .T. ) ;
#6208=EDGE_CURVE ( 'NONE', #8736, #13131, #11849, .T. ) ;
#6209=EDGE_LOOP ( 'NONE', ( #14476, #3364, #17301, #6745 ) ) ;
#6210=CARTESIAN_POINT ( 'NONE',  ( 0.000000000000000000, 40.58063702438344933, 39.14194549634378006 ) ) ;
#6213=DIRECTION ( 'NONE',  ( 0.000000000000000000, -0.9510565162951499785, -0.3090169943749582204 ) ) ;
#6217=CARTESIAN_POINT ( 'NONE',  ( 10.00000000000000000, -1.335003989221234200, -56.23315539212691760 ) ) ;
#6220=ORIENTED_EDGE ( 'NONE', *, *, #2272, .T. ) ;
#6230=CARTESIAN_POINT ( 'NONE',  ( 10.00000000000000000, -16.10733642026445978, -53.89344778774828626 ) ) ;
#6232=CIRCLE ( 'NONE', #15673, 56.24900000005625600 ) ;
#6234=DIRECTION ( 'NONE',  ( -1.000000000000000000, -0.000000000000000000, -0.000000000000000000 ) ) ;
#6237=VERTEX_POINT ( 'NONE', #17842 ) ;
#6240=CIRCLE ( 'NONE', #1384, 63.00000000006298961 ) ;
#6243=AXIS2_PLACEMENT_3D ( 'NONE', #15463, #18118, #6702 ) ;
#6247=ORIENTED_EDGE ( 'NONE', *, *, #5822, .T. ) ;
#6250=CARTESIAN_POINT ( 'NONE',  ( 10.00000000000000000, -40.70683587897930522, -38.81885513160031564 ) ) ;
#6252=CYLINDRICAL_SURFACE ( 'NONE', #13989, 24.00000000002399858 ) ;
#6259=ORIENTED_EDGE ( 'NONE', *, *, #7196, .F. ) ;
#6270=CARTESIAN_POINT ( 'NONE',  ( 10.00000000000000000, -55.83748330407413363, 7.813799127873079620 ) ) ;
#6271=CIRCLE ( 'NONE', #17235, 24.00000000002400569 ) ;
#6273=ORIENTED_EDGE ( 'NONE', *, *, #9923, .F. ) ;
#6277=DIRECTION ( 'NONE',  ( 0.000000000000000000, 0.000000000000000000, 1.000000000000000000 ) ) ;
#6280=AXIS2_PLACEMENT_3D ( 'NONE', #6477, #12477, #6571 ) ;
#6283=AXIS2_PLACEMENT_3D ( 'NONE', #14783, #10595, #6121 ) ;
#6284=AXIS2_PLACEMENT_3D ( 'NONE', #3918, #5039, #9616 ) ;
#6289=FACE_OUTER_BOUND ( 'NONE', #3099, .T. ) ;
#6292=CIRCLE ( 'NONE', #8440, 24.00000000002399858 ) ;
#6293=DIRECTION ( 'NONE',  ( -1.000000000000000000, -0.000000000000000000, 0.000000000000000000 ) ) ;
#6294=ORIENTED_EDGE ( 'NONE', *, *, #14776, .T. ) ;
#6296=CIRCLE ( 'NONE', #7522, 56.24900000005625600 ) ;
#6297=FACE_OUTER_BOUND ( 'NONE', #5457, .T. ) ;
#6300=AXIS2_PLACEMENT_3D ( 'NONE', #12121, #12302, #14898 ) ;
#6301=ORIENTED_EDGE ( 'NONE', *, *, #4286, .T. ) ;
#6303=EDGE_CURVE ( 'NONE', #16309, #9028, #3949, .T. ) ;
#6311=DIRECTION ( 'NONE',  ( 0.000000000000000000, -1.000000000000000000, -1.047444401652940007E-14 ) ) ;
#6313=EDGE_CURVE ( 'NONE', #6177, #12431, #16997, .T. ) ;
#6317=CARTESIAN_POINT ( 'NONE',  ( 10.00000000000000000, 0.000000000000000000, 0.000000000000000000 ) ) ;
#6318=ORIENTED_EDGE ( 'NONE', *, *, #13646, .F. ) ;
#6319=FACE_OUTER_BOUND ( 'NONE', #13161, .T. ) ;
#6321=DIRECTION ( 'NONE',  ( 0.000000000000000000, 0.000000000000000000, 1.000000000000000000 ) ) ;
#6322=EDGE_CURVE ( 'NONE', #7275, #10830, #5125, .T. ) ;
#6324=DIRECTION ( 'NONE',  ( -1.000000000000000000, 0.000000000000000000, 0.000000000000000000 ) ) ;
#6326=ORIENTED_EDGE ( 'NONE', *, *, #12052, .F. ) ;
#6334=CIRCLE ( 'NONE', #14863, 24.00000000002399858 ) ;
#6335=EDGE_CURVE ( 'NONE', #1805, #6013, #7557, .T. ) ;
#6339=EDGE_CURVE ( 'NONE', #5103, #13033, #3746, .T. ) ;
#6342=CARTESIAN_POINT ( 'NONE',  ( 0.000000000000000000, 26.45033635316149301, 33.75576474687247241 ) ) ;
#6346=AXIS2_PLACEMENT_3D ( 'NONE', #10563, #17710, #6277 ) ;
#6347=AXIS2_PLACEMENT_3D ( 'NONE', #5253, #9537, #15551 ) ;
#6350=DIRECTION ( 'NONE',  ( 0.000000000000000000, 0.000000000000000000, 1.000000000000000000 ) ) ;
#6352=CARTESIAN_POINT ( 'NONE',  ( 10.00000000000000000, -56.37237871411034718, 1.017308535512174261 ) ) ;
#6362=AXIS2_PLACEMENT_3D ( 'NONE', #18734, #4276, #13125 ) ;
#6365=ORIENTED_EDGE ( 'NONE', *, *, #10984, .T. ) ;
#6366=AXIS2_PLACEMENT_3D ( 'NONE', #6110, #7539, #13361 ) ;
#6367=ORIENTED_EDGE ( 'NONE', *, *, #14132, .T. ) ;
#6369=DIRECTION ( 'NONE',  ( -1.000000000000000000, 0.000000000000000000, -0.000000000000000000 ) ) ;
#6372=DIRECTION ( 'NONE',  ( -1.000000000000000000, 0.000000000000000000, 0.000000000000000000 ) ) ;
#6377=VERTEX_POINT ( 'NONE', #4974 ) ;
#6381=CARTESIAN_POINT ( 'NONE',  ( 10.00000000000000000, -7.813799127873676476, 55.83748330407405547 ) ) ;
#6382=CIRCLE ( 'NONE', #15809, 24.00000000002399858 ) ;
#6383=AXIS2_PLACEMENT_3D ( 'NONE', #15855, #15765, #1198 ) ;
#6394=DIRECTION ( 'NONE',  ( 0.000000000000000000, 0.000000000000000000, 1.000000000000000000 ) ) ;
#6397=LINE ( 'NONE', #16580, #5432 ) ;
#6398=ORIENTED_EDGE ( 'NONE', *, *, #235, .T. ) ;
#6403=ORIENTED_EDGE ( 'NONE', *, *, #3824, .F. ) ;
#6404=VERTEX_POINT ( 'NONE', #2127 ) ;
#6405=DIRECTION ( 'NONE',  ( -1.000000000000000000, -0.000000000000000000, -0.000000000000000000 ) ) ;
#6407=CARTESIAN_POINT ( 'NONE',  ( 10.00000000000000000, 0.000000000000000000, 0.000000000000000000 ) ) ;
#6410=CARTESIAN_POINT ( 'NONE',  ( 10.00000000000000000, -56.23315539212691050, 1.335003989221430487 ) ) ;
#6416=DIRECTION ( 'NONE',  ( -1.000000000000000000, -0.000000000000000000, -0.000000000000000000 ) ) ;
#6424=DIRECTION ( 'NONE',  ( 0.000000000000000000, 0.000000000000000000, 1.000000000000000000 ) ) ;
#6425=ORIENTED_EDGE ( 'NONE', *, *, #11490, .T. ) ;
#6427=DIRECTION ( 'NONE',  ( 0.000000000000000000, 0.000000000000000000, 1.000000000000000000 ) ) ;
#6429=CYLINDRICAL_SURFACE ( 'NONE', #16975, 56.24900000005625600 ) ;
#6430=ORIENTED_EDGE ( 'NONE', *, *, #15174, .T. ) ;
#6431=CARTESIAN_POINT ( 'NONE',  ( 10.00000000000000000, -18.38754094778203552, -53.29895248911694239 ) ) ;
#6436=VERTEX_POINT ( 'NONE', #18224 ) ;
#6444=ORIENTED_EDGE ( 'NONE', *, *, #465, .F. ) ;
#6447=ORIENTED_EDGE ( 'NONE', *, *, #16221, .T. ) ;
#6449=ADVANCED_FACE ( 'NONE', ( #8685 ), #35, .T. ) ;
#6454=ORIENTED_EDGE ( 'NONE', *, *, #14959, .F. ) ;
#6456=CARTESIAN_POINT ( 'NONE',  ( 10.00000000000000000, -50.69000562871659810, 24.68609584167141691 ) ) ;
#6458=DIRECTION ( 'NONE',  ( -1.000000000000000000, -0.000000000000000000, 0.000000000000000000 ) ) ;
#6463=FACE_OUTER_BOUND ( 'NONE', #8475, .T. ) ;
#6468=ORIENTED_EDGE ( 'NONE', *, *, #6335, .T. ) ;
#6471=DIRECTION ( 'NONE',  ( -1.000000000000000000, 0.000000000000000000, 0.000000000000000000 ) ) ;
#6477=CARTESIAN_POINT ( 'NONE',  ( 10.00000000000000000, 45.00825343885021113, 33.95787273855260935 ) ) ;
#6481=CARTESIAN_POINT ( 'NONE',  ( 10.00000000000000000, -33.71303790549312396, 53.22058882792185130 ) ) ;
#6482=DIRECTION ( 'NONE',  ( -1.000000000000000000, -0.000000000000000000, 0.000000000000000000 ) ) ;
#6483=CYLINDRICAL_SURFACE ( 'NONE', #17523, 24.00000000002399858 ) ;
#6485=DIRECTION ( 'NONE',  ( 0.000000000000000000, 0.000000000000000000, 1.000000000000000000 ) ) ;
#6488=EDGE_CURVE ( 'NONE', #8855, #2916, #11235, .T. ) ;
#6490=VECTOR ( 'NONE', #2508, 1000.000000000000000 ) ;
#6497=DIRECTION ( 'NONE',  ( 0.000000000000000000, -0.1564344650402171299, -0.9876883405951398798 ) ) ;
#6498=AXIS2_PLACEMENT_3D ( 'NONE', #7349, #13171, #8509 ) ;
#6499=ADVANCED_FACE ( 'NONE', ( #2791 ), #15929, .T. ) ;
#6503=EDGE_LOOP ( 'NONE', ( #17420, #2453, #1809, #6679 ) ) ;
#6508=CARTESIAN_POINT ( 'NONE',  ( 10.00000000000000000, 34.13306034420185853, 44.70888270294173594 ) ) ;
#6509=VERTEX_POINT ( 'NONE', #5559 ) ;
#6510=EDGE_LOOP ( 'NONE', ( #6318, #17787, #10513, #1301 ) ) ;
#6518=CYLINDRICAL_SURFACE ( 'NONE', #5086, 63.00000000006298961 ) ;
#6520=CARTESIAN_POINT ( 'NONE',  ( 10.00000000000000000, 0.000000000000000000, 0.000000000000000000 ) ) ;
#6523=DIRECTION ( 'NONE',  ( 0.000000000000000000, -0.5877852522924622569, -0.8090169943749552228 ) ) ;
#6524=ORIENTED_EDGE ( 'NONE', *, *, #13090, .T. ) ;
#6526=DIRECTION ( 'NONE',  ( 0.000000000000000000, 0.000000000000000000, 1.000000000000000000 ) ) ;
#6539=LINE ( 'NONE', #14582, #219 ) ;
#6545=DIRECTION ( 'NONE',  ( 1.000000000000000000, 0.000000000000000000, -0.000000000000000000 ) ) ;
#6550=DIRECTION ( 'NONE',  ( 0.000000000000000000, 0.5877852522924742473, -0.8090169943749465631 ) ) ;
#6554=DIRECTION ( 'NONE',  ( 0.000000000000000000, 0.000000000000000000, -1.000000000000000000 ) ) ;
#6556=CARTESIAN_POINT ( 'NONE',  ( 10.00000000000000000, 26.45033635316149301, 39.05576474687247668 ) ) ;
#6557=VERTEX_POINT ( 'NONE', #4229 ) ;
#6561=AXIS2_PLACEMENT_3D ( 'NONE', #8719, #4534, #2634 ) ;
#6565=AXIS2_PLACEMENT_3D ( 'NONE', #18433, #13776, #735 ) ;
#6570=EDGE_LOOP ( 'NONE', ( #18716, #17875, #11757, #17064 ) ) ;
#6571=DIRECTION ( 'NONE',  ( 0.000000000000000000, 0.8910065241883690090, -0.4539904997395448616 ) ) ;
#6575=DIRECTION ( 'NONE',  ( -1.000000000000000000, -0.000000000000000000, 0.000000000000000000 ) ) ;
#6576=ADVANCED_FACE ( 'NONE', ( #16297 ), #7714, .T. ) ;
#6577=DIRECTION ( 'NONE',  ( -1.000000000000000000, 0.000000000000000000, -0.000000000000000000 ) ) ;
#6579=LINE ( 'NONE', #3355, #11745 ) ;
#6581=CARTESIAN_POINT ( 'NONE',  ( 10.00000000000000000, -10.11537145609416122, 55.33199130079781014 ) ) ;
#6585=CIRCLE ( 'NONE', #491, 24.00000000002400213 ) ;
#6593=AXIS2_PLACEMENT_3D ( 'NONE', #17065, #9717, #8287 ) ;
#6594=VECTOR ( 'NONE', #17688, 1000.000000000000000 ) ;
#6595=DIRECTION ( 'NONE',  ( -1.000000000000000000, 0.000000000000000000, 0.000000000000000000 ) ) ;
#6598=VECTOR ( 'NONE', #1999, 1000.000000000000000 ) ;
#6599=LINE ( 'NONE', #18021, #15216 ) ;
#6600=DIRECTION ( 'NONE',  ( 0.000000000000000000, 0.000000000000000000, -1.000000000000000000 ) ) ;
#6601=DIRECTION ( 'NONE',  ( 0.000000000000000000, 0.000000000000000000, 1.000000000000000000 ) ) ;
#6603=CARTESIAN_POINT ( 'NONE',  ( 0.000000000000000000, 18.38754094778314752, -53.29895248911656580 ) ) ;
#6605=AXIS2_PLACEMENT_3D ( 'NONE', #3959, #2799, #1284 ) ;
#6608=DIRECTION ( 'NONE',  ( 0.000000000000000000, 0.000000000000000000, 1.000000000000000000 ) ) ;
#6611=EDGE_LOOP ( 'NONE', ( #12785, #14367, #13409, #2510 ) ) ;
#6617=CIRCLE ( 'NONE', #18773, 56.24900000005625600 ) ;
#6624=EDGE_LOOP ( 'NONE', ( #15615, #3356, #10401, #7936, #521, #9517, #7804, #10679, #16439, #13089, #838, #1713, #15289, #18026, #16806, #733, #15116, #10801, #4645, #13838, #5173, #11838, #5357, #3774, #8921, #17187, #6273, #2752, #16284, #14223, #7478, #8232, #7271, #6797, #8042, #13993, #8184, #8273, #17389, #3573, #4629, #2852, #15466, #17415, #7587, #14615, #18104, #5059, #18012, #15205, #12914, #16688, #15971, #7816, #14162, #6863, #14650, #7332, #2838, #15777, #4635, #7583, #145, #12751, #10303, #16778, #12377, #6116, #16209, #11735, #7567, #64, #3984, #18050, #14881, #17876, #8038, #10042, #6664, #12439, #11643, #11153, #7393, #9444, #8163, #16084, #7097, #11882, #10673, #14390, #442, #9479, #3734, #6972, #7825, #1549, #11716, #9964, #14772, #11168, #14278, #14525, #8775, #17040, #2147, #1705, #5610, #3972, #18099, #556, #2466, #10789, #14272, #2391, #5651, #10603, #16096, #10358, #5619, #11512, #6709, #6425, #13720, #13673, #757, #16181, #14246, #18638, #7032, #14819, #2035, #17202, #2227, #10535, #5907, #5778, #2684, #17383, #11107, #18342, #14141, #17806, #15814, #2078, #9534, #5990, #11976, #2796, #12656, #7095, #16483, #16827, #7306, #788, #16375, #569, #10991, #4701, #1986, #3502, #13506, #18671, #10070, #5218, #1573 ) ) ;
#6631=DIRECTION ( 'NONE',  ( 0.000000000000000000, 0.7071067811865486830, -0.7071067811865463515 ) ) ;
#6632=CARTESIAN_POINT ( 'NONE',  ( 0.000000000000000000, 56.37237871411034007, 25.01730853553658207 ) ) ;
#6633=CARTESIAN_POINT ( 'NONE',  ( 10.00000000000000000, 23.24033432160436874, 58.55669782892469755 ) ) ;
#6634=CIRCLE ( 'NONE', #14536, 24.00000000002399858 ) ;
#6637=CIRCLE ( 'NONE', #17292, 24.00000000002399858 ) ;
#6639=ORIENTED_EDGE ( 'NONE', *, *, #14450, .T. ) ;
#6642=VECTOR ( 'NONE', #2197, 1000.000000000000000 ) ;
#6646=CIRCLE ( 'NONE', #10894, 56.24900000005625600 ) ;
#6648=VERTEX_POINT ( 'NONE', #12105 ) ;
#6652=LINE ( 'NONE', #13882, #16982 ) ;
#6653=ORIENTED_EDGE ( 'NONE', *, *, #18788, .T. ) ;
#6656=CARTESIAN_POINT ( 'NONE',  ( 10.00000000000000000, -56.37237871411034718, 25.01730853553617351 ) ) ;
#6663=ADVANCED_FACE ( 'NONE', ( #4400 ), #10476, .T. ) ;
#6664=ORIENTED_EDGE ( 'NONE', *, *, #8367, .T. ) ;
#6667=CIRCLE ( 'NONE', #10903, 63.00000000006298961 ) ;
#6670=VERTEX_POINT ( 'NONE', #7435 ) ;
#6674=CARTESIAN_POINT ( 'NONE',  ( 10.00000000000000000, -54.20017844242489247, -32.11449294037253566 ) ) ;
#6675=CARTESIAN_POINT ( 'NONE',  ( 10.00000000000000000, -34.13306034420153168, -44.70888270294199884 ) ) ;
#6678=DIRECTION ( 'NONE',  ( -1.000000000000000000, 0.000000000000000000, -0.000000000000000000 ) ) ;
#6679=ORIENTED_EDGE ( 'NONE', *, *, #1727, .T. ) ;
#6681=ADVANCED_FACE ( 'NONE', ( #10312 ), #10582, .T. ) ;
#6685=AXIS2_PLACEMENT_3D ( 'NONE', #7330, #5901, #16098 ) ;
#6686=DIRECTION ( 'NONE',  ( 1.000000000000000000, 0.000000000000000000, 0.000000000000000000 ) ) ;
#6693=EDGE_CURVE ( 'NONE', #14039, #8760, #275, .T. ) ;
#6697=CARTESIAN_POINT ( 'NONE',  ( 0.000000000000000000, 0.000000000000000000, 0.000000000000000000 ) ) ;
#6699=CARTESIAN_POINT ( 'NONE',  ( 10.00000000000000000, -55.83748330407401284, -7.813799127873885197 ) ) ;
#6702=DIRECTION ( 'NONE',  ( 0.000000000000000000, 0.000000000000000000, 1.000000000000000000 ) ) ;
#6705=ORIENTED_EDGE ( 'NONE', *, *, #6917, .F. ) ;
#6706=EDGE_CURVE ( 'NONE', #4819, #17330, #8797, .T. ) ;
#6707=CARTESIAN_POINT ( 'NONE',  ( 0.000000000000000000, 46.20417134726132247, 32.31183295104789011 ) ) ;
#6709=ORIENTED_EDGE ( 'NONE', *, *, #11031, .F. ) ;
#6711=CARTESIAN_POINT ( 'NONE',  ( 10.00000000000000000, 26.45033635316149301, 36.40576474687247099 ) ) ;
#6712=CARTESIAN_POINT ( 'NONE',  ( -10.00000000000000000, 0.000000000000000000, 0.000000000000000000 ) ) ;
#6714=EDGE_CURVE ( 'NONE', #11663, #7605, #12755, .T. ) ;
#6718=CARTESIAN_POINT ( 'NONE',  ( 0.000000000000000000, -47.29147401531984229, 41.62350880771904826 ) ) ;
#6720=DIRECTION ( 'NONE',  ( 0.000000000000000000, -0.7071067811865535679, 0.7071067811865414665 ) ) ;
#6722=ORIENTED_EDGE ( 'NONE', *, *, #15173, .F. ) ;
#6729=CARTESIAN_POINT ( 'NONE',  ( 10.00000000000000000, 0.000000000000000000, 0.000000000000000000 ) ) ;
#6731=CARTESIAN_POINT ( 'NONE',  ( 10.00000000000000000, 1.017308535512385870, 56.37237871411034007 ) ) ;
#6732=EDGE_CURVE ( 'NONE', #16786, #16509, #3729, .T. ) ;
#6734=CARTESIAN_POINT ( 'NONE',  ( 10.00000000000000000, -46.27827401617379621, -31.97297851452475470 ) ) ;
#6735=VERTEX_POINT ( 'NONE', #971 ) ;
#6738=EDGE_LOOP ( 'NONE', ( #8603, #8961, #10355, #7885 ) ) ;
#6740=CARTESIAN_POINT ( 'NONE',  ( 10.00000000000000000, 0.000000000000000000, 0.000000000000000000 ) ) ;
#6743=ORIENTED_EDGE ( 'NONE', *, *, #17885, .T. ) ;
#6745=ORIENTED_EDGE ( 'NONE', *, *, #3753, .F. ) ;
#6746=DIRECTION ( 'NONE',  ( -1.000000000000000000, -0.000000000000000000, -0.000000000000000000 ) ) ;
#6752=ORIENTED_EDGE ( 'NONE', *, *, #2185, .F. ) ;
#6753=CARTESIAN_POINT ( 'NONE',  ( 0.000000000000000000, 0.000000000000000000, 0.000000000000000000 ) ) ;
#6758=ORIENTED_EDGE ( 'NONE', *, *, #4003, .T. ) ;
#6761=CARTESIAN_POINT ( 'NONE',  ( -10.00000000000000000, 0.000000000000000000, 0.000000000000000000 ) ) ;
#6762=FACE_BOUND ( 'NONE', #12312, .T. ) ;
#6763=AXIS2_PLACEMENT_3D ( 'NONE', #4654, #10456, #16272 ) ;
#6765=DIRECTION ( 'NONE',  ( -1.000000000000000000, -0.000000000000000000, 0.000000000000000000 ) ) ;
#6767=ORIENTED_EDGE ( 'NONE', *, *, #1346, .T. ) ;
#6768=CARTESIAN_POINT ( 'NONE',  ( 0.000000000000000000, -40.58063702438316511, -39.14194549634407139 ) ) ;
#6774=AXIS2_PLACEMENT_3D ( 'NONE', #6835, #18460, #8364 ) ;
#6778=EDGE_CURVE ( 'NONE', #10374, #5915, #3818, .T. ) ;
#6779=EDGE_CURVE ( 'NONE', #3645, #2724, #15800, .T. ) ;
#6781=CYLINDRICAL_SURFACE ( 'NONE', #11150, 24.00000000002399858 ) ;
#6783=CARTESIAN_POINT ( 'NONE',  ( 10.00000000000000000, 46.20417134726132247, 32.31183295104789011 ) ) ;
#6784=CARTESIAN_POINT ( 'NONE',  ( 10.00000000000000000, 0.000000000000000000, 0.000000000000000000 ) ) ;
#6785=FACE_OUTER_BOUND ( 'NONE', #734, .T. ) ;
#6786=DIRECTION ( 'NONE',  ( 0.000000000000000000, -0.1564344650402170467, -0.9876883405951398798 ) ) ;
#6787=EDGE_CURVE ( 'NONE', #11293, #1465, #12449, .T. ) ;
#6788=CARTESIAN_POINT ( 'NONE',  ( 0.000000000000000000, 41.62350880771986539, -47.29147401531912465 ) ) ;
#6793=VERTEX_POINT ( 'NONE', #6581 ) ;
#6794=AXIS2_PLACEMENT_3D ( 'NONE', #2064, #13497, #7872 ) ;
#6795=DIRECTION ( 'NONE',  ( 0.000000000000000000, 0.000000000000000000, -1.000000000000000000 ) ) ;
#6797=ORIENTED_EDGE ( 'NONE', *, *, #1172, .T. ) ;
#6799=FACE_OUTER_BOUND ( 'NONE', #11488, .T. ) ;
#6802=ADVANCED_FACE ( 'NONE', ( #13638 ), #588, .T. ) ;
#6814=DIRECTION ( 'NONE',  ( 0.000000000000000000, -0.9510565162951500895, -0.3090169943749581649 ) ) ;
#6819=ORIENTED_EDGE ( 'NONE', *, *, #1664, .F. ) ;
#6821=CARTESIAN_POINT ( 'NONE',  ( 10.00000000000000000, 1.335003989221626997, 56.23315539212691050 ) ) ;
#6829=VECTOR ( 'NONE', #6545, 1000.000000000000000 ) ;
#6835=CARTESIAN_POINT ( 'NONE',  ( 0.000000000000000000, -42.79754323328189969, -13.90576474687263264 ) ) ;
#6843=CIRCLE ( 'NONE', #14451, 63.00000000006298961 ) ;
#6846=ORIENTED_EDGE ( 'NONE', *, *, #14720, .F. ) ;
#6848=ORIENTED_EDGE ( 'NONE', *, *, #4458, .F. ) ;
#6850=CARTESIAN_POINT ( 'NONE',  ( 0.000000000000000000, 40.70683587897958233, 38.81885513160002432 ) ) ;
#6854=CARTESIAN_POINT ( 'NONE',  ( 0.000000000000000000, 16.45250512421934630, -53.92768374110874419 ) ) ;
#6860=CARTESIAN_POINT ( 'NONE',  ( 10.00000000000000000, 0.000000000000000000, 0.000000000000000000 ) ) ;
#6863=ORIENTED_EDGE ( 'NONE', *, *, #6322, .T. ) ;
#6867=ORIENTED_EDGE ( 'NONE', *, *, #16913, .F. ) ;
#6871=CARTESIAN_POINT ( 'NONE',  ( 0.000000000000000000, 0.000000000000000000, 0.000000000000000000 ) ) ;
#6872=DIRECTION ( 'NONE',  ( -1.000000000000000000, 0.000000000000000000, -0.000000000000000000 ) ) ;
#6874=DIRECTION ( 'NONE',  ( -1.000000000000000000, 0.000000000000000000, -0.000000000000000000 ) ) ;
#6878=CIRCLE ( 'NONE', #18437, 24.00000000002399858 ) ;
#6882=AXIS2_PLACEMENT_3D ( 'NONE', #9727, #2484, #15629 ) ;
#6883=ORIENTED_EDGE ( 'NONE', *, *, #3479, .F. ) ;
#6886=CARTESIAN_POINT ( 'NONE',  ( 10.00000000000000000, -55.83748330407401284, -7.813799127873885197 ) ) ;
#6887=VERTEX_POINT ( 'NONE', #18380 ) ;
#6888=AXIS2_PLACEMENT_3D ( 'NONE', #7248, #4033, #1445 ) ;
#6906=DIRECTION ( 'NONE',  ( -1.000000000000000000, 0.000000000000000000, -0.000000000000000000 ) ) ;
#6909=CARTESIAN_POINT ( 'NONE',  ( 0.000000000000000000, 61.47135697633778051, 13.79392154159156014 ) ) ;
#6910=CARTESIAN_POINT ( 'NONE',  ( 0.000000000000000000, 0.000000000000000000, 0.000000000000000000 ) ) ;
#6912=ORIENTED_EDGE ( 'NONE', *, *, #16153, .F. ) ;
#6914=CARTESIAN_POINT ( 'NONE',  ( 0.000000000000000000, -10.11537145609416122, 55.33199130079781014 ) ) ;
#6916=AXIS2_PLACEMENT_3D ( 'NONE', #4651, #14379, #10453 ) ;
#6917=EDGE_CURVE ( 'NONE', #10253, #16801, #12765, .T. ) ;
#6922=EDGE_CURVE ( 'NONE', #5103, #10364, #7293, .T. ) ;
#6925=CARTESIAN_POINT ( 'NONE',  ( 0.000000000000000000, -55.83748330407401284, 16.18620087215011338 ) ) ;
#6926=CARTESIAN_POINT ( 'NONE',  ( 10.00000000000000000, 26.49895292618005271, 49.76630880786320432 ) ) ;
#6933=PRODUCT_DEFINITION_CONTEXT ( 'detailed design', #2938, 'design' ) ;
#6935=CARTESIAN_POINT ( 'NONE',  ( 10.00000000000000000, -5.876895005581972420, -62.72529079327814117 ) ) ;
#6937=ORIENTED_EDGE ( 'NONE', *, *, #15298, .T. ) ;
#6939=VERTEX_POINT ( 'NONE', #6967 ) ;
#6948=CIRCLE ( 'NONE', #7245, 63.00000000006298961 ) ;
#6956=CYLINDRICAL_SURFACE ( 'NONE', #3854, 24.00000000002400213 ) ;
#6961=DIRECTION ( 'NONE',  ( 1.000000000000000000, 0.000000000000000000, 0.000000000000000000 ) ) ;
#6962=DIRECTION ( 'NONE',  ( 0.000000000000000000, 0.000000000000000000, 1.000000000000000000 ) ) ;
#6964=LINE ( 'NONE', #4015, #17779 ) ;
#6967=CARTESIAN_POINT ( 'NONE',  ( 10.00000000000000000, -44.70888270294135936, -34.13306034420235591 ) ) ;
#6970=CARTESIAN_POINT ( 'NONE',  ( 10.00000000000000000, 0.000000000000000000, 0.000000000000000000 ) ) ;
#6972=ORIENTED_EDGE ( 'NONE', *, *, #15774, .T. ) ;
#6974=EDGE_CURVE ( 'NONE', #14902, #18755, #3041, .T. ) ;
#6975=AXIS2_PLACEMENT_3D ( 'NONE', #7592, #14931, #1874 ) ;
#6980=DIRECTION ( 'NONE',  ( -1.000000000000000000, 0.000000000000000000, 0.000000000000000000 ) ) ;
#6981=CYLINDRICAL_SURFACE ( 'NONE', #7493, 24.00000000002399858 ) ;
#6982=CYLINDRICAL_SURFACE ( 'NONE', #3272, 56.24900000005625600 ) ;
#6986=ORIENTED_EDGE ( 'NONE', *, *, #13834, .F. ) ;
#6993=CARTESIAN_POINT ( 'NONE',  ( 0.000000000000000000, 24.68609584167159454, 50.69000562871650573 ) ) ;
#6996=CARTESIAN_POINT ( 'NONE',  ( 10.00000000000000000, -40.70683587897985234, 38.81885513159974010 ) ) ;
#7006=DIRECTION ( 'NONE',  ( 0.000000000000000000, 0.000000000000000000, 1.000000000000000000 ) ) ;
#7008=DIRECTION ( 'NONE',  ( 0.000000000000000000, -0.9510565162951565288, 0.3090169943749384029 ) ) ;
#7012=ORIENTED_EDGE ( 'NONE', *, *, #11152, .T. ) ;
#7015=DIRECTION ( 'NONE',  ( 0.000000000000000000, -0.9510565162951502005, -0.3090169943749579984 ) ) ;
#7016=EDGE_CURVE ( 'NONE', #1879, #14399, #2427, .T. ) ;
#7020=AXIS2_PLACEMENT_3D ( 'NONE', #8584, #14398, #11550 ) ;
#7027=DIRECTION ( 'NONE',  ( 1.000000000000000000, 0.000000000000000000, -0.000000000000000000 ) ) ;
#7032=ORIENTED_EDGE ( 'NONE', *, *, #11424, .F. ) ;
#7033=VERTEX_POINT ( 'NONE', #106 ) ;
#7034=DIRECTION ( 'NONE',  ( -1.000000000000000000, 0.000000000000000000, 0.000000000000000000 ) ) ;
#7036=DIRECTION ( 'NONE',  ( -1.000000000000000000, 0.000000000000000000, 0.000000000000000000 ) ) ;
#7039=ADVANCED_FACE ( 'NONE', ( #7613 ), #10459, .T. ) ;
#7041=EDGE_CURVE ( 'NONE', #4390, #5560, #6382, .T. ) ;
#7046=DIRECTION ( 'NONE',  ( 0.000000000000000000, 0.000000000000000000, 1.000000000000000000 ) ) ;
#7056=AXIS2_PLACEMENT_3D ( 'NONE', #15325, #15613, #14288 ) ;
#7064=VERTEX_POINT ( 'NONE', #10375 ) ;
#7066=CYLINDRICAL_SURFACE ( 'NONE', #5361, 24.00000000002400213 ) ;
#7071=DIRECTION ( 'NONE',  ( 0.000000000000000000, 0.000000000000000000, -1.000000000000000000 ) ) ;
#7075=ORIENTED_EDGE ( 'NONE', *, *, #13500, .F. ) ;
#7079=ORIENTED_EDGE ( 'NONE', *, *, #2726, .F. ) ;
#7085=DIRECTION ( 'NONE',  ( 0.000000000000000000, 0.000000000000000000, 1.000000000000000000 ) ) ;
#7087=EDGE_CURVE ( 'NONE', #8855, #18145, #8811, .T. ) ;
#7090=ORIENTED_EDGE ( 'NONE', *, *, #3166, .T. ) ;
#7091=DIRECTION ( 'NONE',  ( -1.000000000000000000, -0.000000000000000000, 0.000000000000000000 ) ) ;
#7095=ORIENTED_EDGE ( 'NONE', *, *, #11569, .T. ) ;
#7097=ORIENTED_EDGE ( 'NONE', *, *, #1661, .T. ) ;
#7098=AXIS2_PLACEMENT_3D ( 'NONE', #3184, #9174, #14800 ) ;
#7099=CARTESIAN_POINT ( 'NONE',  ( 0.000000000000000000, 7.813799127873274131, 55.83748330407410521 ) ) ;
#7101=EDGE_LOOP ( 'NONE', ( #4700, #16166, #10209, #3872 ) ) ;
#7103=VERTEX_POINT ( 'NONE', #3054 ) ;
#7109=CARTESIAN_POINT ( 'NONE',  ( 10.00000000000000000, 16.45250512421856470, 53.92768374110897156 ) ) ;
#7110=DIRECTION ( 'NONE',  ( -1.000000000000000000, 0.000000000000000000, -0.000000000000000000 ) ) ;
#7117=LINE ( 'NONE', #11948, #366 ) ;
#7120=COLOUR_RGB ( '',1.000000000000000000, 0.9490196078431372140, 0.9098039215686274384 ) ;
#7130=EDGE_CURVE ( 'NONE', #18246, #3993, #18237, .T. ) ;
#7138=ORIENTED_EDGE ( 'NONE', *, *, #1557, .T. ) ;
#7139=CARTESIAN_POINT ( 'NONE',  ( 10.00000000000000000, 7.478235706488965739, 55.74967257055886449 ) ) ;
#7140=DIRECTION ( 'NONE',  ( 0.000000000000000000, 0.000000000000000000, 1.000000000000000000 ) ) ;
#7143=EDGE_CURVE ( 'NONE', #607, #5984, #10026, .T. ) ;
#7145=EDGE_CURVE ( 'NONE', #6377, #3492, #12456, .T. ) ;
#7147=EDGE_CURVE ( 'NONE', #15934, #743, #5779, .T. ) ;
#7149=VERTEX_POINT ( 'NONE', #6633 ) ;
#7152=FACE_OUTER_BOUND ( 'NONE', #13311, .T. ) ;
#7154=CIRCLE ( 'NONE', #5334, 24.00000000002399858 ) ;
#7155=CARTESIAN_POINT ( 'NONE',  ( 0.000000000000000000, -50.69000562871624993, -24.68609584167212745 ) ) ;
#7162=CYLINDRICAL_SURFACE ( 'NONE', #9658, 63.00000000006298961 ) ;
#7163=EDGE_LOOP ( 'NONE', ( #15544, #17477, #5599, #16458 ) ) ;
#7164=CIRCLE ( 'NONE', #8690, 24.00000000002399858 ) ;
#7167=CIRCLE ( 'NONE', #2915, 30.00000000000000000 ) ;
#7171=CARTESIAN_POINT ( 'NONE',  ( 10.00000000000000000, -55.83748330407413363, 7.813799127873079620 ) ) ;
#7173=VECTOR ( 'NONE', #10780, 1000.000000000000000 ) ;
#7178=VECTOR ( 'NONE', #13966, 1000.000000000000000 ) ;
#7184=DIRECTION ( 'NONE',  ( 0.000000000000000000, 0.000000000000000000, 1.000000000000000000 ) ) ;
#7185=ORIENTED_EDGE ( 'NONE', *, *, #9430, .F. ) ;
#7190=EDGE_LOOP ( 'NONE', ( #2256, #12555, #5937, #13819 ) ) ;
#7194=AXIS2_PLACEMENT_3D ( 'NONE', #6210, #12012, #17829 ) ;
#7195=AXIS2_PLACEMENT_3D ( 'NONE', #1052, #18759, #15620 ) ;
#7196=EDGE_CURVE ( 'NONE', #18189, #7033, #11089, .T. ) ;
#7197=LINE ( 'NONE', #5684, #15682 ) ;
#7200=AXIS2_PLACEMENT_3D ( 'NONE', #12769, #5612, #18575 ) ;
#7203=ORIENTED_EDGE ( 'NONE', *, *, #7723, .T. ) ;
#7207=LINE ( 'NONE', #8551, #2711 ) ;
#7209=AXIS2_PLACEMENT_3D ( 'NONE', #13202, #155, #10345 ) ;
#7210=VERTEX_POINT ( 'NONE', #10998 ) ;
#7212=CIRCLE ( 'NONE', #2345, 24.00000000002400213 ) ;
#7213=EDGE_CURVE ( 'NONE', #8606, #3467, #5389, .T. ) ;
#7214=DIRECTION ( 'NONE',  ( 0.000000000000000000, 0.8910065241883654563, 0.4539904997395512454 ) ) ;
#7215=SHAPE_REPRESENTATION_RELATIONSHIP ( 'NONE' , 'NONE' ,  #5670, #8303 ) ;
#7222=ORIENTED_EDGE ( 'NONE', *, *, #16221, .F. ) ;
#7225=CARTESIAN_POINT ( 'NONE',  ( -10.00000000000000000, 0.000000000000000000, 0.000000000000000000 ) ) ;
#7226=DIRECTION ( 'NONE',  ( 0.000000000000000000, 0.000000000000000000, 1.000000000000000000 ) ) ;
#7230=EDGE_CURVE ( 'NONE', #16509, #2331, #13091, .T. ) ;
#7236=DIRECTION ( 'NONE',  ( -1.000000000000000000, 0.000000000000000000, -0.000000000000000000 ) ) ;
#7239=VERTEX_POINT ( 'NONE', #11194 ) ;
#7245=AXIS2_PLACEMENT_3D ( 'NONE', #12050, #8911, #10350 ) ;
#7248=CARTESIAN_POINT ( 'NONE',  ( -10.00000000000000000, 0.000000000000000000, 0.000000000000000000 ) ) ;
#7249=LINE ( 'NONE', #8773, #13119 ) ;
#7255=CARTESIAN_POINT ( 'NONE',  ( 10.00000000000000000, 0.000000000000000000, 0.000000000000000000 ) ) ;
#7257=EDGE_CURVE ( 'NONE', #11551, #1152, #10940, .T. ) ;
#7262=ORIENTED_EDGE ( 'NONE', *, *, #12990, .F. ) ;
#7263=EDGE_CURVE ( 'NONE', #8465, #15167, #2242, .T. ) ;
#7266=CIRCLE ( 'NONE', #16390, 24.00000000002399503 ) ;
#7269=AXIS2_PLACEMENT_3D ( 'NONE', #9601, #13898, #7987 ) ;
#7270=EDGE_CURVE ( 'NONE', #6793, #4158, #13968, .T. ) ;
#7271=ORIENTED_EDGE ( 'NONE', *, *, #8537, .T. ) ;
#7275=VERTEX_POINT ( 'NONE', #831 ) ;
#7277=DIRECTION ( 'NONE',  ( 1.000000000000000000, 0.000000000000000000, 0.000000000000000000 ) ) ;
#7279=DIRECTION ( 'NONE',  ( -1.000000000000000000, 0.000000000000000000, 0.000000000000000000 ) ) ;
#7284=ORIENTED_EDGE ( 'NONE', *, *, #4813, .T. ) ;
#7293=CIRCLE ( 'NONE', #1216, 24.00000000002400569 ) ;
#7298=ORIENTED_EDGE ( 'NONE', *, *, #18560, .F. ) ;
#7299=FACE_OUTER_BOUND ( 'NONE', #9687, .T. ) ;
#7301=ORIENTED_EDGE ( 'NONE', *, *, #5854, .T. ) ;
#7305=ORIENTED_EDGE ( 'NONE', *, *, #5386, .F. ) ;
#7306=ORIENTED_EDGE ( 'NONE', *, *, #3841, .T. ) ;
#7311=ORIENTED_EDGE ( 'NONE', *, *, #235, .F. ) ;
#7320=DIRECTION ( 'NONE',  ( -1.000000000000000000, -0.000000000000000000, -0.000000000000000000 ) ) ;
#7324=DIRECTION ( 'NONE',  ( -1.000000000000000000, 0.000000000000000000, 0.000000000000000000 ) ) ;
#7325=EDGE_CURVE ( 'NONE', #13928, #16309, #8222, .T. ) ;
#7326=DIRECTION ( 'NONE',  ( -1.000000000000000000, 0.000000000000000000, -0.000000000000000000 ) ) ;
#7327=FACE_OUTER_BOUND ( 'NONE', #7598, .T. ) ;
#7329=ORIENTED_EDGE ( 'NONE', *, *, #7962, .T. ) ;
#7330=CARTESIAN_POINT ( 'NONE',  ( 0.000000000000000000, 0.000000000000000000, 0.000000000000000000 ) ) ;
#7332=ORIENTED_EDGE ( 'NONE', *, *, #11664, .T. ) ;
#7335=ORIENTED_EDGE ( 'NONE', *, *, #18370, .F. ) ;
#7338=CYLINDRICAL_SURFACE ( 'NONE', #7020, 56.24900000005625600 ) ;
#7343=DIRECTION ( 'NONE',  ( -1.000000000000000000, 0.000000000000000000, 0.000000000000000000 ) ) ;
#7345=DIRECTION ( 'NONE',  ( -1.000000000000000000, 0.000000000000000000, 0.000000000000000000 ) ) ;
#7347=DIRECTION ( 'NONE',  ( -1.000000000000000000, -0.000000000000000000, 0.000000000000000000 ) ) ;
#7349=CARTESIAN_POINT ( 'NONE',  ( 0.000000000000000000, -40.58063702438372644, 39.14194549634347453 ) ) ;
#7350=CYLINDRICAL_SURFACE ( 'NONE', #16676, 24.00000000002399858 ) ;
#7354=EDGE_CURVE ( 'NONE', #3048, #8307, #5785, .T. ) ;
#7357=CARTESIAN_POINT ( 'NONE',  ( 10.00000000000000000, 0.000000000000000000, 0.000000000000000000 ) ) ;
#7361=DIRECTION ( 'NONE',  ( 0.000000000000000000, 0.000000000000000000, 1.000000000000000000 ) ) ;
#7362=EDGE_CURVE ( 'NONE', #6404, #4385, #14518, .T. ) ;
#7363=DIRECTION ( 'NONE',  ( -1.000000000000000000, -0.000000000000000000, 0.000000000000000000 ) ) ;
#7364=CYLINDRICAL_SURFACE ( 'NONE', #10132, 63.00000000006298961 ) ;
#7365=CARTESIAN_POINT ( 'NONE',  ( 0.000000000000000000, -53.89344778774800204, -16.10733642026540124 ) ) ;
#7366=VERTEX_POINT ( 'NONE', #14339 ) ;
#7369=DIRECTION ( 'NONE',  ( -1.000000000000000000, 0.000000000000000000, 0.000000000000000000 ) ) ;
#7370=CIRCLE ( 'NONE', #4349, 24.00000000002399858 ) ;
#7371=DIRECTION ( 'NONE',  ( -1.000000000000000000, -0.000000000000000000, -0.000000000000000000 ) ) ;
#7372=ORIENTED_EDGE ( 'NONE', *, *, #141, .T. ) ;
#7373=EDGE_LOOP ( 'NONE', ( #2556, #15033, #10077, #1817 ) ) ;
#7374=CARTESIAN_POINT ( 'NONE',  ( 0.000000000000000000, -56.37237871411032586, -1.017308535512989609 ) ) ;
#7377=EDGE_CURVE ( 'NONE', #9315, #16736, #18551, .T. ) ;
#7381=CARTESIAN_POINT ( 'NONE',  ( -10.00000000000000000, 0.000000000000000000, 0.000000000000000000 ) ) ;
#7382=EDGE_CURVE ( 'NONE', #17073, #17166, #12780, .T. ) ;
#7384=AXIS2_PLACEMENT_3D ( 'NONE', #11162, #15263, #16994 ) ;
#7390=CIRCLE ( 'NONE', #14973, 24.00000000002399503 ) ;
#7393=ORIENTED_EDGE ( 'NONE', *, *, #4143, .T. ) ;
#7400=SURFACE_STYLE_FILL_AREA ( #16258 ) ;
#7403=FACE_OUTER_BOUND ( 'NONE', #17770, .T. ) ;
#7406=VERTEX_POINT ( 'NONE', #5774 ) ;
#7407=ORIENTED_EDGE ( 'NONE', *, *, #986, .F. ) ;
#7410=DIRECTION ( 'NONE',  ( 1.000000000000000000, 0.000000000000000000, 0.000000000000000000 ) ) ;
#7411=EDGE_LOOP ( 'NONE', ( #2751, #9487, #16289, #17680 ) ) ;
#7413=CARTESIAN_POINT ( 'NONE',  ( 50.00005079999999680, 3.673940397442059178E-15, -30.00000000000000000 ) ) ;
#7414=DIRECTION ( 'NONE',  ( -1.000000000000000000, 0.000000000000000000, 0.000000000000000000 ) ) ;
#7420=CARTESIAN_POINT ( 'NONE',  ( 0.000000000000000000, 48.50907078259382388, 40.19788616105627455 ) ) ;
#7421=DIRECTION ( 'NONE',  ( -1.000000000000000000, 0.000000000000000000, -0.000000000000000000 ) ) ;
#7428=CARTESIAN_POINT ( 'NONE',  ( 10.00000000000000000, 0.000000000000000000, 0.000000000000000000 ) ) ;
#7429=CARTESIAN_POINT ( 'NONE',  ( 10.00000000000000000, -40.70683587897985234, 38.81885513159974010 ) ) ;
#7431=CARTESIAN_POINT ( 'NONE',  ( 10.00000000000000000, -55.74967257055877212, -7.478235706489567924 ) ) ;
#7432=CARTESIAN_POINT ( 'NONE',  ( 10.00000000000000000, 24.68609584167159454, 50.69000562871650573 ) ) ;
#7433=DIRECTION ( 'NONE',  ( 0.000000000000000000, 0.000000000000000000, 1.000000000000000000 ) ) ;
#7435=CARTESIAN_POINT ( 'NONE',  ( 0.000000000000000000, 47.29147401531955097, 41.62350880771938222 ) ) ;
#7437=AXIS2_PLACEMENT_3D ( 'NONE', #6740, #2357, #8071 ) ;
#7444=ADVANCED_FACE ( 'NONE', ( #4612 ), #7565, .T. ) ;
#7446=AXIS2_PLACEMENT_3D ( 'NONE', #8992, #12042, #3108 ) ;
#7447=CIRCLE ( 'NONE', #15675, 24.00000000002399858 ) ;
#7449=DIRECTION ( 'NONE',  ( 1.000000000000000000, 0.000000000000000000, 0.000000000000000000 ) ) ;
#7458=EDGE_CURVE ( 'NONE', #1332, #7103, #5407, .T. ) ;
#7463=AXIS2_PLACEMENT_3D ( 'NONE', #7099, #1579, #68 ) ;
#7464=VERTEX_POINT ( 'NONE', #2041 ) ;
#7465=CIRCLE ( 'NONE', #1998, 63.00000000006298961 ) ;
#7469=EDGE_LOOP ( 'NONE', ( #6722, #9798, #385, #4740 ) ) ;
#7471=AXIS2_PLACEMENT_3D ( 'NONE', #5450, #6416, #17076 ) ;
#7472=CARTESIAN_POINT ( 'NONE',  ( 0.000000000000000000, 0.000000000000000000, 0.000000000000000000 ) ) ;
#7473=CARTESIAN_POINT ( 'NONE',  ( 0.000000000000000000, 0.000000000000000000, 0.000000000000000000 ) ) ;
#7475=AXIS2_PLACEMENT_3D ( 'NONE', #9252, #16310, #7551 ) ;
#7478=ORIENTED_EDGE ( 'NONE', *, *, #8039, .T. ) ;
#7480=ORIENTED_EDGE ( 'NONE', *, *, #8880, .F. ) ;
#7487=CYLINDRICAL_SURFACE ( 'NONE', #11133, 24.00000000002399858 ) ;
#7490=ORIENTED_EDGE ( 'NONE', *, *, #14415, .T. ) ;
#7491=ORIENTED_EDGE ( 'NONE', *, *, #15401, .F. ) ;
#7492=DIRECTION ( 'NONE',  ( -1.000000000000000000, -0.000000000000000000, 0.000000000000000000 ) ) ;
#7493=AXIS2_PLACEMENT_3D ( 'NONE', #14401, #12981, #14111 ) ;
#7494=EDGE_CURVE ( 'NONE', #13122, #7406, #9347, .T. ) ;
#7495=ORIENTED_EDGE ( 'NONE', *, *, #5277, .T. ) ;
#7500=CARTESIAN_POINT ( 'NONE',  ( 10.00000000000000000, -9.823366686500245137, -55.51919907100663920 ) ) ;
#7501=VECTOR ( 'NONE', #3808, 1000.000000000000000 ) ;
#7502=ORIENTED_EDGE ( 'NONE', *, *, #11323, .F. ) ;
#7503=AXIS2_PLACEMENT_3D ( 'NONE', #3784, #11008, #16744 ) ;
#7506=CIRCLE ( 'NONE', #13294, 56.24900000005625600 ) ;
#7507=DIRECTION ( 'NONE',  ( 1.000000000000000000, 0.000000000000000000, 0.000000000000000000 ) ) ;
#7511=EDGE_CURVE ( 'NONE', #14764, #18692, #6006, .T. ) ;
#7512=DIRECTION ( 'NONE',  ( -1.000000000000000000, -0.000000000000000000, 0.000000000000000000 ) ) ;
#7517=CARTESIAN_POINT ( 'NONE',  ( -10.00000000000000000, 0.000000000000000000, 0.000000000000000000 ) ) ;
#7518=ORIENTED_EDGE ( 'NONE', *, *, #11893, .T. ) ;
#7522=AXIS2_PLACEMENT_3D ( 'NONE', #1522, #10095, #1608 ) ;
#7534=DIRECTION ( 'NONE',  ( 1.000000000000000000, 0.000000000000000000, -0.000000000000000000 ) ) ;
#7535=AXIS2_PLACEMENT_3D ( 'NONE', #16586, #8798, #15942 ) ;
#7539=DIRECTION ( 'NONE',  ( -1.000000000000000000, -0.000000000000000000, -0.000000000000000000 ) ) ;
#7540=EDGE_LOOP ( 'NONE', ( #8158, #16024, #8639, #14458 ) ) ;
#7546=AXIS2_PLACEMENT_3D ( 'NONE', #7954, #13767, #8044 ) ;
#7550=ORIENTED_EDGE ( 'NONE', *, *, #14758, .T. ) ;
#7551=DIRECTION ( 'NONE',  ( 0.000000000000000000, 0.7071067811865436870, 0.7071067811865513475 ) ) ;
#7553=CYLINDRICAL_SURFACE ( 'NONE', #4823, 63.00000000006298961 ) ;
#7554=ADVANCED_FACE ( 'NONE', ( #3283 ), #14906, .T. ) ;
#7555=CYLINDRICAL_SURFACE ( 'NONE', #15221, 56.24900000005625600 ) ;
#7556=DIRECTION ( 'NONE',  ( 0.000000000000000000, 0.9510565162951520879, 0.3090169943749517811 ) ) ;
#7557=CIRCLE ( 'NONE', #3016, 24.00000000002399858 ) ;
#7565=CYLINDRICAL_SURFACE ( 'NONE', #13320, 24.00000000002399858 ) ;
#7567=ORIENTED_EDGE ( 'NONE', *, *, #4369, .T. ) ;
#7574=AXIS2_PLACEMENT_3D ( 'NONE', #4041, #18693, #7071 ) ;
#7575=VECTOR ( 'NONE', #7036, 1000.000000000000000 ) ;
#7576=CARTESIAN_POINT ( 'NONE',  ( 4.999999999999999112, -13.79392154159179640, 61.47135697633775209 ) ) ;
#7579=ORIENTED_EDGE ( 'NONE', *, *, #1431, .T. ) ;
#7581=VERTEX_POINT ( 'NONE', #6508 ) ;
#7583=ORIENTED_EDGE ( 'NONE', *, *, #16871, .T. ) ;
#7584=CARTESIAN_POINT ( 'NONE',  ( 0.000000000000000000, -42.79754323328189969, -11.25576474687263229 ) ) ;
#7587=ORIENTED_EDGE ( 'NONE', *, *, #8774, .F. ) ;
#7592=CARTESIAN_POINT ( 'NONE',  ( 10.00000000000000000, 0.000000000000000000, 0.000000000000000000 ) ) ;
#7595=CARTESIAN_POINT ( 'NONE',  ( 4.999999999999999112, 61.03368945066456774, -15.61693798565434044 ) ) ;
#7598=EDGE_LOOP ( 'NONE', ( #15843, #8395, #14802, #4478 ) ) ;
#7602=CARTESIAN_POINT ( 'NONE',  ( 10.00000000000000000, 46.27827401617404490, 31.97297851452441364 ) ) ;
#7604=DIRECTION ( 'NONE',  ( -1.000000000000000000, 0.000000000000000000, 0.000000000000000000 ) ) ;
#7605=VERTEX_POINT ( 'NONE', #1085 ) ;
#7612=ORIENTED_EDGE ( 'NONE', *, *, #9203, .F. ) ;
#7613=FACE_OUTER_BOUND ( 'NONE', #3327, .T. ) ;
#7616=CARTESIAN_POINT ( 'NONE',  ( 0.000000000000000000, -16.45250512421816680, -53.92768374110909235 ) ) ;
#7622=VERTEX_POINT ( 'NONE', #16715 ) ;
#7624=EDGE_CURVE ( 'NONE', #8411, #2359, #12401, .T. ) ;
#7626=DIRECTION ( 'NONE',  ( 0.000000000000000000, 0.000000000000000000, 1.000000000000000000 ) ) ;
#7629=ORIENTED_EDGE ( 'NONE', *, *, #8130, .F. ) ;
#7633=ORIENTED_EDGE ( 'NONE', *, *, #10060, .T. ) ;
#7636=CIRCLE ( 'NONE', #12205, 24.00000000002399858 ) ;
#7640=DIRECTION ( 'NONE',  ( -1.000000000000000000, 0.000000000000000000, 0.000000000000000000 ) ) ;
#7650=DIRECTION ( 'NONE',  ( -1.000000000000000000, 0.000000000000000000, 0.000000000000000000 ) ) ;
#7651=ORIENTED_EDGE ( 'NONE', *, *, #3951, .T. ) ;
#7655=AXIS2_PLACEMENT_3D ( 'NONE', #3073, #8865, #5643 ) ;
#7656=DIRECTION ( 'NONE',  ( 0.000000000000000000, 0.5877852522924744694, -0.8090169943749464521 ) ) ;
#7658=EDGE_CURVE ( 'NONE', #17166, #10426, #16665, .T. ) ;
#7660=DIRECTION ( 'NONE',  ( 0.000000000000000000, 0.000000000000000000, 1.000000000000000000 ) ) ;
#7667=VERTEX_POINT ( 'NONE', #13751 ) ;
#7668=DIRECTION ( 'NONE',  ( -1.000000000000000000, 0.000000000000000000, 0.000000000000000000 ) ) ;
#7669=CYLINDRICAL_SURFACE ( 'NONE', #6794, 24.00000000002399503 ) ;
#7674=ORIENTED_EDGE ( 'NONE', *, *, #16754, .F. ) ;
#7677=AXIS2_PLACEMENT_3D ( 'NONE', #2641, #15506, #2455 ) ;
#7680=ORIENTED_EDGE ( 'NONE', *, *, #13395, .F. ) ;
#7685=CARTESIAN_POINT ( 'NONE',  ( 10.00000000000000000, 40.58063702438398224, -39.14194549634321163 ) ) ;
#7699=FACE_OUTER_BOUND ( 'NONE', #12000, .T. ) ;
#7703=AXIS2_PLACEMENT_3D ( 'NONE', #7843, #7738, #13665 ) ;
#7705=DIRECTION ( 'NONE',  ( -1.000000000000000000, 0.000000000000000000, 0.000000000000000000 ) ) ;
#7709=DIRECTION ( 'NONE',  ( -1.000000000000000000, 0.000000000000000000, -0.000000000000000000 ) ) ;
#7714=CYLINDRICAL_SURFACE ( 'NONE', #17031, 24.00000000002399858 ) ;
#7715=EDGE_LOOP ( 'NONE', ( #18646, #11820, #18119, #13945 ) ) ;
#7716=ADVANCED_FACE ( 'NONE', ( #15652 ), #7162, .T. ) ;
#7722=VERTEX_POINT ( 'NONE', #16027 ) ;
#7723=EDGE_CURVE ( 'NONE', #607, #10140, #8510, .T. ) ;
#7725=ORIENTED_EDGE ( 'NONE', *, *, #13700, .F. ) ;
#7733=FACE_OUTER_BOUND ( 'NONE', #12583, .T. ) ;
#7738=DIRECTION ( 'NONE',  ( -1.000000000000000000, 0.000000000000000000, 0.000000000000000000 ) ) ;
#7741=ORIENTED_EDGE ( 'NONE', *, *, #12735, .F. ) ;
#7746=EDGE_LOOP ( 'NONE', ( #679, #3362, #15853, #18714 ) ) ;
#7747=CIRCLE ( 'NONE', #18390, 63.00000000006298961 ) ;
#7753=VERTEX_POINT ( 'NONE', #8788 ) ;
#7754=CARTESIAN_POINT ( 'NONE',  ( 10.00000000000000000, 0.000000000000000000, 0.000000000000000000 ) ) ;
#7759=CIRCLE ( 'NONE', #3819, 56.24900000005625600 ) ;
#7760=ORIENTED_EDGE ( 'NONE', *, *, #13802, .F. ) ;
#7761=CARTESIAN_POINT ( 'NONE',  ( 10.00000000000000000, 26.49895292618076326, -49.76630880786279931 ) ) ;
#7762=CARTESIAN_POINT ( 'NONE',  ( -10.00000000000000000, 0.000000000000000000, 0.000000000000000000 ) ) ;
#7764=ORIENTED_EDGE ( 'NONE', *, *, #12092, .F. ) ;
#7769=AXIS2_PLACEMENT_3D ( 'NONE', #8809, #11587, #11294 ) ;
#7770=AXIS2_PLACEMENT_3D ( 'NONE', #11378, #17198, #4155 ) ;
#7775=ORIENTED_EDGE ( 'NONE', *, *, #11514, .F. ) ;
#7776=CIRCLE ( 'NONE', #9006, 24.00000000002399858 ) ;
#7777=VERTEX_POINT ( 'NONE', #17095 ) ;
#7779=LINE ( 'NONE', #13705, #6829 ) ;
#7783=ORIENTED_EDGE ( 'NONE', *, *, #4485, .F. ) ;
#7787=CARTESIAN_POINT ( 'NONE',  ( 10.00000000000000000, -55.33199130079777461, -10.11537145609435306 ) ) ;
#7789=LINE ( 'NONE', #9133, #10231 ) ;
#7790=ORIENTED_EDGE ( 'NONE', *, *, #16216, .F. ) ;
#7792=AXIS2_PLACEMENT_3D ( 'NONE', #18670, #18764, #14198 ) ;
#7793=CARTESIAN_POINT ( 'NONE',  ( 0.000000000000000000, -49.49802920186203892, -26.71881558261783951 ) ) ;
#7799=AXIS2_PLACEMENT_3D ( 'NONE', #5981, #17697, #1692 ) ;
#7800=CIRCLE ( 'NONE', #6882, 56.24900000005626310 ) ;
#7801=AXIS2_PLACEMENT_3D ( 'NONE', #13914, #9899, #15818 ) ;
#7804=ORIENTED_EDGE ( 'NONE', *, *, #541, .F. ) ;
#7805=EDGE_CURVE ( 'NONE', #14399, #17073, #17881, .T. ) ;
#7810=AXIS2_PLACEMENT_3D ( 'NONE', #11801, #17608, #3223 ) ;
#7813=DIRECTION ( 'NONE',  ( -1.000000000000000000, -0.000000000000000000, -0.000000000000000000 ) ) ;
#7815=CARTESIAN_POINT ( 'NONE',  ( 5.000000000000000000, -48.50907078259410099, 40.19788616105593348 ) ) ;
#7816=ORIENTED_EDGE ( 'NONE', *, *, #2491, .T. ) ;
#7818=VECTOR ( 'NONE', #16595, 1000.000000000000000 ) ;
#7820=ORIENTED_EDGE ( 'NONE', *, *, #18368, .F. ) ;
#7824=ADVANCED_FACE ( 'NONE', ( #15933 ), #37, .T. ) ;
#7825=ORIENTED_EDGE ( 'NONE', *, *, #11679, .T. ) ;
#7827=DIRECTION ( 'NONE',  ( -1.000000000000000000, 0.000000000000000000, 0.000000000000000000 ) ) ;
#7835=ADVANCED_FACE ( 'NONE', ( #14410 ), #7350, .T. ) ;
#7838=CYLINDRICAL_SURFACE ( 'NONE', #11106, 24.00000000002399503 ) ;
#7841=ORIENTED_EDGE ( 'NONE', *, *, #562, .T. ) ;
#7842=DIRECTION ( 'NONE',  ( 0.000000000000000000, 0.000000000000000000, 1.000000000000000000 ) ) ;
#7843=CARTESIAN_POINT ( 'NONE',  ( 10.00000000000000000, 0.000000000000000000, 0.000000000000000000 ) ) ;
#7844=DIRECTION ( 'NONE',  ( -1.000000000000000000, 0.000000000000000000, 0.000000000000000000 ) ) ;
#7846=ORIENTED_EDGE ( 'NONE', *, *, #14359, .T. ) ;
#7847=VERTEX_POINT ( 'NONE', #17373 ) ;
#7850=VECTOR ( 'NONE', #12002, 1000.000000000000000 ) ;
#7854=CIRCLE ( 'NONE', #18500, 56.24900000005625600 ) ;
#7857=EDGE_CURVE ( 'NONE', #3893, #9406, #11520, .T. ) ;
#7858=DIRECTION ( 'NONE',  ( -1.000000000000000000, -0.000000000000000000, -0.000000000000000000 ) ) ;
#7865=VECTOR ( 'NONE', #18111, 1000.000000000000000 ) ;
#7866=VERTEX_POINT ( 'NONE', #1635 ) ;
#7872=DIRECTION ( 'NONE',  ( 0.000000000000000000, 0.000000000000000000, 1.000000000000000000 ) ) ;
#7875=CARTESIAN_POINT ( 'NONE',  ( 10.00000000000000000, 53.92768374110868734, 16.45250512421953459 ) ) ;
#7877=CARTESIAN_POINT ( 'NONE',  ( 5.000000000000000000, 33.71303790549352186, -53.22058882792159551 ) ) ;
#7879=AXIS2_PLACEMENT_3D ( 'NONE', #8469, #1325, #9707 ) ;
#7881=DIRECTION ( 'NONE',  ( 0.000000000000000000, 0.8090169943749486725, -0.5877852522924713607 ) ) ;
#7884=AXIS2_PLACEMENT_3D ( 'NONE', #8936, #4383, #17794 ) ;
#7885=ORIENTED_EDGE ( 'NONE', *, *, #3262, .F. ) ;
#7886=DIRECTION ( 'NONE',  ( -1.000000000000000000, -0.000000000000000000, -0.000000000000000000 ) ) ;
#7892=CIRCLE ( 'NONE', #3952, 24.00000000002399858 ) ;
#7898=ORIENTED_EDGE ( 'NONE', *, *, #15276, .F. ) ;
#7899=CARTESIAN_POINT ( 'NONE',  ( -10.00000000000000000, -42.79754323328189969, -13.90576474687263264 ) ) ;
#7900=CARTESIAN_POINT ( 'NONE',  ( 0.000000000000000000, 16.45250512421856470, 53.92768374110897156 ) ) ;
#7901=AXIS2_PLACEMENT_3D ( 'NONE', #12874, #4297, #10100 ) ;
#7903=ADVANCED_FACE ( 'NONE', ( #16212 ), #8957, .T. ) ;
#7922=AXIS2_PLACEMENT_3D ( 'NONE', #17444, #14583, #5737 ) ;
#7924=DIRECTION ( 'NONE',  ( 1.000000000000000000, 0.000000000000000000, 0.000000000000000000 ) ) ;
#7933=CARTESIAN_POINT ( 'NONE',  ( 10.00000000000000000, -53.22058882792171630, -33.71303790549333712 ) ) ;
#7936=ORIENTED_EDGE ( 'NONE', *, *, #14244, .T. ) ;
#7943=ORIENTED_EDGE ( 'NONE', *, *, #5867, .F. ) ;
#7944=EDGE_CURVE ( 'NONE', #8606, #12076, #13041, .T. ) ;
#7945=EDGE_CURVE ( 'NONE', #13284, #10808, #6202, .T. ) ;
#7948=DIRECTION ( 'NONE',  ( -1.000000000000000000, 0.000000000000000000, 0.000000000000000000 ) ) ;
#7949=ORIENTED_EDGE ( 'NONE', *, *, #5967, .T. ) ;
#7951=DIRECTION ( 'NONE',  ( -1.000000000000000000, 0.000000000000000000, 0.000000000000000000 ) ) ;
#7954=CARTESIAN_POINT ( 'NONE',  ( 0.000000000000000000, 9.823366686501460165, -55.51919907100641893 ) ) ;
#7958=AXIS2_PLACEMENT_3D ( 'NONE', #3906, #2468, #8283 ) ;
#7959=CARTESIAN_POINT ( 'NONE',  ( 10.00000000000000000, 1.017308535512385870, 56.37237871411034007 ) ) ;
#7962=EDGE_CURVE ( 'NONE', #5427, #17735, #18498, .T. ) ;
#7963=DIRECTION ( 'NONE',  ( -1.000000000000000000, -0.000000000000000000, 0.000000000000000000 ) ) ;
#7965=EDGE_CURVE ( 'NONE', #2359, #13122, #12420, .T. ) ;
#7969=ADVANCED_FACE ( 'NONE', ( #6297 ), #13542, .F. ) ;
#7981=CARTESIAN_POINT ( 'NONE',  ( -10.00000000000000000, 0.000000000000000000, 0.000000000000000000 ) ) ;
#7983=ORIENTED_EDGE ( 'NONE', *, *, #6706, .F. ) ;
#7985=AXIS2_PLACEMENT_3D ( 'NONE', #6270, #13794, #756 ) ;
#7987=DIRECTION ( 'NONE',  ( 0.000000000000000000, 1.000000000000000000, 3.491481338843133355E-15 ) ) ;
#7989=CARTESIAN_POINT ( 'NONE',  ( 0.000000000000000000, 42.79754323328179311, -13.90576474687299680 ) ) ;
#7995=VECTOR ( 'NONE', #14306, 1000.000000000000000 ) ;
#7999=DIRECTION ( 'NONE',  ( -1.000000000000000000, -0.000000000000000000, -0.000000000000000000 ) ) ;
#8000=DIRECTION ( 'NONE',  ( 0.000000000000000000, -0.4539904997395350916, -0.8910065241883737830 ) ) ;
#8008=EDGE_CURVE ( 'NONE', #8632, #11858, #13731, .T. ) ;
#8009=AXIS2_PLACEMENT_3D ( 'NONE', #15775, #9958, #8707 ) ;
#8010=VERTEX_POINT ( 'NONE', #15445 ) ;
#8011=ORIENTED_EDGE ( 'NONE', *, *, #3824, .T. ) ;
#8015=CARTESIAN_POINT ( 'NONE',  ( 10.00000000000000000, 0.000000000000000000, 0.000000000000000000 ) ) ;
#8017=AXIS2_PLACEMENT_3D ( 'NONE', #12801, #14324, #9934 ) ;
#8018=CARTESIAN_POINT ( 'NONE',  ( 10.00000000000000000, -26.71881558261695133, -49.49802920186252209 ) ) ;
#8020=CARTESIAN_POINT ( 'NONE',  ( 0.000000000000000000, -31.97297851452390915, -46.27827401617439307 ) ) ;
#8022=DIRECTION ( 'NONE',  ( 0.000000000000000000, 0.7071067811865486830, -0.7071067811865463515 ) ) ;
#8023=VERTEX_POINT ( 'NONE', #13814 ) ;
#8025=DIRECTION ( 'NONE',  ( -1.000000000000000000, -0.000000000000000000, -0.000000000000000000 ) ) ;
#8032=DIRECTION ( 'NONE',  ( 0.000000000000000000, 0.000000000000000000, 1.000000000000000000 ) ) ;
#8037=DIRECTION ( 'NONE',  ( 0.000000000000000000, 0.000000000000000000, 1.000000000000000000 ) ) ;
#8038=ORIENTED_EDGE ( 'NONE', *, *, #14776, .F. ) ;
#8039=EDGE_CURVE ( 'NONE', #9028, #5885, #10287, .T. ) ;
#8041=EDGE_CURVE ( 'NONE', #16577, #7464, #4805, .T. ) ;
#8042=ORIENTED_EDGE ( 'NONE', *, *, #17293, .T. ) ;
#8044=DIRECTION ( 'NONE',  ( 0.000000000000000000, -0.8090169943749402348, -0.5877852522924830181 ) ) ;
#8045=ORIENTED_EDGE ( 'NONE', *, *, #2535, .T. ) ;
#8048=LINE ( 'NONE', #9286, #7178 ) ;
#8049=CYLINDRICAL_SURFACE ( 'NONE', #10137, 24.00000000002399858 ) ;
#8051=ORIENTED_EDGE ( 'NONE', *, *, #18511, .F. ) ;
#8056=ORIENTED_EDGE ( 'NONE', *, *, #5110, .F. ) ;
#8059=VECTOR ( 'NONE', #12753, 1000.000000000000000 ) ;
#8066=CARTESIAN_POINT ( 'NONE',  ( 10.00000000000000000, -42.79754323328189969, -16.55576474687263300 ) ) ;
#8069=ORIENTED_EDGE ( 'NONE', *, *, #18302, .F. ) ;
#8071=DIRECTION ( 'NONE',  ( 0.000000000000000000, 0.000000000000000000, 1.000000000000000000 ) ) ;
#8073=ORIENTED_EDGE ( 'NONE', *, *, #13595, .F. ) ;
#8077=DIRECTION ( 'NONE',  ( 0.000000000000000000, 0.000000000000000000, 1.000000000000000000 ) ) ;
#8078=CYLINDRICAL_SURFACE ( 'NONE', #14380, 63.00000000006298961 ) ;
#8080=ORIENTED_EDGE ( 'NONE', *, *, #13975, .F. ) ;
#8083=ORIENTED_EDGE ( 'NONE', *, *, #11068, .F. ) ;
#8084=DIRECTION ( 'NONE',  ( -1.000000000000000000, 0.000000000000000000, -0.000000000000000000 ) ) ;
#8088=EDGE_CURVE ( 'NONE', #3360, #18126, #9438, .T. ) ;
#8089=AXIS2_PLACEMENT_3D ( 'NONE', #8525, #1297, #6321 ) ;
#8090=ORIENTED_EDGE ( 'NONE', *, *, #7130, .T. ) ;
#8093=AXIS2_PLACEMENT_3D ( 'NONE', #16810, #3583, #16617 ) ;
#8095=LINE ( 'NONE', #13910, #2337 ) ;
#8096=CIRCLE ( 'NONE', #18746, 56.24900000005625600 ) ;
#8104=DIRECTION ( 'NONE',  ( 0.000000000000000000, 0.000000000000000000, 1.000000000000000000 ) ) ;
#8105=EDGE_CURVE ( 'NONE', #11121, #11814, #6397, .T. ) ;
#8107=ORIENTED_EDGE ( 'NONE', *, *, #16099, .F. ) ;
#8108=AXIS2_PLACEMENT_3D ( 'NONE', #14804, #15095, #3102 ) ;
#8110=CIRCLE ( 'NONE', #7801, 56.24900000005625600 ) ;
#8111=ORIENTED_EDGE ( 'NONE', *, *, #15403, .T. ) ;
#8112=AXIS2_PLACEMENT_3D ( 'NONE', #6026, #321, #13178 ) ;
#8115=ORIENTED_EDGE ( 'NONE', *, *, #5822, .F. ) ;
#8117=DIRECTION ( 'NONE',  ( 0.000000000000000000, 0.1564344650402312575, -0.9876883405951376593 ) ) ;
#8118=CARTESIAN_POINT ( 'NONE',  ( 0.000000000000000000, -33.95787273855213328, -45.00825343885058061 ) ) ;
#8123=CARTESIAN_POINT ( 'NONE',  ( 0.000000000000000000, -10.11537145609335653, -55.33199130079795225 ) ) ;
#8124=VECTOR ( 'NONE', #5297, 1000.000000000000000 ) ;
#8125=DIRECTION ( 'NONE',  ( 0.000000000000000000, 0.000000000000000000, 1.000000000000000000 ) ) ;
#8130=EDGE_CURVE ( 'NONE', #10934, #451, #10857, .T. ) ;
#8131=CARTESIAN_POINT ( 'NONE',  ( 10.00000000000000000, -34.13306034420217827, 44.70888270294149436 ) ) ;
#8133=ORIENTED_EDGE ( 'NONE', *, *, #17033, .T. ) ;
#8135=DIRECTION ( 'NONE',  ( 0.000000000000000000, 0.000000000000000000, 1.000000000000000000 ) ) ;
#8138=ORIENTED_EDGE ( 'NONE', *, *, #14359, .F. ) ;
#8141=AXIS2_PLACEMENT_3D ( 'NONE', #12149, #4623, #10430 ) ;
#8147=FACE_OUTER_BOUND ( 'NONE', #11800, .T. ) ;
#8152=EDGE_LOOP ( 'NONE', ( #12776, #512, #3798, #5876 ) ) ;
#8154=CYLINDRICAL_SURFACE ( 'NONE', #4151, 24.00000000002399858 ) ;
#8156=DIRECTION ( 'NONE',  ( 1.000000000000000000, -0.000000000000000000, -0.000000000000000000 ) ) ;
#8158=ORIENTED_EDGE ( 'NONE', *, *, #11514, .T. ) ;
#8163=ORIENTED_EDGE ( 'NONE', *, *, #2202, .F. ) ;
#8169=CIRCLE ( 'NONE', #17905, 63.00000000006298961 ) ;
#8173=VERTEX_POINT ( 'NONE', #5241 ) ;
#8177=ORIENTED_EDGE ( 'NONE', *, *, #3516, .F. ) ;
#8179=ORIENTED_EDGE ( 'NONE', *, *, #5234, .T. ) ;
#8181=DIRECTION ( 'NONE',  ( 0.000000000000000000, 0.000000000000000000, 1.000000000000000000 ) ) ;
#8183=ORIENTED_EDGE ( 'NONE', *, *, #396, .F. ) ;
#8184=ORIENTED_EDGE ( 'NONE', *, *, #18761, .F. ) ;
#8186=VERTEX_POINT ( 'NONE', #11046 ) ;
#8193=EDGE_CURVE ( 'NONE', #17735, #5117, #15157, .T. ) ;
#8195=ORIENTED_EDGE ( 'NONE', *, *, #3067, .F. ) ;
#8199=DIRECTION ( 'NONE',  ( 0.000000000000000000, 0.1564344650402243464, 0.9876883405951388806 ) ) ;
#8201=DIRECTION ( 'NONE',  ( -1.000000000000000000, -0.000000000000000000, -0.000000000000000000 ) ) ;
#8202=FACE_BOUND ( 'NONE', #17901, .T. ) ;
#8207=EDGE_LOOP ( 'NONE', ( #4576, #8409, #1048, #18510 ) ) ;
#8209=DIRECTION ( 'NONE',  ( 0.000000000000000000, 0.000000000000000000, 1.000000000000000000 ) ) ;
#8210=DIRECTION ( 'NONE',  ( 0.000000000000000000, 0.000000000000000000, 1.000000000000000000 ) ) ;
#8211=CARTESIAN_POINT ( 'NONE',  ( 10.00000000000000000, -44.70888270294186384, 34.13306034420170931 ) ) ;
#8212=EDGE_CURVE ( 'NONE', #5044, #18322, #4301, .T. ) ;
#8214=AXIS2_PLACEMENT_3D ( 'NONE', #697, #2029, #11056 ) ;
#8220=CARTESIAN_POINT ( 'NONE',  ( 10.00000000000000000, -24.33982105418938602, 50.71018745830434682 ) ) ;
#8221=DIRECTION ( 'NONE',  ( 0.000000000000000000, 0.000000000000000000, 1.000000000000000000 ) ) ;
#8222=CIRCLE ( 'NONE', #9421, 24.00000000002399858 ) ;
#8224=FACE_OUTER_BOUND ( 'NONE', #8782, .T. ) ;
#8225=VECTOR ( 'NONE', #11282, 1000.000000000000000 ) ;
#8227=DIRECTION ( 'NONE',  ( -1.000000000000000000, -0.000000000000000000, -0.000000000000000000 ) ) ;
#8231=CARTESIAN_POINT ( 'NONE',  ( 0.000000000000000000, 0.000000000000000000, 0.000000000000000000 ) ) ;
#8232=ORIENTED_EDGE ( 'NONE', *, *, #14283, .F. ) ;
#8233=FACE_OUTER_BOUND ( 'NONE', #13260, .T. ) ;
#8242=EDGE_CURVE ( 'NONE', #1465, #1879, #14264, .T. ) ;
#8243=CYLINDRICAL_SURFACE ( 'NONE', #8093, 63.00000000006298961 ) ;
#8246=DIRECTION ( 'NONE',  ( 0.000000000000000000, 0.000000000000000000, 1.000000000000000000 ) ) ;
#8247=ORIENTED_EDGE ( 'NONE', *, *, #1001, .T. ) ;
#8250=VECTOR ( 'NONE', #1715, 1000.000000000000000 ) ;
#8254=ORIENTED_EDGE ( 'NONE', *, *, #8875, .T. ) ;
#8257=LINE ( 'NONE', #9488, #5944 ) ;
#8259=EDGE_CURVE ( 'NONE', #1496, #8307, #18674, .T. ) ;
#8263=AXIS2_PLACEMENT_3D ( 'NONE', #10901, #16729, #8246 ) ;
#8272=CARTESIAN_POINT ( 'NONE',  ( 0.000000000000000000, 0.000000000000000000, 0.000000000000000000 ) ) ;
#8273=ORIENTED_EDGE ( 'NONE', *, *, #18511, .T. ) ;
#8274=CARTESIAN_POINT ( 'NONE',  ( 0.000000000000000000, -15.61693798565454827, -61.03368945066451801 ) ) ;
#8279=ORIENTED_EDGE ( 'NONE', *, *, #7362, .T. ) ;
#8280=DIRECTION ( 'NONE',  ( 0.000000000000000000, 0.7071067811865439090, 0.7071067811865511255 ) ) ;
#8281=ORIENTED_EDGE ( 'NONE', *, *, #3241, .F. ) ;
#8282=DIRECTION ( 'NONE',  ( -1.000000000000000000, -0.000000000000000000, -0.000000000000000000 ) ) ;
#8283=DIRECTION ( 'NONE',  ( 0.000000000000000000, 0.000000000000000000, 1.000000000000000000 ) ) ;
#8287=DIRECTION ( 'NONE',  ( 0.000000000000000000, 0.000000000000000000, 1.000000000000000000 ) ) ;
#8293=EDGE_CURVE ( 'NONE', #5770, #9182, #17255, .T. ) ;
#8301=CARTESIAN_POINT ( 'NONE',  ( 10.00000000000000000, -45.00825343885045271, 33.95787273855228960 ) ) ;
#8303=ADVANCED_BREP_SHAPE_REPRESENTATION ( '', ( #9854, #8017 ), #2559 ) ;
#8305=EDGE_LOOP ( 'NONE', ( #17888, #1347, #7185, #14407 ) ) ;
#8306=AXIS2_PLACEMENT_3D ( 'NONE', #16074, #3030, #15886 ) ;
#8307=VERTEX_POINT ( 'NONE', #4210 ) ;
#8310=AXIS2_PLACEMENT_3D ( 'NONE', #7989, #2182, #763 ) ;
#8314=DIRECTION ( 'NONE',  ( 0.000000000000000000, 0.000000000000000000, -1.000000000000000000 ) ) ;
#8317=ADVANCED_FACE ( 'NONE', ( #7699 ), #11985, .T. ) ;
#8319=CARTESIAN_POINT ( 'NONE',  ( 10.00000000000000000, -61.47135697633788709, 13.79392154159114092 ) ) ;
#8323=ORIENTED_EDGE ( 'NONE', *, *, #10175, .F. ) ;
#8326=CARTESIAN_POINT ( 'NONE',  ( 0.000000000000000000, -38.81885513160016643, 40.70683587897944022 ) ) ;
#8330=CARTESIAN_POINT ( 'NONE',  ( 10.00000000000000000, -53.29895248911662264, -18.38754094778296277 ) ) ;
#8335=CIRCLE ( 'NONE', #1634, 56.24900000005625600 ) ;
#8338=LINE ( 'NONE', #5279, #9338 ) ;
#8339=CARTESIAN_POINT ( 'NONE',  ( 10.00000000000000000, 0.000000000000000000, 0.000000000000000000 ) ) ;
#8342=CARTESIAN_POINT ( 'NONE',  ( 10.00000000000000000, 7.813799127874054840, -55.83748330407399152 ) ) ;
#8344=CARTESIAN_POINT ( 'NONE',  ( 0.000000000000000000, 49.76630880786309064, 26.49895292618021614 ) ) ;
#8345=ORIENTED_EDGE ( 'NONE', *, *, #11334, .T. ) ;
#8346=ORIENTED_EDGE ( 'NONE', *, *, #18566, .F. ) ;
#8347=EDGE_CURVE ( 'NONE', #10140, #3048, #11205, .T. ) ;
#8348=DIRECTION ( 'NONE',  ( 0.000000000000000000, -1.000000000000000000, -1.040834085585043434E-14 ) ) ;
#8350=DIRECTION ( 'NONE',  ( -1.000000000000000000, -0.000000000000000000, -0.000000000000000000 ) ) ;
#8356=CARTESIAN_POINT ( 'NONE',  ( 5.000000000000000000, 62.87238730325621106, -4.007856633823612569 ) ) ;
#8359=AXIS2_PLACEMENT_3D ( 'NONE', #17513, #5893, #3224 ) ;
#8362=VERTEX_POINT ( 'NONE', #14860 ) ;
#8364=DIRECTION ( 'NONE',  ( 0.000000000000000000, 0.000000000000000000, -1.000000000000000000 ) ) ;
#8367=EDGE_CURVE ( 'NONE', #5418, #16626, #13349, .T. ) ;
#8370=CARTESIAN_POINT ( 'NONE',  ( -10.00000000000000000, -42.79754323328189969, -16.55576474687263300 ) ) ;
#8371=CYLINDRICAL_SURFACE ( 'NONE', #7958, 56.24900000005625600 ) ;
#8377=AXIS2_PLACEMENT_3D ( 'NONE', #12059, #13692, #12248 ) ;
#8386=DIRECTION ( 'NONE',  ( -1.000000000000000000, 0.000000000000000000, 0.000000000000000000 ) ) ;
#8389=VERTEX_POINT ( 'NONE', #3344 ) ;
#8391=VECTOR ( 'NONE', #12985, 1000.000000000000000 ) ;
#8395=ORIENTED_EDGE ( 'NONE', *, *, #7658, .T. ) ;
#8398=CIRCLE ( 'NONE', #5666, 24.00000000002399858 ) ;
#8399=AXIS2_PLACEMENT_3D ( 'NONE', #10457, #8934, #191 ) ;
#8406=CARTESIAN_POINT ( 'NONE',  ( 0.000000000000000000, 0.000000000000000000, 0.000000000000000000 ) ) ;
#8408=CARTESIAN_POINT ( 'NONE',  ( 0.000000000000000000, 0.000000000000000000, 0.000000000000000000 ) ) ;
#8409=ORIENTED_EDGE ( 'NONE', *, *, #7723, .F. ) ;
#8411=VERTEX_POINT ( 'NONE', #9139 ) ;
#8414=DIRECTION ( 'NONE',  ( -1.000000000000000000, 0.000000000000000000, 0.000000000000000000 ) ) ;
#8417=AXIS2_PLACEMENT_3D ( 'NONE', #3867, #17022, #6631 ) ;
#8421=ORIENTED_EDGE ( 'NONE', *, *, #2354, .T. ) ;
#8423=EDGE_CURVE ( 'NONE', #16326, #13451, #11533, .T. ) ;
#8425=AXIS2_PLACEMENT_3D ( 'NONE', #16859, #2380, #8199 ) ;
#8432=DIRECTION ( 'NONE',  ( 0.000000000000000000, 0.000000000000000000, -1.000000000000000000 ) ) ;
#8438=DIRECTION ( 'NONE',  ( 0.000000000000000000, 0.000000000000000000, 1.000000000000000000 ) ) ;
#8439=DIRECTION ( 'NONE',  ( 1.000000000000000000, 0.000000000000000000, 0.000000000000000000 ) ) ;
#8440=AXIS2_PLACEMENT_3D ( 'NONE', #9211, #7604, #11974 ) ;
#8441=VERTEX_POINT ( 'NONE', #16192 ) ;
#8443=CYLINDRICAL_SURFACE ( 'NONE', #12342, 24.00000000002399503 ) ;
#8447=CYLINDRICAL_SURFACE ( 'NONE', #15812, 24.00000000002399858 ) ;
#8453=ORIENTED_EDGE ( 'NONE', *, *, #15278, .T. ) ;
#8460=ORIENTED_EDGE ( 'NONE', *, *, #1001, .F. ) ;
#8464=DIRECTION ( 'NONE',  ( 0.000000000000000000, 0.1564344650402244297, 0.9876883405951387696 ) ) ;
#8465=VERTEX_POINT ( 'NONE', #7420 ) ;
#8467=DIRECTION ( 'NONE',  ( -1.000000000000000000, 0.000000000000000000, 0.000000000000000000 ) ) ;
#8468=ORIENTED_EDGE ( 'NONE', *, *, #13180, .F. ) ;
#8469=CARTESIAN_POINT ( 'NONE',  ( 0.000000000000000000, 26.45033635316149301, 36.40576474687247099 ) ) ;
#8474=EDGE_CURVE ( 'NONE', #1940, #11202, #4570, .T. ) ;
#8475=EDGE_LOOP ( 'NONE', ( #4994, #13413, #2276, #8732 ) ) ;
#8476=ORIENTED_EDGE ( 'NONE', *, *, #15774, .F. ) ;
#8477=DIRECTION ( 'NONE',  ( 0.000000000000000000, 0.000000000000000000, 1.000000000000000000 ) ) ;
#8482=CARTESIAN_POINT ( 'NONE',  ( 0.000000000000000000, -62.72529079327811274, 5.876895005582225551 ) ) ;
#8484=AXIS2_PLACEMENT_3D ( 'NONE', #12854, #5607, #7656 ) ;
#8489=CARTESIAN_POINT ( 'NONE',  ( 10.00000000000000000, 4.007856633824264492, -62.87238730325616132 ) ) ;
#8502=CARTESIAN_POINT ( 'NONE',  ( 0.000000000000000000, -44.70888270294185673, 34.13306034420170221 ) ) ;
#8505=CARTESIAN_POINT ( 'NONE',  ( 5.000000000000000000, 15.61693798565496394, 61.03368945066441142 ) ) ;
#8509=DIRECTION ( 'NONE',  ( 0.000000000000000000, 0.3090169943749411785, 0.9510565162951555296 ) ) ;
#8510=LINE ( 'NONE', #5835, #11180 ) ;
#8517=CARTESIAN_POINT ( 'NONE',  ( 10.00000000000000000, -26.45033635316118747, 36.40576474687271258 ) ) ;
#8525=CARTESIAN_POINT ( 'NONE',  ( 10.00000000000000000, 0.000000000000000000, 0.000000000000000000 ) ) ;
#8530=AXIS2_PLACEMENT_3D ( 'NONE', #17016, #12814, #3965 ) ;
#8534=ADVANCED_FACE ( 'NONE', ( #13622 ), #18181, .F. ) ;
#8537=EDGE_CURVE ( 'NONE', #17827, #8441, #1192, .T. ) ;
#8538=DIRECTION ( 'NONE',  ( 0.000000000000000000, 1.000000000000000000, 3.491481338843133355E-15 ) ) ;
#8540=DIRECTION ( 'NONE',  ( 1.000000000000000000, -0.000000000000000000, 0.000000000000000000 ) ) ;
#8542=CARTESIAN_POINT ( 'NONE',  ( 10.00000000000000000, 61.47135697633797946, -13.79392154159067196 ) ) ;
#8551=CARTESIAN_POINT ( 'NONE',  ( 4.999999999999999112, -4.007856633823834613, 62.87238730325619684 ) ) ;
#8556=EDGE_CURVE ( 'NONE', #5984, #3048, #5131, .T. ) ;
#8557=ORIENTED_EDGE ( 'NONE', *, *, #9581, .T. ) ;
#8559=DIRECTION ( 'NONE',  ( 0.000000000000000000, 0.9510565162951545304, -0.3090169943749446202 ) ) ;
#8560=EDGE_CURVE ( 'NONE', #2359, #16326, #2369, .T. ) ;
#8561=CIRCLE ( 'NONE', #13725, 24.00000000002399503 ) ;
#8565=ORIENTED_EDGE ( 'NONE', *, *, #13530, .F. ) ;
#8566=DIRECTION ( 'NONE',  ( -1.000000000000000000, 0.000000000000000000, 0.000000000000000000 ) ) ;
#8578=DIRECTION ( 'NONE',  ( 0.000000000000000000, -0.1564344650402381964, 0.9876883405951365491 ) ) ;
#8580=EDGE_CURVE ( 'NONE', #15091, #5686, #9704, .T. ) ;
#8581=ORIENTED_EDGE ( 'NONE', *, *, #2944, .F. ) ;
#8584=CARTESIAN_POINT ( 'NONE',  ( 10.00000000000000000, 0.000000000000000000, 0.000000000000000000 ) ) ;
#8588=DIRECTION ( 'NONE',  ( 0.000000000000000000, 0.4539904997395412534, 0.8910065241883706744 ) ) ;
#8591=ORIENTED_EDGE ( 'NONE', *, *, #12638, .T. ) ;
#8593=ORIENTED_EDGE ( 'NONE', *, *, #1231, .T. ) ;
#8601=VECTOR ( 'NONE', #10282, 1000.000000000000000 ) ;
#8603=ORIENTED_EDGE ( 'NONE', *, *, #4568, .T. ) ;
#8604=AXIS2_PLACEMENT_3D ( 'NONE', #18396, #15555, #2502 ) ;
#8606=VERTEX_POINT ( 'NONE', #17993 ) ;
#8607=DIRECTION ( 'NONE',  ( -1.000000000000000000, 0.000000000000000000, -0.000000000000000000 ) ) ;
#8612=AXIS2_PLACEMENT_3D ( 'NONE', #13591, #16448, #9005 ) ;
#8617=FACE_OUTER_BOUND ( 'NONE', #3541, .T. ) ;
#8626=CYLINDRICAL_SURFACE ( 'NONE', #10270, 56.24900000005625600 ) ;
#8629=EDGE_CURVE ( 'NONE', #8023, #15168, #15498, .T. ) ;
#8632=VERTEX_POINT ( 'NONE', #18652 ) ;
#8636=CARTESIAN_POINT ( 'NONE',  ( 0.000000000000000000, -58.55669782892444886, -23.24033432160500823 ) ) ;
#8638=ORIENTED_EDGE ( 'NONE', *, *, #4241, .F. ) ;
#8639=ORIENTED_EDGE ( 'NONE', *, *, #12620, .F. ) ;
#8648=ADVANCED_FACE ( 'NONE', ( #12939 ), #5606, .T. ) ;
#8651=ORIENTED_EDGE ( 'NONE', *, *, #6208, .T. ) ;
#8658=CARTESIAN_POINT ( 'NONE',  ( 10.00000000000000000, -1.017308535511979972, -56.37237871411034718 ) ) ;
#8659=EDGE_CURVE ( 'NONE', #14764, #4178, #11319, .T. ) ;
#8670=ORIENTED_EDGE ( 'NONE', *, *, #11534, .F. ) ;
#8671=EDGE_CURVE ( 'NONE', #1723, #3100, #2557, .T. ) ;
#8675=DIRECTION ( 'NONE',  ( 0.000000000000000000, 0.000000000000000000, -1.000000000000000000 ) ) ;
#8680=DIRECTION ( 'NONE',  ( 1.000000000000000000, 0.000000000000000000, 0.000000000000000000 ) ) ;
#8684=VERTEX_POINT ( 'NONE', #18468 ) ;
#8685=FACE_OUTER_BOUND ( 'NONE', #6570, .T. ) ;
#8690=AXIS2_PLACEMENT_3D ( 'NONE', #7875, #7492, #261 ) ;
#8692=VERTEX_POINT ( 'NONE', #2756 ) ;
#8695=DIRECTION ( 'NONE',  ( 0.000000000000000000, 0.000000000000000000, 1.000000000000000000 ) ) ;
#8696=DIRECTION ( 'NONE',  ( -1.000000000000000000, 0.000000000000000000, 0.000000000000000000 ) ) ;
#8698=CARTESIAN_POINT ( 'NONE',  ( 10.00000000000000000, 0.000000000000000000, 0.000000000000000000 ) ) ;
#8699=EDGE_CURVE ( 'NONE', #10072, #2652, #14085, .T. ) ;
#8700=CARTESIAN_POINT ( 'NONE',  ( 10.00000000000000000, 0.000000000000000000, 0.000000000000000000 ) ) ;
#8701=CIRCLE ( 'NONE', #18439, 63.00000000006298961 ) ;
#8702=CIRCLE ( 'NONE', #201, 56.24900000005625600 ) ;
#8703=DIRECTION ( 'NONE',  ( 0.000000000000000000, 0.000000000000000000, 1.000000000000000000 ) ) ;
#8706=CARTESIAN_POINT ( 'NONE',  ( 0.000000000000000000, 18.64666490672447097, -53.06836994729213330 ) ) ;
#8707=DIRECTION ( 'NONE',  ( 0.000000000000000000, -0.8090169943749402348, -0.5877852522924830181 ) ) ;
#8709=VERTEX_POINT ( 'NONE', #15892 ) ;
#8710=ORIENTED_EDGE ( 'NONE', *, *, #15790, .T. ) ;
#8713=CIRCLE ( 'NONE', #2023, 56.24900000005626310 ) ;
#8715=CIRCLE ( 'NONE', #2028, 56.24900000005625600 ) ;
#8719=CARTESIAN_POINT ( 'NONE',  ( 0.000000000000000000, 0.000000000000000000, 0.000000000000000000 ) ) ;
#8723=DIRECTION ( 'NONE',  ( 1.000000000000000000, 0.000000000000000000, 0.000000000000000000 ) ) ;
#8728=EDGE_LOOP ( 'NONE', ( #319, #18492, #12844, #11674 ) ) ;
#8731=AXIS2_PLACEMENT_3D ( 'NONE', #9045, #4577, #12347 ) ;
#8732=ORIENTED_EDGE ( 'NONE', *, *, #9650, .T. ) ;
#8735=CYLINDRICAL_SURFACE ( 'NONE', #11768, 56.24900000005625600 ) ;
#8736=VERTEX_POINT ( 'NONE', #5521 ) ;
#8737=DIRECTION ( 'NONE',  ( -1.000000000000000000, -0.000000000000000000, -0.000000000000000000 ) ) ;
#8741=EDGE_LOOP ( 'NONE', ( #4907, #488, #3404, #14730 ) ) ;
#8747=ORIENTED_EDGE ( 'NONE', *, *, #1305, .T. ) ;
#8750=DIRECTION ( 'NONE',  ( -1.000000000000000000, 0.000000000000000000, 0.000000000000000000 ) ) ;
#8751=AXIS2_PLACEMENT_3D ( 'NONE', #11084, #12438, #16819 ) ;
#8753=ORIENTED_EDGE ( 'NONE', *, *, #2535, .F. ) ;
#8760=VERTEX_POINT ( 'NONE', #17501 ) ;
#8762=FACE_BOUND ( 'NONE', #117, .T. ) ;
#8764=AXIS2_PLACEMENT_3D ( 'NONE', #6854, #6961, #16776 ) ;
#8767=EDGE_CURVE ( 'NONE', #1784, #10254, #16409, .T. ) ;
#8770=EDGE_LOOP ( 'NONE', ( #2020, #18450, #2961, #10023 ) ) ;
#8773=CARTESIAN_POINT ( 'NONE',  ( 10.00000000000000000, -26.71881558261766898, 49.49802920186213129 ) ) ;
#8774=EDGE_CURVE ( 'NONE', #8186, #13820, #6051, .T. ) ;
#8775=ORIENTED_EDGE ( 'NONE', *, *, #14780, .T. ) ;
#8779=DIRECTION ( 'NONE',  ( 0.000000000000000000, 0.000000000000000000, 1.000000000000000000 ) ) ;
#8780=CARTESIAN_POINT ( 'NONE',  ( 10.00000000000000000, 4.007856633823390524, 62.87238730325622527 ) ) ;
#8782=EDGE_LOOP ( 'NONE', ( #8133, #16516, #2493, #359 ) ) ;
#8786=ADVANCED_FACE ( 'NONE', ( #263 ), #10169, .T. ) ;
#8788=CARTESIAN_POINT ( 'NONE',  ( 0.000000000000000000, 24.33982105418901298, 50.71018745830453156 ) ) ;
#8789=VECTOR ( 'NONE', #16508, 1000.000000000000000 ) ;
#8790=ORIENTED_EDGE ( 'NONE', *, *, #1555, .F. ) ;
#8793=CIRCLE ( 'NONE', #3938, 63.00000000006298961 ) ;
#8795=CARTESIAN_POINT ( 'NONE',  ( 0.000000000000000000, -5.876895005581972420, -62.72529079327814117 ) ) ;
#8797=CIRCLE ( 'NONE', #10916, 24.00000000002399858 ) ;
#8798=DIRECTION ( 'NONE',  ( -1.000000000000000000, 0.000000000000000000, -0.000000000000000000 ) ) ;
#8801=CARTESIAN_POINT ( 'NONE',  ( 10.00000000000000000, -47.29147401531984229, 41.62350880771904826 ) ) ;
#8808=ORIENTED_EDGE ( 'NONE', *, *, #13401, .F. ) ;
#8809=CARTESIAN_POINT ( 'NONE',  ( 0.000000000000000000, 0.000000000000000000, 0.000000000000000000 ) ) ;
#8811=CIRCLE ( 'NONE', #6685, 56.24900000005625600 ) ;
#8813=VECTOR ( 'NONE', #11373, 1000.000000000000000 ) ;
#8830=DIRECTION ( 'NONE',  ( 0.000000000000000000, 0.000000000000000000, 1.000000000000000000 ) ) ;
#8841=EDGE_CURVE ( 'NONE', #6436, #15930, #16712, .T. ) ;
#8843=DIRECTION ( 'NONE',  ( 0.000000000000000000, -1.000000000000000000, -1.040834085585043434E-14 ) ) ;
#8853=VECTOR ( 'NONE', #2604, 1000.000000000000000 ) ;
#8854=ADVANCED_FACE ( 'NONE', ( #7403 ), #357, .T. ) ;
#8855=VERTEX_POINT ( 'NONE', #16362 ) ;
#8857=ADVANCED_FACE ( 'NONE', ( #1598 ), #13317, .T. ) ;
#8859=VERTEX_POINT ( 'NONE', #9116 ) ;
#8860=DIRECTION ( 'NONE',  ( -1.000000000000000000, 0.000000000000000000, 0.000000000000000000 ) ) ;
#8865=DIRECTION ( 'NONE',  ( -1.000000000000000000, -0.000000000000000000, -0.000000000000000000 ) ) ;
#8866=DIRECTION ( 'NONE',  ( -1.000000000000000000, -0.000000000000000000, -0.000000000000000000 ) ) ;
#8867=VERTEX_POINT ( 'NONE', #3124 ) ;
#8869=EDGE_LOOP ( 'NONE', ( #17319, #16550, #5437, #8710 ) ) ;
#8871=DIRECTION ( 'NONE',  ( 0.000000000000000000, 0.000000000000000000, 1.000000000000000000 ) ) ;
#8873=SHAPE_DEFINITION_REPRESENTATION ( #4958, #5670 ) ;
#8874=VERTEX_POINT ( 'NONE', #11609 ) ;
#8875=EDGE_CURVE ( 'NONE', #79, #1653, #6070, .T. ) ;
#8880=EDGE_CURVE ( 'NONE', #10905, #3687, #10720, .T. ) ;
#8881=CARTESIAN_POINT ( 'NONE',  ( 10.00000000000000000, 53.89344778774834310, -16.10733642026427148 ) ) ;
#8884=AXIS2_PLACEMENT_3D ( 'NONE', #339, #13391, #8559 ) ;
#8887=DIRECTION ( 'NONE',  ( -1.000000000000000000, -0.000000000000000000, 0.000000000000000000 ) ) ;
#8892=DIRECTION ( 'NONE',  ( -1.000000000000000000, 0.000000000000000000, 0.000000000000000000 ) ) ;
#8894=AXIS2_PLACEMENT_3D ( 'NONE', #5846, #11660, #10228 ) ;
#8897=VERTEX_POINT ( 'NONE', #11004 ) ;
#8901=DIRECTION ( 'NONE',  ( -1.000000000000000000, 0.000000000000000000, -0.000000000000000000 ) ) ;
#8903=AXIS2_PLACEMENT_3D ( 'NONE', #10997, #2528, #12821 ) ;
#8904=CYLINDRICAL_SURFACE ( 'NONE', #3217, 2.649999999999999467 ) ;
#8906=CIRCLE ( 'NONE', #1310, 63.00000000006298961 ) ;
#8907=CARTESIAN_POINT ( 'NONE',  ( 10.00000000000000000, 56.23315539212690339, -1.335003989221823062 ) ) ;
#8909=CYLINDRICAL_SURFACE ( 'NONE', #17679, 24.00000000002400213 ) ;
#8911=DIRECTION ( 'NONE',  ( -1.000000000000000000, -0.000000000000000000, -0.000000000000000000 ) ) ;
#8913=EDGE_CURVE ( 'NONE', #7210, #14803, #2072, .T. ) ;
#8914=DIRECTION ( 'NONE',  ( 0.000000000000000000, 0.000000000000000000, 1.000000000000000000 ) ) ;
#8917=EDGE_LOOP ( 'NONE', ( #5311, #6220, #2831, #10317 ) ) ;
#8918=CARTESIAN_POINT ( 'NONE',  ( 10.00000000000000000, -40.70683587897930522, -38.81885513160031564 ) ) ;
#8921=ORIENTED_EDGE ( 'NONE', *, *, #648, .T. ) ;
#8924=ORIENTED_EDGE ( 'NONE', *, *, #6208, .F. ) ;
#8925=VERTEX_POINT ( 'NONE', #9577 ) ;
#8926=FACE_OUTER_BOUND ( 'NONE', #9525, .T. ) ;
#8927=CARTESIAN_POINT ( 'NONE',  ( 0.000000000000000000, -53.89344778774823652, 16.10733642026462675 ) ) ;
#8930=CARTESIAN_POINT ( 'NONE',  ( 10.00000000000000000, 58.55669782892493203, -23.24033432160376478 ) ) ;
#8934=DIRECTION ( 'NONE',  ( -1.000000000000000000, -0.000000000000000000, -0.000000000000000000 ) ) ;
#8936=CARTESIAN_POINT ( 'NONE',  ( 10.00000000000000000, 0.000000000000000000, 0.000000000000000000 ) ) ;
#8939=DIRECTION ( 'NONE',  ( 0.000000000000000000, -0.9876883405951359940, -0.1564344650402419989 ) ) ;
#8940=FACE_BOUND ( 'NONE', #9910, .T. ) ;
#8943=ORIENTED_EDGE ( 'NONE', *, *, #465, .T. ) ;
#8948=DIRECTION ( 'NONE',  ( 0.000000000000000000, 0.000000000000000000, -1.000000000000000000 ) ) ;
#8952=DIRECTION ( 'NONE',  ( 0.000000000000000000, -0.5877852522924623679, -0.8090169943749552228 ) ) ;
#8957=CYLINDRICAL_SURFACE ( 'NONE', #11191, 24.00000000002399858 ) ;
#8961=ORIENTED_EDGE ( 'NONE', *, *, #66, .T. ) ;
#8966=FACE_OUTER_BOUND ( 'NONE', #2931, .T. ) ;
#8967=CARTESIAN_POINT ( 'NONE',  ( 0.000000000000000000, -46.27827401617427228, 31.97297851452409034 ) ) ;
#8968=DIRECTION ( 'NONE',  ( -1.000000000000000000, 0.000000000000000000, 0.000000000000000000 ) ) ;
#8970=AXIS2_PLACEMENT_3D ( 'NONE', #9508, #1143, #8280 ) ;
#8971=CARTESIAN_POINT ( 'NONE',  ( 0.000000000000000000, 13.79392154159134876, 61.47135697633785156 ) ) ;
#8973=ORIENTED_EDGE ( 'NONE', *, *, #4649, .T. ) ;
#8974=CARTESIAN_POINT ( 'NONE',  ( 10.00000000000000000, 0.000000000000000000, 0.000000000000000000 ) ) ;
#8975=DIRECTION ( 'NONE',  ( -1.000000000000000000, -0.000000000000000000, -0.000000000000000000 ) ) ;
#8976=CARTESIAN_POINT ( 'NONE',  ( 10.00000000000000000, -40.58063702438372644, 39.14194549634347453 ) ) ;
#8981=ADVANCED_FACE ( 'NONE', ( #5003 ), #6252, .T. ) ;
#8987=ORIENTED_EDGE ( 'NONE', *, *, #3061, .T. ) ;
#8989=CIRCLE ( 'NONE', #17510, 24.00000000002399858 ) ;
#8990=AXIS2_PLACEMENT_3D ( 'NONE', #15948, #5490, #4061 ) ;
#8991=CARTESIAN_POINT ( 'NONE',  ( 10.00000000000000000, 55.74967257055894265, -7.478235706488370660 ) ) ;
#8992=CARTESIAN_POINT ( 'NONE',  ( 10.00000000000000000, 0.000000000000000000, 0.000000000000000000 ) ) ;
#8995=DIRECTION ( 'NONE',  ( 0.000000000000000000, 0.8910065241883656784, 0.4539904997395510788 ) ) ;
#8996=VECTOR ( 'NONE', #6086, 1000.000000000000000 ) ;
#8997=ORIENTED_EDGE ( 'NONE', *, *, #8629, .T. ) ;
#8998=DIRECTION ( 'NONE',  ( 0.000000000000000000, 0.000000000000000000, -1.000000000000000000 ) ) ;
#9005=DIRECTION ( 'NONE',  ( 0.000000000000000000, 0.000000000000000000, -1.000000000000000000 ) ) ;
#9006=AXIS2_PLACEMENT_3D ( 'NONE', #1942, #17948, #17574 ) ;
#9010=CARTESIAN_POINT ( 'NONE',  ( 10.00000000000000000, -18.64666490672410148, 53.06836994729227541 ) ) ;
#9012=EDGE_LOOP ( 'NONE', ( #146, #7284, #13021, #15038 ) ) ;
#9015=CIRCLE ( 'NONE', #12686, 63.00000000006298961 ) ;
#9017=ADVANCED_FACE ( 'NONE', ( #15121 ), #13779, .T. ) ;
#9018=DIRECTION ( 'NONE',  ( -1.000000000000000000, -0.000000000000000000, 0.000000000000000000 ) ) ;
#9019=CIRCLE ( 'NONE', #6280, 24.00000000002399148 ) ;
#9020=CIRCLE ( 'NONE', #5063, 56.24900000005625600 ) ;
#9022=AXIS2_PLACEMENT_3D ( 'NONE', #15621, #3811, #12670 ) ;
#9025=DIRECTION ( 'NONE',  ( -1.000000000000000000, 0.000000000000000000, 0.000000000000000000 ) ) ;
#9028=VERTEX_POINT ( 'NONE', #12827 ) ;
#9029=CARTESIAN_POINT ( 'NONE',  ( 10.00000000000000000, -41.62350880771954564, 47.29147401531940176 ) ) ;
#9035=CARTESIAN_POINT ( 'NONE',  ( 10.00000000000000000, 53.89344778774812994, 16.10733642026502466 ) ) ;
#9037=CARTESIAN_POINT ( 'NONE',  ( 0.000000000000000000, 0.000000000000000000, 0.000000000000000000 ) ) ;
#9041=AXIS2_PLACEMENT_3D ( 'NONE', #11955, #13490, #431 ) ;
#9044=ORIENTED_EDGE ( 'NONE', *, *, #10591, .F. ) ;
#9045=CARTESIAN_POINT ( 'NONE',  ( 10.00000000000000000, 0.000000000000000000, 0.000000000000000000 ) ) ;
#9049=DIRECTION ( 'NONE',  ( 0.000000000000000000, 0.000000000000000000, 1.000000000000000000 ) ) ;
#9051=AXIS2_PLACEMENT_3D ( 'NONE', #237, #6324, #11941 ) ;
#9052=FACE_OUTER_BOUND ( 'NONE', #12024, .T. ) ;
#9053=DIRECTION ( 'NONE',  ( 0.000000000000000000, 0.000000000000000000, 1.000000000000000000 ) ) ;
#9059=EDGE_CURVE ( 'NONE', #10237, #12166, #7892, .T. ) ;
#9062=DIRECTION ( 'NONE',  ( -1.000000000000000000, -0.000000000000000000, 0.000000000000000000 ) ) ;
#9065=ORIENTED_EDGE ( 'NONE', *, *, #12, .T. ) ;
#9066=AXIS2_PLACEMENT_3D ( 'NONE', #17681, #14724, #6350 ) ;
#9067=AXIS2_PLACEMENT_3D ( 'NONE', #6970, #4021, #8578 ) ;
#9073=DIRECTION ( 'NONE',  ( 1.000000000000000000, 0.000000000000000000, 0.000000000000000000 ) ) ;
#9076=LINE ( 'NONE', #13744, #16957 ) ;
#9078=DIRECTION ( 'NONE',  ( -1.000000000000000000, -0.000000000000000000, -0.000000000000000000 ) ) ;
#9079=CARTESIAN_POINT ( 'NONE',  ( 10.00000000000000000, -55.51919907100644735, -9.823366686501268319 ) ) ;
#9082=AXIS2_PLACEMENT_3D ( 'NONE', #13521, #16004, #11815 ) ;
#9085=CIRCLE ( 'NONE', #8484, 24.00000000002400569 ) ;
#9086=AXIS2_PLACEMENT_3D ( 'NONE', #15901, #15988, #11420 ) ;
#9089=CIRCLE ( 'NONE', #895, 2.649999999999999467 ) ;
#9090=CARTESIAN_POINT ( 'NONE',  ( 10.00000000000000000, 33.71303790549275448, 53.22058882792208578 ) ) ;
#9092=DIRECTION ( 'NONE',  ( 0.000000000000000000, 0.000000000000000000, 1.000000000000000000 ) ) ;
#9094=AXIS2_PLACEMENT_3D ( 'NONE', #2108, #15336, #6394 ) ;
#9097=FACE_OUTER_BOUND ( 'NONE', #15059, .T. ) ;
#9098=DIRECTION ( 'NONE',  ( -1.000000000000000000, 0.000000000000000000, 0.000000000000000000 ) ) ;
#9104=CARTESIAN_POINT ( 'NONE',  ( 10.00000000000000000, -46.20417134726153563, 32.31183295104756326 ) ) ;
#9106=ADVANCED_FACE ( 'NONE', ( #4163 ), #5585, .T. ) ;
#9108=CARTESIAN_POINT ( 'NONE',  ( -10.00000000000000000, 0.000000000000000000, 0.000000000000000000 ) ) ;
#9116=CARTESIAN_POINT ( 'NONE',  ( 10.00000000000000000, 56.23315539212690339, -1.335003989221823062 ) ) ;
#9123=ADVANCED_FACE ( 'NONE', ( #2629 ), #8447, .T. ) ;
#9124=ORIENTED_EDGE ( 'NONE', *, *, #4832, .F. ) ;
#9128=VERTEX_POINT ( 'NONE', #9679 ) ;
#9133=CARTESIAN_POINT ( 'NONE',  ( 5.000000000000000000, 47.29147401532013362, -41.62350880771872852 ) ) ;
#9134=ORIENTED_EDGE ( 'NONE', *, *, #17857, .F. ) ;
#9139=CARTESIAN_POINT ( 'NONE',  ( 10.00000000000000000, -55.83748330407401284, 16.18620087215011338 ) ) ;
#9144=ORIENTED_EDGE ( 'NONE', *, *, #12611, .F. ) ;
#9147=DIRECTION ( 'NONE',  ( 0.000000000000000000, 0.000000000000000000, 1.000000000000000000 ) ) ;
#9160=VECTOR ( 'NONE', #5556, 1000.000000000000000 ) ;
#9163=VECTOR ( 'NONE', #5132, 1000.000000000000000 ) ;
#9164=CARTESIAN_POINT ( 'NONE',  ( 10.00000000000000000, -45.00825343884996954, -33.95787273855293620 ) ) ;
#9168=DIRECTION ( 'NONE',  ( 0.000000000000000000, -0.4539904997395351471, -0.8910065241883737830 ) ) ;
#9169=ORIENTED_EDGE ( 'NONE', *, *, #16808, .T. ) ;
#9173=DIRECTION ( 'NONE',  ( 0.000000000000000000, 0.4539904997395412534, 0.8910065241883705633 ) ) ;
#9174=DIRECTION ( 'NONE',  ( -1.000000000000000000, -0.000000000000000000, 0.000000000000000000 ) ) ;
#9175=DIRECTION ( 'NONE',  ( 0.000000000000000000, 0.000000000000000000, 1.000000000000000000 ) ) ;
#9177=ORIENTED_EDGE ( 'NONE', *, *, #11793, .F. ) ;
#9180=AXIS2_PLACEMENT_3D ( 'NONE', #14466, #2859, #15994 ) ;
#9182=VERTEX_POINT ( 'NONE', #16791 ) ;
#9183=EDGE_CURVE ( 'NONE', #10830, #6436, #15349, .T. ) ;
#9189=EDGE_CURVE ( 'NONE', #380, #7033, #593, .T. ) ;
#9194=CARTESIAN_POINT ( 'NONE',  ( 0.000000000000000000, -61.47135697633769524, -13.79392154159200068 ) ) ;
#9197=VERTEX_POINT ( 'NONE', #12120 ) ;
#9199=LINE ( 'NONE', #8918, #11417 ) ;
#9203=EDGE_CURVE ( 'NONE', #7581, #11551, #10686, .T. ) ;
#9207=PRODUCT ( 'spur gear 1_iso_ISO - Spur gear 3M 40T 20PA 10FW ---S40A75H50L60.0N', 'spur gear 1_iso_ISO - Spur gear 3M 40T 20PA 10FW ---S40A75H50L60.0N', '', ( #130 ) ) ;
#9210=LINE ( 'NONE', #13984, #11093 ) ;
#9211=CARTESIAN_POINT ( 'NONE',  ( 10.00000000000000000, -56.37237871411034718, 1.017308535512174261 ) ) ;
#9220=CARTESIAN_POINT ( 'NONE',  ( 10.00000000000000000, 55.33199130079785277, 10.11537145609396404 ) ) ;
#9225=ADVANCED_FACE ( 'NONE', ( #9539 ), #902, .T. ) ;
#9231=DIRECTION ( 'NONE',  ( 1.000000000000000000, 0.000000000000000000, 0.000000000000000000 ) ) ;
#9232=ADVANCED_FACE ( 'NONE', ( #2301 ), #3832, .T. ) ;
#9239=DIRECTION ( 'NONE',  ( 1.000000000000000000, -0.000000000000000000, -0.000000000000000000 ) ) ;
#9240=ORIENTED_EDGE ( 'NONE', *, *, #14283, .T. ) ;
#9241=CARTESIAN_POINT ( 'NONE',  ( 10.00000000000000000, 0.000000000000000000, 0.000000000000000000 ) ) ;
#9246=EDGE_CURVE ( 'NONE', #16356, #1379, #6599, .T. ) ;
#9252=CARTESIAN_POINT ( 'NONE',  ( 0.000000000000000000, 0.000000000000000000, 0.000000000000000000 ) ) ;
#9253=CARTESIAN_POINT ( 'NONE',  ( -10.00000000000000000, -26.45033635316118747, 36.40576474687271258 ) ) ;
#9259=FACE_OUTER_BOUND ( 'NONE', #5020, .T. ) ;
#9271=CYLINDRICAL_SURFACE ( 'NONE', #18409, 63.00000000006298961 ) ;
#9275=CARTESIAN_POINT ( 'NONE',  ( 10.00000000000000000, -42.79754323328189969, -13.90576474687263264 ) ) ;
#9285=ORIENTED_EDGE ( 'NONE', *, *, #5027, .F. ) ;
#9286=CARTESIAN_POINT ( 'NONE',  ( 4.999999999999999112, 24.97244012287502102, 57.83923611457328207 ) ) ;
#9287=CARTESIAN_POINT ( 'NONE',  ( 0.000000000000000000, -55.74967257055877212, -7.478235706489567924 ) ) ;
#9288=ORIENTED_EDGE ( 'NONE', *, *, #4908, .T. ) ;
#9292=VERTEX_POINT ( 'NONE', #920 ) ;
#9294=AXIS2_PLACEMENT_3D ( 'NONE', #4894, #11143, #610 ) ;
#9303=DIRECTION ( 'NONE',  ( -1.000000000000000000, 0.000000000000000000, -0.000000000000000000 ) ) ;
#9305=VERTEX_POINT ( 'NONE', #6718 ) ;
#9308=CARTESIAN_POINT ( 'NONE',  ( 0.000000000000000000, 56.23315539212690339, -1.335003989221823062 ) ) ;
#9311=CARTESIAN_POINT ( 'NONE',  ( 4.999999999999999112, -54.20017844242534721, 32.11449294037177538 ) ) ;
#9314=DIRECTION ( 'NONE',  ( -1.000000000000000000, 0.000000000000000000, 0.000000000000000000 ) ) ;
#9315=VERTEX_POINT ( 'NONE', #10897 ) ;
#9326=LINE ( 'NONE', #12284, #1136 ) ;
#9330=AXIS2_PLACEMENT_3D ( 'NONE', #3332, #14742, #363 ) ;
#9335=EDGE_CURVE ( 'NONE', #4356, #10680, #16123, .T. ) ;
#9338=VECTOR ( 'NONE', #13848, 1000.000000000000000 ) ;
#9342=ORIENTED_EDGE ( 'NONE', *, *, #141, .F. ) ;
#9343=ORIENTED_EDGE ( 'NONE', *, *, #17857, .T. ) ;
#9347=CIRCLE ( 'NONE', #13625, 24.00000000002399858 ) ;
#9348=LINE ( 'NONE', #16788, #14189 ) ;
#9350=CIRCLE ( 'NONE', #553, 24.00000000002399148 ) ;
#9352=DIRECTION ( 'NONE',  ( -1.000000000000000000, -0.000000000000000000, -0.000000000000000000 ) ) ;
#9358=DIRECTION ( 'NONE',  ( 0.000000000000000000, 0.000000000000000000, -1.000000000000000000 ) ) ;
#9361=ORIENTED_EDGE ( 'NONE', *, *, #11326, .F. ) ;
#9362=ADVANCED_FACE ( 'NONE', ( #13580 ), #10795, .T. ) ;
#9367=ORIENTED_EDGE ( 'NONE', *, *, #15278, .F. ) ;
#9373=DIRECTION ( 'NONE',  ( -1.000000000000000000, -0.000000000000000000, -0.000000000000000000 ) ) ;
#9374=ORIENTED_EDGE ( 'NONE', *, *, #15636, .F. ) ;
#9378=DIRECTION ( 'NONE',  ( 0.000000000000000000, 0.000000000000000000, 1.000000000000000000 ) ) ;
#9379=CARTESIAN_POINT ( 'NONE',  ( 10.00000000000000000, 32.31183295104772668, 46.20417134726143615 ) ) ;
#9381=DIRECTION ( 'NONE',  ( 0.000000000000000000, 0.000000000000000000, 1.000000000000000000 ) ) ;
#9382=VERTEX_POINT ( 'NONE', #5278 ) ;
#9383=DIRECTION ( 'NONE',  ( -1.000000000000000000, 0.000000000000000000, 0.000000000000000000 ) ) ;
#9384=VECTOR ( 'NONE', #4386, 1000.000000000000000 ) ;
#9391=CARTESIAN_POINT ( 'NONE',  ( 0.000000000000000000, -49.76630880786289879, -26.49895292618059273 ) ) ;
#9392=DIRECTION ( 'NONE',  ( -1.000000000000000000, -0.000000000000000000, -0.000000000000000000 ) ) ;
#9398=ORIENTED_EDGE ( 'NONE', *, *, #18415, .T. ) ;
#9401=CARTESIAN_POINT ( 'NONE',  ( 0.000000000000000000, 0.000000000000000000, 0.000000000000000000 ) ) ;
#9406=VERTEX_POINT ( 'NONE', #12811 ) ;
#9412=EDGE_CURVE ( 'NONE', #5044, #5875, #16435, .T. ) ;
#9419=DIRECTION ( 'NONE',  ( -1.000000000000000000, -0.000000000000000000, -0.000000000000000000 ) ) ;
#9421=AXIS2_PLACEMENT_3D ( 'NONE', #4337, #11486, #14425 ) ;
#9422=AXIS2_PLACEMENT_3D ( 'NONE', #11656, #4327, #14784 ) ;
#9424=ORIENTED_EDGE ( 'NONE', *, *, #562, .F. ) ;
#9430=EDGE_CURVE ( 'NONE', #8692, #15353, #2430, .T. ) ;
#9431=DIRECTION ( 'NONE',  ( -1.000000000000000000, 0.000000000000000000, 0.000000000000000000 ) ) ;
#9435=DIRECTION ( 'NONE',  ( -1.000000000000000000, -0.000000000000000000, 0.000000000000000000 ) ) ;
#9438=LINE ( 'NONE', #7815, #13632 ) ;
#9444=ORIENTED_EDGE ( 'NONE', *, *, #3407, .T. ) ;
#9452=CARTESIAN_POINT ( 'NONE',  ( 10.00000000000000000, -7.478235706489372525, 55.74967257055880054 ) ) ;
#9460=VERTEX_POINT ( 'NONE', #3858 ) ;
#9463=AXIS2_PLACEMENT_3D ( 'NONE', #17866, #17763, #5953 ) ;
#9469=ADVANCED_FACE ( 'NONE', ( #18705 ), #11476, .T. ) ;
#9475=AXIS2_PLACEMENT_3D ( 'NONE', #8700, #13376, #4515 ) ;
#9479=ORIENTED_EDGE ( 'NONE', *, *, #5167, .T. ) ;
#9480=EDGE_CURVE ( 'NONE', #10707, #1691, #9761, .T. ) ;
#9483=CIRCLE ( 'NONE', #18011, 24.00000000002399503 ) ;
#9487=ORIENTED_EDGE ( 'NONE', *, *, #5167, .F. ) ;
#9488=CARTESIAN_POINT ( 'NONE',  ( -10.00000000000000000, 26.45033635316149301, 39.05576474687247668 ) ) ;
#9492=AXIS2_PLACEMENT_3D ( 'NONE', #1660, #16151, #9092 ) ;
#9493=CARTESIAN_POINT ( 'NONE',  ( 0.000000000000000000, 0.000000000000000000, 0.000000000000000000 ) ) ;
#9497=ORIENTED_EDGE ( 'NONE', *, *, #7196, .T. ) ;
#9499=DIRECTION ( 'NONE',  ( -1.000000000000000000, 0.000000000000000000, 0.000000000000000000 ) ) ;
#9507=EDGE_LOOP ( 'NONE', ( #17269, #3358, #4670, #14890 ) ) ;
#9508=CARTESIAN_POINT ( 'NONE',  ( 10.00000000000000000, -53.29895248911688554, 18.38754094778222026 ) ) ;
#9512=CIRCLE ( 'NONE', #7384, 24.00000000002400213 ) ;
#9515=EDGE_CURVE ( 'NONE', #8709, #4490, #11572, .T. ) ;
#9517=ORIENTED_EDGE ( 'NONE', *, *, #740, .T. ) ;
#9519=CLOSED_SHELL ( 'NONE', ( #5978, #15376, #13782, #2139, #7969, #5952, #500, #13771, #4255, #13736, #2937, #129, #4940, #15659, #7716, #17789, #866, #1899, #10486, #3413, #13777, #4514, #16582, #10640, #9225, #17835, #13193, #4531, #3361, #3647, #17721, #17460, #3176, #14484, #2446, #15643, #5808, #170, #6160, #18066, #723, #15304, #16194, #15135, #1047, #13571, #18135, #14271, #18086, #13904, #4620, #11452, #9017, #8317, #4359, #10864, #9566, #4195, #515, #11321, #11081, #15006, #10626, #16452, #8648, #3718, #4935, #16112, #7039, #730, #5144, #11076, #1054, #3432, #11033, #13902, #8786, #5453, #7903, #871, #2967, #9817, #15520, #12662, #4719, #6105, #2936, #269, #15099, #2114, #3335, #17524, #17772, #2000, #6663, #12018, #12815, #13215, #7835, #6681, #6802, #2779, #15210, #9106, #18257, #3167, #9830, #6576, #17628, #17924, #4683, #5648, #3411, #18519, #13371, #2793, #2798, #2729, #17995, #623, #17647, #6499, #16239, #18179, #3851, #12152, #16941, #8857, #3201, #4477, #17580, #12010, #4012, #8854, #18721, #2129, #9956, #9823, #9232, #10726, #18112, #7444, #7824, #16564, #3928, #18655, #8981, #17439, #12146, #14309, #15832, #1655, #13873, #9469, #16467, #9123, #10307, #1962, #18660, #18093, #7554, #12165, #17720, #10724, #9979, #324, #18785, #9362, #10225, #10411, #17165, #4928, #6449, #15936, #1502, #15177, #16944, #15642, #8534 ) ) ;
#9522=DIRECTION ( 'NONE',  ( 0.000000000000000000, -0.3090169943749547787, 0.9510565162951511997 ) ) ;
#9525=EDGE_LOOP ( 'NONE', ( #40, #6444, #8111, #7372 ) ) ;
#9533=ORIENTED_EDGE ( 'NONE', *, *, #16153, .T. ) ;
#9534=ORIENTED_EDGE ( 'NONE', *, *, #15401, .T. ) ;
#9537=DIRECTION ( 'NONE',  ( -1.000000000000000000, 0.000000000000000000, 0.000000000000000000 ) ) ;
#9539=FACE_OUTER_BOUND ( 'NONE', #12457, .T. ) ;
#9540=AXIS2_PLACEMENT_3D ( 'NONE', #4320, #15932, #14227 ) ;
#9543=LINE ( 'NONE', #10971, #2588 ) ;
#9544=ORIENTED_EDGE ( 'NONE', *, *, #12189, .F. ) ;
#9545=DIRECTION ( 'NONE',  ( -1.000000000000000000, 0.000000000000000000, 0.000000000000000000 ) ) ;
#9554=ORIENTED_EDGE ( 'NONE', *, *, #9412, .T. ) ;
#9558=ORIENTED_EDGE ( 'NONE', *, *, #13123, .T. ) ;
#9564=EDGE_CURVE ( 'NONE', #16736, #9315, #4554, .T. ) ;
#9566=ADVANCED_FACE ( 'NONE', ( #2998 ), #16311, .T. ) ;
#9571=CIRCLE ( 'NONE', #13266, 63.00000000006298961 ) ;
#9576=VERTEX_POINT ( 'NONE', #17464 ) ;
#9577=CARTESIAN_POINT ( 'NONE',  ( 0.000000000000000000, 4.007856633824268044, -62.87238730325617553 ) ) ;
#9578=EDGE_CURVE ( 'NONE', #5984, #1496, #10941, .T. ) ;
#9580=CARTESIAN_POINT ( 'NONE',  ( 0.000000000000000000, 0.000000000000000000, 0.000000000000000000 ) ) ;
#9581=EDGE_CURVE ( 'NONE', #8760, #5879, #4601, .T. ) ;
#9588=DIRECTION ( 'NONE',  ( 0.000000000000000000, 0.000000000000000000, 1.000000000000000000 ) ) ;
#9591=LINE ( 'NONE', #3792, #16955 ) ;
#9593=VERTEX_POINT ( 'NONE', #8881 ) ;
#9595=LINE ( 'NONE', #12465, #16696 ) ;
#9601=CARTESIAN_POINT ( 'NONE',  ( 0.000000000000000000, 0.000000000000000000, 0.000000000000000000 ) ) ;
#9602=DIRECTION ( 'NONE',  ( 0.000000000000000000, 0.000000000000000000, 1.000000000000000000 ) ) ;
#9603=AXIS2_PLACEMENT_3D ( 'NONE', #16154, #12041, #625 ) ;
#9606=VECTOR ( 'NONE', #12138, 1000.000000000000000 ) ;
#9612=CARTESIAN_POINT ( 'NONE',  ( 10.00000000000000000, 49.49802920186260735, -26.71881558261677370 ) ) ;
#9616=DIRECTION ( 'NONE',  ( 0.000000000000000000, 0.000000000000000000, 1.000000000000000000 ) ) ;
#9617=CARTESIAN_POINT ( 'NONE',  ( 0.000000000000000000, 0.000000000000000000, 0.000000000000000000 ) ) ;
#9622=DIRECTION ( 'NONE',  ( 0.000000000000000000, -0.4539904997395351471, -0.8910065241883737830 ) ) ;
#9626=CIRCLE ( 'NONE', #12058, 63.00000000006298961 ) ;
#9637=DIRECTION ( 'NONE',  ( 0.000000000000000000, 0.000000000000000000, -1.000000000000000000 ) ) ;
#9638=CARTESIAN_POINT ( 'NONE',  ( 10.00000000000000000, -5.120903701083534543E-13, -45.00000000000000000 ) ) ;
#9641=EDGE_CURVE ( 'NONE', #12447, #8465, #10058, .T. ) ;
#9645=DIRECTION ( 'NONE',  ( 0.000000000000000000, 0.000000000000000000, 1.000000000000000000 ) ) ;
#9646=ORIENTED_EDGE ( 'NONE', *, *, #12611, .T. ) ;
#9650=EDGE_CURVE ( 'NONE', #16064, #6648, #14923, .T. ) ;
#9651=DIRECTION ( 'NONE',  ( 0.000000000000000000, 0.000000000000000000, 1.000000000000000000 ) ) ;
#9653=EDGE_LOOP ( 'NONE', ( #16296, #5266, #14630, #11870 ) ) ;
#9654=ORIENTED_EDGE ( 'NONE', *, *, #815, .F. ) ;
#9658=AXIS2_PLACEMENT_3D ( 'NONE', #15752, #17284, #13086 ) ;
#9659=AXIS2_PLACEMENT_3D ( 'NONE', #10393, #1274, #17448 ) ;
#9665=EDGE_LOOP ( 'NONE', ( #8183, #13464, #11115, #15051 ) ) ;
#9670=LINE ( 'NONE', #15490, #10427 ) ;
#9673=ORIENTED_EDGE ( 'NONE', *, *, #4631, .F. ) ;
#9676=DIRECTION ( 'NONE',  ( 0.000000000000000000, 0.000000000000000000, 1.000000000000000000 ) ) ;
#9679=CARTESIAN_POINT ( 'NONE',  ( 10.00000000000000000, -57.83923611457302627, -24.97244012287563919 ) ) ;
#9682=LINE ( 'NONE', #12738, #14763 ) ;
#9686=CARTESIAN_POINT ( 'NONE',  ( 0.000000000000000000, -7.813799127872885997, -55.83748330407415494 ) ) ;
#9687=EDGE_LOOP ( 'NONE', ( #8557, #14281, #10623, #3607 ) ) ;
#9692=CARTESIAN_POINT ( 'NONE',  ( 10.00000000000000000, -50.69000562871659810, 24.68609584167141691 ) ) ;
#9694=ORIENTED_EDGE ( 'NONE', *, *, #11334, .F. ) ;
#9702=ORIENTED_EDGE ( 'NONE', *, *, #456, .T. ) ;
#9703=DIRECTION ( 'NONE',  ( 0.000000000000000000, 0.000000000000000000, 1.000000000000000000 ) ) ;
#9704=CIRCLE ( 'NONE', #7269, 56.24900000005625600 ) ;
#9707=DIRECTION ( 'NONE',  ( 0.000000000000000000, 0.000000000000000000, -1.000000000000000000 ) ) ;
#9712=AXIS2_PLACEMENT_3D ( 'NONE', #1082, #17452, #15842 ) ;
#9717=DIRECTION ( 'NONE',  ( -1.000000000000000000, 0.000000000000000000, -0.000000000000000000 ) ) ;
#9720=EDGE_CURVE ( 'NONE', #7866, #14075, #943, .T. ) ;
#9721=CARTESIAN_POINT ( 'NONE',  ( 0.000000000000000000, 0.000000000000000000, 0.000000000000000000 ) ) ;
#9722=CARTESIAN_POINT ( 'NONE',  ( 5.000000000000000000, 40.19788616105610402, 48.50907078259395888 ) ) ;
#9725=ORIENTED_EDGE ( 'NONE', *, *, #3407, .F. ) ;
#9727=CARTESIAN_POINT ( 'NONE',  ( 0.000000000000000000, 0.000000000000000000, 0.000000000000000000 ) ) ;
#9733=ORIENTED_EDGE ( 'NONE', *, *, #5246, .T. ) ;
#9735=ORIENTED_EDGE ( 'NONE', *, *, #18200, .T. ) ;
#9736=CARTESIAN_POINT ( 'NONE',  ( 10.00000000000000000, 53.29895248911675765, 18.38754094778260040 ) ) ;
#9737=( NAMED_UNIT ( * ) PLANE_ANGLE_UNIT ( ) SI_UNIT ( $, .RADIAN. ) );
#9741=DIRECTION ( 'NONE',  ( 1.000000000000000000, 0.000000000000000000, 0.000000000000000000 ) ) ;
#9744=DIRECTION ( 'NONE',  ( 0.000000000000000000, 0.000000000000000000, 1.000000000000000000 ) ) ;
#9747=ORIENTED_EDGE ( 'NONE', *, *, #7213, .T. ) ;
#9752=ORIENTED_EDGE ( 'NONE', *, *, #14589, .F. ) ;
#9756=DIRECTION ( 'NONE',  ( -1.000000000000000000, 0.000000000000000000, 0.000000000000000000 ) ) ;
#9759=AXIS2_PLACEMENT_3D ( 'NONE', #13931, #18593, #11445 ) ;
#9761=LINE ( 'NONE', #17104, #8225 ) ;
#9762=DIRECTION ( 'NONE',  ( -1.000000000000000000, -0.000000000000000000, -0.000000000000000000 ) ) ;
#9764=CARTESIAN_POINT ( 'NONE',  ( 10.00000000000000000, 0.000000000000000000, 0.000000000000000000 ) ) ;
#9766=DIRECTION ( 'NONE',  ( 0.000000000000000000, 0.000000000000000000, 1.000000000000000000 ) ) ;
#9770=DIRECTION ( 'NONE',  ( -1.000000000000000000, 0.000000000000000000, 0.000000000000000000 ) ) ;
#9776=EDGE_CURVE ( 'NONE', #5801, #16413, #1835, .T. ) ;
#9778=EDGE_CURVE ( 'NONE', #7033, #8362, #3060, .T. ) ;
#9779=DIRECTION ( 'NONE',  ( 0.000000000000000000, 0.8090169943749445647, 0.5877852522924770229 ) ) ;
#9783=CIRCLE ( 'NONE', #2802, 56.24900000005625600 ) ;
#9784=EDGE_LOOP ( 'NONE', ( #13564, #10763 ) ) ;
#9786=LINE ( 'NONE', #17659, #14224 ) ;
#9798=ORIENTED_EDGE ( 'NONE', *, *, #11534, .T. ) ;
#9800=CARTESIAN_POINT ( 'NONE',  ( 0.000000000000000000, 33.95787273855309252, -45.00825343884985585 ) ) ;
#9807=CARTESIAN_POINT ( 'NONE',  ( 10.00000000000000000, 0.000000000000000000, 0.000000000000000000 ) ) ;
#9811=CARTESIAN_POINT ( 'NONE',  ( 10.00000000000000000, -53.92768374110902840, 16.45250512421837641 ) ) ;
#9817=ADVANCED_FACE ( 'NONE', ( #11353 ), #15456, .T. ) ;
#9819=DIRECTION ( 'NONE',  ( 0.000000000000000000, 0.000000000000000000, 1.000000000000000000 ) ) ;
#9822=DIRECTION ( 'NONE',  ( -1.000000000000000000, 0.000000000000000000, 0.000000000000000000 ) ) ;
#9823=ADVANCED_FACE ( 'NONE', ( #5252 ), #14026, .T. ) ;
#9824=EDGE_LOOP ( 'NONE', ( #9177, #4228, #8195, #8056 ) ) ;
#9826=AXIS2_PLACEMENT_3D ( 'NONE', #7762, #14827, #10714 ) ;
#9830=ADVANCED_FACE ( 'NONE', ( #899 ), #17267, .T. ) ;
#9831=CARTESIAN_POINT ( 'NONE',  ( 10.00000000000000000, -7.813799127872885997, -55.83748330407415494 ) ) ;
#9834=DIRECTION ( 'NONE',  ( 0.000000000000000000, 0.000000000000000000, 1.000000000000000000 ) ) ;
#9837=CARTESIAN_POINT ( 'NONE',  ( 10.00000000000000000, 0.000000000000000000, 0.000000000000000000 ) ) ;
#9840=ORIENTED_EDGE ( 'NONE', *, *, #7377, .T. ) ;
#9843=LINE ( 'NONE', #5362, #6490 ) ;
#9844=CARTESIAN_POINT ( 'NONE',  ( 10.00000000000000000, -56.37237871411032586, -1.017308535512989609 ) ) ;
#9848=CARTESIAN_POINT ( 'NONE',  ( 10.00000000000000000, 0.000000000000000000, 0.000000000000000000 ) ) ;
#9852=DIRECTION ( 'NONE',  ( 0.000000000000000000, 0.5877852522924685852, 0.8090169943749505599 ) ) ;
#9854=MANIFOLD_SOLID_BREP ( 'M5 Clearance Hole1', #9519 ) ;
#9855=DIRECTION ( 'NONE',  ( -1.000000000000000000, 0.000000000000000000, 0.000000000000000000 ) ) ;
#9859=FACE_OUTER_BOUND ( 'NONE', #17568, .T. ) ;
#9860=CARTESIAN_POINT ( 'NONE',  ( 4.999999999999999112, -5.876895005582878362, 62.72529079327805590 ) ) ;
#9863=ORIENTED_EDGE ( 'NONE', *, *, #2828, .F. ) ;
#9868=EDGE_CURVE ( 'NONE', #15243, #6017, #1246, .T. ) ;
#9871=EDGE_LOOP ( 'NONE', ( #17260, #6468, #6767, #6524 ) ) ;
#9872=CARTESIAN_POINT ( 'NONE',  ( 0.000000000000000000, -16.10733642026445978, -53.89344778774828626 ) ) ;
#9876=CARTESIAN_POINT ( 'NONE',  ( 0.000000000000000000, 5.876895005583346432, -62.72529079327799906 ) ) ;
#9877=DIRECTION ( 'NONE',  ( 0.000000000000000000, 0.000000000000000000, 1.000000000000000000 ) ) ;
#9880=DIRECTION ( 'NONE',  ( -1.000000000000000000, 0.000000000000000000, -0.000000000000000000 ) ) ;
#9883=CYLINDRICAL_SURFACE ( 'NONE', #2403, 24.00000000002400213 ) ;
#9888=EDGE_CURVE ( 'NONE', #16606, #18250, #10384, .T. ) ;
#9896=DIRECTION ( 'NONE',  ( 0.000000000000000000, 0.000000000000000000, 1.000000000000000000 ) ) ;
#9899=DIRECTION ( 'NONE',  ( -1.000000000000000000, 0.000000000000000000, 0.000000000000000000 ) ) ;
#9903=AXIS2_PLACEMENT_3D ( 'NONE', #17860, #12230, #18043 ) ;
#9910=EDGE_LOOP ( 'NONE', ( #15012, #3871 ) ) ;
#9915=EDGE_CURVE ( 'NONE', #1879, #3205, #7249, .T. ) ;
#9916=VERTEX_POINT ( 'NONE', #17361 ) ;
#9920=VERTEX_POINT ( 'NONE', #11822 ) ;
#9923=EDGE_CURVE ( 'NONE', #1081, #1734, #10362, .T. ) ;
#9925=DIRECTION ( 'NONE',  ( -1.000000000000000000, 0.000000000000000000, 0.000000000000000000 ) ) ;
#9928=VERTEX_POINT ( 'NONE', #14672 ) ;
#9933=CIRCLE ( 'NONE', #13867, 24.00000000002399858 ) ;
#9934=DIRECTION ( 'NONE',  ( 1.000000000000000000, 0.000000000000000000, 0.000000000000000000 ) ) ;
#9943=EDGE_CURVE ( 'NONE', #7667, #7777, #16199, .T. ) ;
#9949=CIRCLE ( 'NONE', #18461, 24.00000000002399503 ) ;
#9951=CARTESIAN_POINT ( 'NONE',  ( 0.000000000000000000, 0.000000000000000000, 0.000000000000000000 ) ) ;
#9953=EDGE_CURVE ( 'NONE', #18738, #12029, #12495, .T. ) ;
#9955=ORIENTED_EDGE ( 'NONE', *, *, #938, .F. ) ;
#9956=ADVANCED_FACE ( 'NONE', ( #10022 ), #7338, .T. ) ;
#9958=DIRECTION ( 'NONE',  ( -1.000000000000000000, -0.000000000000000000, 0.000000000000000000 ) ) ;
#9959=CARTESIAN_POINT ( 'NONE',  ( 10.00000000000000000, 0.000000000000000000, 0.000000000000000000 ) ) ;
#9960=AXIS2_PLACEMENT_3D ( 'NONE', #13227, #17087, #3943 ) ;
#9964=ORIENTED_EDGE ( 'NONE', *, *, #11567, .T. ) ;
#9966=VECTOR ( 'NONE', #8540, 1000.000000000000000 ) ;
#9973=CIRCLE ( 'NONE', #1168, 56.24900000005625600 ) ;
#9976=DIRECTION ( 'NONE',  ( -1.000000000000000000, -0.000000000000000000, 0.000000000000000000 ) ) ;
#9978=LINE ( 'NONE', #1317, #18414 ) ;
#9979=ADVANCED_FACE ( 'NONE', ( #7152 ), #18779, .T. ) ;
#9981=CARTESIAN_POINT ( 'NONE',  ( 0.000000000000000000, -54.20017844242489247, -32.11449294037253566 ) ) ;
#9982=DIRECTION ( 'NONE',  ( -1.000000000000000000, -0.000000000000000000, 0.000000000000000000 ) ) ;
#9984=VERTEX_POINT ( 'NONE', #4309 ) ;
#9988=CARTESIAN_POINT ( 'NONE',  ( 0.000000000000000000, -7.813799127873676476, 55.83748330407405547 ) ) ;
#9989=CIRCLE ( 'NONE', #15769, 63.00000000006298961 ) ;
#9995=EDGE_CURVE ( 'NONE', #2244, #2800, #4298, .T. ) ;
#9996=VECTOR ( 'NONE', #5074, 1000.000000000000000 ) ;
#9999=DIRECTION ( 'NONE',  ( -1.000000000000000000, 0.000000000000000000, -0.000000000000000000 ) ) ;
#10005=VECTOR ( 'NONE', #14295, 1000.000000000000000 ) ;
#10009=DIRECTION ( 'NONE',  ( 0.000000000000000000, 0.5877852522924744694, -0.8090169943749464521 ) ) ;
#10013=CARTESIAN_POINT ( 'NONE',  ( -10.00000000000000000, 0.000000000000000000, 0.000000000000000000 ) ) ;
#10018=EDGE_CURVE ( 'NONE', #6670, #8465, #14632, .T. ) ;
#10021=DIRECTION ( 'NONE',  ( -1.000000000000000000, -0.000000000000000000, 0.000000000000000000 ) ) ;
#10022=FACE_OUTER_BOUND ( 'NONE', #11073, .T. ) ;
#10023=ORIENTED_EDGE ( 'NONE', *, *, #10061, .T. ) ;
#10026=CIRCLE ( 'NONE', #1812, 56.24900000005625600 ) ;
#10031=ORIENTED_EDGE ( 'NONE', *, *, #12446, .F. ) ;
#10032=VECTOR ( 'NONE', #15078, 1000.000000000000000 ) ;
#10038=FACE_OUTER_BOUND ( 'NONE', #9665, .T. ) ;
#10042=ORIENTED_EDGE ( 'NONE', *, *, #13333, .T. ) ;
#10050=DIRECTION ( 'NONE',  ( 0.000000000000000000, 0.000000000000000000, 1.000000000000000000 ) ) ;
#10051=CARTESIAN_POINT ( 'NONE',  ( 10.00000000000000000, 0.000000000000000000, 0.000000000000000000 ) ) ;
#10054=ORIENTED_EDGE ( 'NONE', *, *, #9776, .F. ) ;
#10058=CIRCLE ( 'NONE', #5799, 24.00000000002399858 ) ;
#10060=EDGE_CURVE ( 'NONE', #16942, #2331, #15239, .T. ) ;
#10061=EDGE_CURVE ( 'NONE', #484, #14748, #15502, .T. ) ;
#10063=EDGE_CURVE ( 'NONE', #18755, #12204, #1556, .T. ) ;
#10070=ORIENTED_EDGE ( 'NONE', *, *, #10156, .F. ) ;
#10072=VERTEX_POINT ( 'NONE', #8066 ) ;
#10073=CARTESIAN_POINT ( 'NONE',  ( 10.00000000000000000, -33.95787273855277988, 45.00825343885009033 ) ) ;
#10076=FACE_OUTER_BOUND ( 'NONE', #4, .T. ) ;
#10077=ORIENTED_EDGE ( 'NONE', *, *, #2740, .F. ) ;
#10084=EDGE_CURVE ( 'NONE', #1683, #11596, #11879, .T. ) ;
#10085=VECTOR ( 'NONE', #11357, 1000.000000000000000 ) ;
#10088=ORIENTED_EDGE ( 'NONE', *, *, #1538, .F. ) ;
#10095=DIRECTION ( 'NONE',  ( -1.000000000000000000, -0.000000000000000000, 0.000000000000000000 ) ) ;
#10097=FACE_OUTER_BOUND ( 'NONE', #6611, .T. ) ;
#10100=DIRECTION ( 'NONE',  ( 0.000000000000000000, -0.9876883405951393247, 0.1564344650402205161 ) ) ;
#10101=DIRECTION ( 'NONE',  ( -1.000000000000000000, -0.000000000000000000, -0.000000000000000000 ) ) ;
#10106=DIRECTION ( 'NONE',  ( -1.000000000000000000, -0.000000000000000000, -0.000000000000000000 ) ) ;
#10107=EDGE_LOOP ( 'NONE', ( #17989, #6743 ) ) ;
#10111=AXIS2_PLACEMENT_3D ( 'NONE', #5329, #6765, #14299 ) ;
#10113=CARTESIAN_POINT ( 'NONE',  ( 0.000000000000000000, 32.31183295104772668, 46.20417134726143615 ) ) ;
#10114=ORIENTED_EDGE ( 'NONE', *, *, #18543, .F. ) ;
#10130=CIRCLE ( 'NONE', #4049, 56.24900000005625600 ) ;
#10131=ORIENTED_EDGE ( 'NONE', *, *, #747, .F. ) ;
#10132=AXIS2_PLACEMENT_3D ( 'NONE', #17566, #2543, #12643 ) ;
#10134=DIRECTION ( 'NONE',  ( 1.000000000000000000, -0.000000000000000000, -0.000000000000000000 ) ) ;
#10136=CYLINDRICAL_SURFACE ( 'NONE', #10376, 24.00000000002399858 ) ;
#10137=AXIS2_PLACEMENT_3D ( 'NONE', #18535, #15670, #8438 ) ;
#10140=VERTEX_POINT ( 'NONE', #9872 ) ;
#10150=CARTESIAN_POINT ( 'NONE',  ( -10.00000000000000000, 0.000000000000000000, 0.000000000000000000 ) ) ;
#10156=EDGE_CURVE ( 'NONE', #3960, #2157, #11598, .T. ) ;
#10157=EDGE_LOOP ( 'NONE', ( #6705, #10612, #360, #9533 ) ) ;
#10164=DIRECTION ( 'NONE',  ( 0.000000000000000000, 0.000000000000000000, 1.000000000000000000 ) ) ;
#10168=EDGE_LOOP ( 'NONE', ( #1369, #7298, #9646, #9747 ) ) ;
#10169=CYLINDRICAL_SURFACE ( 'NONE', #6975, 56.24900000005625600 ) ;
#10173=EDGE_LOOP ( 'NONE', ( #13224, #6197, #8460, #12443 ) ) ;
#10175=EDGE_CURVE ( 'NONE', #6237, #2958, #5505, .T. ) ;
#10176=EDGE_LOOP ( 'NONE', ( #16690, #11540, #3256, #10236 ) ) ;
#10177=DIRECTION ( 'NONE',  ( -1.000000000000000000, 0.000000000000000000, -0.000000000000000000 ) ) ;
#10178=CARTESIAN_POINT ( 'NONE',  ( 10.00000000000000000, -10.11537145609335830, -55.33199130079796646 ) ) ;
#10179=DIRECTION ( 'NONE',  ( 0.000000000000000000, -0.7071067811865389130, -0.7071067811865561215 ) ) ;
#10180=CARTESIAN_POINT ( 'NONE',  ( 0.000000000000000000, 40.19788616105610402, 48.50907078259395888 ) ) ;
#10183=DIRECTION ( 'NONE',  ( -1.000000000000000000, -0.000000000000000000, 0.000000000000000000 ) ) ;
#10184=DIRECTION ( 'NONE',  ( 1.000000000000000000, 0.000000000000000000, 0.000000000000000000 ) ) ;
#10194=AXIS2_PLACEMENT_3D ( 'NONE', #15312, #6369, #9588 ) ;
#10198=AXIS2_PLACEMENT_3D ( 'NONE', #10702, #13672, #2226 ) ;
#10199=DIRECTION ( 'NONE',  ( -1.000000000000000000, -0.000000000000000000, -0.000000000000000000 ) ) ;
#10200=AXIS2_PLACEMENT_3D ( 'NONE', #15681, #1218, #8538 ) ;
#10203=DIRECTION ( 'NONE',  ( 0.000000000000000000, 0.9876883405951371042, 0.1564344650402347547 ) ) ;
#10206=CARTESIAN_POINT ( 'NONE',  ( 0.000000000000000000, -48.50907078259351835, -40.19788616105663692 ) ) ;
#10209=ORIENTED_EDGE ( 'NONE', *, *, #2615, .F. ) ;
#10215=CIRCLE ( 'NONE', #490, 56.24900000005626310 ) ;
#10218=CIRCLE ( 'NONE', #16926, 24.00000000002399858 ) ;
#10224=CARTESIAN_POINT ( 'NONE',  ( 10.00000000000000000, 0.000000000000000000, 0.000000000000000000 ) ) ;
#10225=ADVANCED_FACE ( 'NONE', ( #7299 ), #14161, .T. ) ;
#10228=DIRECTION ( 'NONE',  ( 0.000000000000000000, 1.000000000000000000, 3.469446951950144779E-15 ) ) ;
#10229=CIRCLE ( 'NONE', #15106, 24.00000000002399858 ) ;
#10231=VECTOR ( 'NONE', #661, 1000.000000000000000 ) ;
#10235=DIRECTION ( 'NONE',  ( 0.000000000000000000, 0.000000000000000000, 1.000000000000000000 ) ) ;
#10236=ORIENTED_EDGE ( 'NONE', *, *, #11031, .T. ) ;
#10237=VERTEX_POINT ( 'NONE', #2739 ) ;
#10240=VERTEX_POINT ( 'NONE', #8542 ) ;
#10241=AXIS2_PLACEMENT_3D ( 'NONE', #17423, #1154, #18663 ) ;
#10249=DIRECTION ( 'NONE',  ( 0.000000000000000000, 0.000000000000000000, -1.000000000000000000 ) ) ;
#10250=CIRCLE ( 'NONE', #9960, 63.00000000006298961 ) ;
#10253=VERTEX_POINT ( 'NONE', #14350 ) ;
#10254=VERTEX_POINT ( 'NONE', #1313 ) ;
#10255=CIRCLE ( 'NONE', #17801, 24.00000000002399858 ) ;
#10256=CYLINDRICAL_SURFACE ( 'NONE', #16097, 56.24900000005625600 ) ;
#10259=ORIENTED_EDGE ( 'NONE', *, *, #6714, .F. ) ;
#10260=ORIENTED_EDGE ( 'NONE', *, *, #9868, .F. ) ;
#10265=EDGE_CURVE ( 'NONE', #11258, #16371, #12818, .T. ) ;
#10266=EDGE_CURVE ( 'NONE', #18700, #14293, #14950, .T. ) ;
#10267=CIRCLE ( 'NONE', #15452, 56.24900000005624889 ) ;
#10270=AXIS2_PLACEMENT_3D ( 'NONE', #5590, #11774, #17583 ) ;
#10274=ORIENTED_EDGE ( 'NONE', *, *, #5342, .T. ) ;
#10279=CARTESIAN_POINT ( 'NONE',  ( 10.00000000000000000, 24.68609584167230153, -50.69000562871616467 ) ) ;
#10282=DIRECTION ( 'NONE',  ( 1.000000000000000000, -0.000000000000000000, -0.000000000000000000 ) ) ;
#10286=DIRECTION ( 'NONE',  ( 0.000000000000000000, 0.8090169943749486725, -0.5877852522924714718 ) ) ;
#10287=CIRCLE ( 'NONE', #6021, 63.00000000006298961 ) ;
#10290=FACE_OUTER_BOUND ( 'NONE', #13169, .T. ) ;
#10295=EDGE_CURVE ( 'NONE', #17597, #475, #7636, .T. ) ;
#10298=EDGE_LOOP ( 'NONE', ( #5048, #15406, #1322, #2926 ) ) ;
#10303=ORIENTED_EDGE ( 'NONE', *, *, #18202, .F. ) ;
#10304=CIRCLE ( 'NONE', #14555, 56.24900000005624889 ) ;
#10305=CYLINDRICAL_SURFACE ( 'NONE', #579, 30.00000000000000000 ) ;
#10307=ADVANCED_FACE ( 'NONE', ( #11957 ), #8909, .T. ) ;
#10308=CARTESIAN_POINT ( 'NONE',  ( 10.00000000000000000, 16.10733642026482570, 53.89344778774818678 ) ) ;
#10309=CARTESIAN_POINT ( 'NONE',  ( 0.000000000000000000, -55.74967257055887870, 7.478235706488783663 ) ) ;
#10310=CARTESIAN_POINT ( 'NONE',  ( 4.999999999999999112, -15.61693798565454472, -61.03368945066451801 ) ) ;
#10311=ORIENTED_EDGE ( 'NONE', *, *, #4005, .F. ) ;
#10312=FACE_OUTER_BOUND ( 'NONE', #8869, .T. ) ;
#10317=ORIENTED_EDGE ( 'NONE', *, *, #15860, .F. ) ;
#10320=ORIENTED_EDGE ( 'NONE', *, *, #12451, .F. ) ;
#10328=DIRECTION ( 'NONE',  ( -1.000000000000000000, 0.000000000000000000, 0.000000000000000000 ) ) ;
#10337=DIRECTION ( 'NONE',  ( 0.000000000000000000, -0.4539904997395542430, 0.8910065241883641241 ) ) ;
#10338=CARTESIAN_POINT ( 'NONE',  ( 0.000000000000000000, 61.03368945066456774, -15.61693798565434399 ) ) ;
#10342=EDGE_CURVE ( 'NONE', #13575, #10719, #15861, .T. ) ;
#10343=FACE_OUTER_BOUND ( 'NONE', #2628, .T. ) ;
#10345=DIRECTION ( 'NONE',  ( 0.000000000000000000, 0.3090169943749480619, -0.9510565162951533091 ) ) ;
#10347=DIRECTION ( 'NONE',  ( 1.000000000000000000, 0.000000000000000000, 0.000000000000000000 ) ) ;
#10350=DIRECTION ( 'NONE',  ( 0.000000000000000000, 0.000000000000000000, 1.000000000000000000 ) ) ;
#10354=ORIENTED_EDGE ( 'NONE', *, *, #18370, .T. ) ;
#10355=ORIENTED_EDGE ( 'NONE', *, *, #1172, .F. ) ;
#10357=DIRECTION ( 'NONE',  ( -1.000000000000000000, 0.000000000000000000, 0.000000000000000000 ) ) ;
#10358=ORIENTED_EDGE ( 'NONE', *, *, #7087, .T. ) ;
#10362=CIRCLE ( 'NONE', #4001, 24.00000000002399858 ) ;
#10363=CARTESIAN_POINT ( 'NONE',  ( 10.00000000000000000, 54.20017844242556748, -32.11449294037137747 ) ) ;
#10364=VERTEX_POINT ( 'NONE', #17585 ) ;
#10374=VERTEX_POINT ( 'NONE', #1862 ) ;
#10375=CARTESIAN_POINT ( 'NONE',  ( 10.00000000000000000, -62.72529079327811274, 5.876895005582225551 ) ) ;
#10376=AXIS2_PLACEMENT_3D ( 'NONE', #15857, #2806, #13004 ) ;
#10379=DIRECTION ( 'NONE',  ( -1.000000000000000000, 0.000000000000000000, 0.000000000000000000 ) ) ;
#10381=VERTEX_POINT ( 'NONE', #14919 ) ;
#10384=LINE ( 'NONE', #13245, #10953 ) ;
#10386=FACE_OUTER_BOUND ( 'NONE', #9012, .T. ) ;
#10393=CARTESIAN_POINT ( 'NONE',  ( -10.00000000000000000, 0.000000000000000000, 0.000000000000000000 ) ) ;
#10394=CYLINDRICAL_SURFACE ( 'NONE', #2183, 24.00000000002400213 ) ;
#10396=ORIENTED_EDGE ( 'NONE', *, *, #11595, .F. ) ;
#10398=ORIENTED_EDGE ( 'NONE', *, *, #18307, .T. ) ;
#10401=ORIENTED_EDGE ( 'NONE', *, *, #12237, .F. ) ;
#10406=EDGE_LOOP ( 'NONE', ( #8565, #3474, #6118, #13719 ) ) ;
#10409=CARTESIAN_POINT ( 'NONE',  ( -10.00000000000000000, 0.000000000000000000, 0.000000000000000000 ) ) ;
#10411=ADVANCED_FACE ( 'NONE', ( #8147 ), #11080, .T. ) ;
#10419=CARTESIAN_POINT ( 'NONE',  ( 0.000000000000000000, 0.000000000000000000, 0.000000000000000000 ) ) ;
#10426=VERTEX_POINT ( 'NONE', #12432 ) ;
#10427=VECTOR ( 'NONE', #2438, 1000.000000000000000 ) ;
#10429=DIRECTION ( 'NONE',  ( -1.000000000000000000, -0.000000000000000000, 0.000000000000000000 ) ) ;
#10430=DIRECTION ( 'NONE',  ( 0.000000000000000000, 0.000000000000000000, 1.000000000000000000 ) ) ;
#10433=EDGE_LOOP ( 'NONE', ( #7579, #1941, #4506, #12197 ) ) ;
#10434=CARTESIAN_POINT ( 'NONE',  ( 10.00000000000000000, -32.11449294037157642, -54.20017844242546090 ) ) ;
#10435=ORIENTED_EDGE ( 'NONE', *, *, #12638, .F. ) ;
#10438=ORIENTED_EDGE ( 'NONE', *, *, #1807, .T. ) ;
#10442=AXIS2_PLACEMENT_3D ( 'NONE', #18314, #8025, #6795 ) ;
#10443=ORIENTED_EDGE ( 'NONE', *, *, #9720, .F. ) ;
#10444=CARTESIAN_POINT ( 'NONE',  ( 0.000000000000000000, 53.92768374110868734, 16.45250512421953459 ) ) ;
#10453=DIRECTION ( 'NONE',  ( 0.000000000000000000, 0.000000000000000000, 1.000000000000000000 ) ) ;
#10454=EDGE_CURVE ( 'NONE', #10381, #18246, #8561, .T. ) ;
#10456=DIRECTION ( 'NONE',  ( -1.000000000000000000, 0.000000000000000000, 0.000000000000000000 ) ) ;
#10457=CARTESIAN_POINT ( 'NONE',  ( 0.000000000000000000, 0.000000000000000000, 0.000000000000000000 ) ) ;
#10459=CYLINDRICAL_SURFACE ( 'NONE', #18542, 24.00000000002399503 ) ;
#10462=CYLINDRICAL_SURFACE ( 'NONE', #404, 24.00000000002399503 ) ;
#10472=CYLINDRICAL_SURFACE ( 'NONE', #885, 24.00000000002399858 ) ;
#10476=CYLINDRICAL_SURFACE ( 'NONE', #590, 56.24900000005625600 ) ;
#10486=ADVANCED_FACE ( 'NONE', ( #18243 ), #4910, .T. ) ;
#10488=CIRCLE ( 'NONE', #14755, 56.24900000005624889 ) ;
#10489=AXIS2_PLACEMENT_3D ( 'NONE', #10073, #13561, #2832 ) ;
#10493=CARTESIAN_POINT ( 'NONE',  ( 0.000000000000000000, 26.49895292618005271, 49.76630880786320432 ) ) ;
#10497=LINE ( 'NONE', #17744, #13610 ) ;
#10509=AXIS2_PLACEMENT_3D ( 'NONE', #13166, #14769, #8952 ) ;
#10510=DIRECTION ( 'NONE',  ( -1.000000000000000000, -0.000000000000000000, 0.000000000000000000 ) ) ;
#10512=CARTESIAN_POINT ( 'NONE',  ( 0.000000000000000000, -42.79754323328189969, -13.90576474687263264 ) ) ;
#10513=ORIENTED_EDGE ( 'NONE', *, *, #2252, .T. ) ;
#10516=CIRCLE ( 'NONE', #15391, 24.00000000002400569 ) ;
#10519=DIRECTION ( 'NONE',  ( 0.000000000000000000, -0.9510565162951500895, -0.3090169943749581649 ) ) ;
#10520=EDGE_CURVE ( 'NONE', #5770, #8874, #1861, .T. ) ;
#10521=CYLINDRICAL_SURFACE ( 'NONE', #4715, 63.00000000006298961 ) ;
#10523=DIRECTION ( 'NONE',  ( -1.000000000000000000, 0.000000000000000000, 0.000000000000000000 ) ) ;
#10525=EDGE_CURVE ( 'NONE', #743, #11942, #11610, .T. ) ;
#10526=ORIENTED_EDGE ( 'NONE', *, *, #18085, .F. ) ;
#10527=CARTESIAN_POINT ( 'NONE',  ( 0.000000000000000000, 56.37237871411035428, -1.017308535511785683 ) ) ;
#10530=CARTESIAN_POINT ( 'NONE',  ( 10.00000000000000000, 31.97297851452424311, 46.27827401617415148 ) ) ;
#10531=ORIENTED_EDGE ( 'NONE', *, *, #12620, .T. ) ;
#10535=ORIENTED_EDGE ( 'NONE', *, *, #889, .F. ) ;
#10536=VERTEX_POINT ( 'NONE', #11480 ) ;
#10537=VECTOR ( 'NONE', #17991, 1000.000000000000000 ) ;
#10539=AXIS2_PLACEMENT_3D ( 'NONE', #9617, #12867, #11040 ) ;
#10541=DIRECTION ( 'NONE',  ( 0.000000000000000000, 0.000000000000000000, 1.000000000000000000 ) ) ;
#10542=AXIS2_PLACEMENT_3D ( 'NONE', #1354, #14107, #12976 ) ;
#10545=AXIS2_PLACEMENT_3D ( 'NONE', #18090, #15433, #2562 ) ;
#10553=DIRECTION ( 'NONE',  ( 0.000000000000000000, 0.000000000000000000, -1.000000000000000000 ) ) ;
#10554=DIRECTION ( 'NONE',  ( 0.000000000000000000, 0.000000000000000000, -1.000000000000000000 ) ) ;
#10555=ORIENTED_EDGE ( 'NONE', *, *, #5872, .F. ) ;
#10557=LINE ( 'NONE', #16377, #15788 ) ;
#10558=DIRECTION ( 'NONE',  ( 0.000000000000000000, 0.000000000000000000, 1.000000000000000000 ) ) ;
#10559=DIRECTION ( 'NONE',  ( 1.000000000000000000, 0.000000000000000000, 0.000000000000000000 ) ) ;
#10563=CARTESIAN_POINT ( 'NONE',  ( 10.00000000000000000, 50.69000562871642046, -24.68609584167177218 ) ) ;
#10566=AXIS2_PLACEMENT_3D ( 'NONE', #17945, #4699, #13283 ) ;
#10567=AXIS2_PLACEMENT_3D ( 'NONE', #15204, #2145, #249 ) ;
#10574=DIRECTION ( 'NONE',  ( 0.000000000000000000, -0.1564344650402382242, 0.9876883405951364381 ) ) ;
#10576=DIRECTION ( 'NONE',  ( -1.000000000000000000, -0.000000000000000000, -0.000000000000000000 ) ) ;
#10578=AXIS2_PLACEMENT_3D ( 'NONE', #5571, #11374, #10771 ) ;
#10580=ORIENTED_EDGE ( 'NONE', *, *, #18550, .T. ) ;
#10581=AXIS2_PLACEMENT_3D ( 'NONE', #9811, #15533, #5328 ) ;
#10582=CYLINDRICAL_SURFACE ( 'NONE', #18527, 24.00000000002399858 ) ;
#10585=CARTESIAN_POINT ( 'NONE',  ( 10.00000000000000000, -46.27827401617427228, 31.97297851452409034 ) ) ;
#10589=VECTOR ( 'NONE', #13304, 1000.000000000000000 ) ;
#10591=EDGE_CURVE ( 'NONE', #2530, #872, #4249, .T. ) ;
#10592=ORIENTED_EDGE ( 'NONE', *, *, #7965, .T. ) ;
#10595=DIRECTION ( 'NONE',  ( -1.000000000000000000, -0.000000000000000000, -0.000000000000000000 ) ) ;
#10598=FACE_OUTER_BOUND ( 'NONE', #2291, .T. ) ;
#10599=CARTESIAN_POINT ( 'NONE',  ( 0.000000000000000000, -53.06836994729246726, 18.64666490672351529 ) ) ;
#10601=DIRECTION ( 'NONE',  ( 0.000000000000000000, 0.000000000000000000, 1.000000000000000000 ) ) ;
#10603=ORIENTED_EDGE ( 'NONE', *, *, #11222, .T. ) ;
#10604=CARTESIAN_POINT ( 'NONE',  ( 5.000000000000000000, -57.83923611457337444, 24.97244012287480430 ) ) ;
#10607=EDGE_CURVE ( 'NONE', #8897, #2152, #14646, .T. ) ;
#10610=VECTOR ( 'NONE', #770, 1000.000000000000000 ) ;
#10612=ORIENTED_EDGE ( 'NONE', *, *, #15431, .F. ) ;
#10613=FACE_OUTER_BOUND ( 'NONE', #10433, .T. ) ;
#10615=DIRECTION ( 'NONE',  ( -1.000000000000000000, 0.000000000000000000, 0.000000000000000000 ) ) ;
#10616=ORIENTED_EDGE ( 'NONE', *, *, #14651, .F. ) ;
#10618=CYLINDRICAL_SURFACE ( 'NONE', #11104, 63.00000000006298961 ) ;
#10620=CARTESIAN_POINT ( 'NONE',  ( 10.00000000000000000, 48.50907078259382388, 40.19788616105626744 ) ) ;
#10623=ORIENTED_EDGE ( 'NONE', *, *, #8212, .T. ) ;
#10626=ADVANCED_FACE ( 'NONE', ( #18529 ), #10136, .T. ) ;
#10630=CARTESIAN_POINT ( 'NONE',  ( 0.000000000000000000, -48.50907078259410099, 40.19788616105593348 ) ) ;
#10634=DIRECTION ( 'NONE',  ( 0.000000000000000000, 0.000000000000000000, 1.000000000000000000 ) ) ;
#10640=ADVANCED_FACE ( 'NONE', ( #5380 ), #11186, .T. ) ;
#10641=EDGE_CURVE ( 'NONE', #5795, #701, #2178, .T. ) ;
#10643=AXIS2_PLACEMENT_3D ( 'NONE', #1209, #4257, #7008 ) ;
#10649=CARTESIAN_POINT ( 'NONE',  ( 5.000000000000000000, 54.20017844242556748, -32.11449294037138458 ) ) ;
#10650=ORIENTED_EDGE ( 'NONE', *, *, #7041, .T. ) ;
#10651=CARTESIAN_POINT ( 'NONE',  ( 10.00000000000000000, 0.000000000000000000, 0.000000000000000000 ) ) ;
#10657=DIRECTION ( 'NONE',  ( -1.000000000000000000, 0.000000000000000000, -0.000000000000000000 ) ) ;
#10663=AXIS2_PLACEMENT_3D ( 'NONE', #6783, #6872, #8117 ) ;
#10668=DIRECTION ( 'NONE',  ( -1.000000000000000000, 0.000000000000000000, 0.000000000000000000 ) ) ;
#10672=CARTESIAN_POINT ( 'NONE',  ( 10.00000000000000000, 18.38754094778314752, -53.29895248911656580 ) ) ;
#10673=ORIENTED_EDGE ( 'NONE', *, *, #11592, .F. ) ;
#10679=ORIENTED_EDGE ( 'NONE', *, *, #13646, .T. ) ;
#10680=VERTEX_POINT ( 'NONE', #5573 ) ;
#10682=DIRECTION ( 'NONE',  ( -1.000000000000000000, -0.000000000000000000, -0.000000000000000000 ) ) ;
#10686=LINE ( 'NONE', #5166, #16418 ) ;
#10689=DIRECTION ( 'NONE',  ( -1.000000000000000000, -0.000000000000000000, 0.000000000000000000 ) ) ;
#10693=EDGE_CURVE ( 'NONE', #1171, #6377, #10951, .T. ) ;
#10694=CYLINDRICAL_SURFACE ( 'NONE', #3226, 56.24900000005625600 ) ;
#10699=DIRECTION ( 'NONE',  ( 0.000000000000000000, -0.3090169943749349057, -0.9510565162951576390 ) ) ;
#10702=CARTESIAN_POINT ( 'NONE',  ( 10.00000000000000000, 49.76630880786347433, -26.49895292617950560 ) ) ;
#10704=CARTESIAN_POINT ( 'NONE',  ( -10.00000000000000000, 26.45033635316149301, 36.40576474687247099 ) ) ;
#10706=DIRECTION ( 'NONE',  ( -1.000000000000000000, 0.000000000000000000, 0.000000000000000000 ) ) ;
#10707=VERTEX_POINT ( 'NONE', #1839 ) ;
#10714=DIRECTION ( 'NONE',  ( 0.000000000000000000, 0.000000000000000000, 1.000000000000000000 ) ) ;
#10719=VERTEX_POINT ( 'NONE', #11845 ) ;
#10720=LINE ( 'NONE', #2343, #4250 ) ;
#10721=VECTOR ( 'NONE', #3772, 1000.000000000000000 ) ;
#10724=ADVANCED_FACE ( 'NONE', ( #17466 ), #325, .T. ) ;
#10726=ADVANCED_FACE ( 'NONE', ( #6029 ), #7555, .T. ) ;
#10728=EDGE_CURVE ( 'NONE', #16959, #5879, #4609, .T. ) ;
#10733=CARTESIAN_POINT ( 'NONE',  ( 10.00000000000000000, -53.06836994729246726, 18.64666490672351529 ) ) ;
#10735=CARTESIAN_POINT ( 'NONE',  ( 5.000000000000000000, 23.24033432160437584, 58.55669782892469755 ) ) ;
#10739=FACE_OUTER_BOUND ( 'NONE', #17737, .T. ) ;
#10741=EDGE_LOOP ( 'NONE', ( #822, #1214, #16732, #15576 ) ) ;
#10744=EDGE_CURVE ( 'NONE', #15168, #8023, #13735, .T. ) ;
#10748=AXIS2_PLACEMENT_3D ( 'NONE', #707, #11064, #6608 ) ;
#10749=EDGE_CURVE ( 'NONE', #10364, #4317, #12171, .T. ) ;
#10755=EDGE_CURVE ( 'NONE', #15153, #4463, #17691, .T. ) ;
#10763=ORIENTED_EDGE ( 'NONE', *, *, #11101, .F. ) ;
#10767=ORIENTED_EDGE ( 'NONE', *, *, #15757, .F. ) ;
#10768=DIRECTION ( 'NONE',  ( -1.000000000000000000, -0.000000000000000000, 0.000000000000000000 ) ) ;
#10771=DIRECTION ( 'NONE',  ( 0.000000000000000000, -0.3090169943749350723, -0.9510565162951576390 ) ) ;
#10774=DIRECTION ( 'NONE',  ( -1.000000000000000000, -0.000000000000000000, -0.000000000000000000 ) ) ;
#10776=FACE_OUTER_BOUND ( 'NONE', #13942, .T. ) ;
#10780=DIRECTION ( 'NONE',  ( 1.000000000000000000, -0.000000000000000000, -0.000000000000000000 ) ) ;
#10781=LINE ( 'NONE', #6131, #12582 ) ;
#10785=DIRECTION ( 'NONE',  ( -1.000000000000000000, -0.000000000000000000, -0.000000000000000000 ) ) ;
#10788=CARTESIAN_POINT ( 'NONE',  ( 0.000000000000000000, 0.000000000000000000, 0.000000000000000000 ) ) ;
#10789=ORIENTED_EDGE ( 'NONE', *, *, #13180, .T. ) ;
#10790=VECTOR ( 'NONE', #2537, 1000.000000000000000 ) ;
#10795=CYLINDRICAL_SURFACE ( 'NONE', #5165, 24.00000000002399503 ) ;
#10801=ORIENTED_EDGE ( 'NONE', *, *, #13733, .T. ) ;
#10802=CARTESIAN_POINT ( 'NONE',  ( 50.00005079999999680, 0.000000000000000000, 0.000000000000000000 ) ) ;
#10804=ORIENTED_EDGE ( 'NONE', *, *, #4089, .F. ) ;
#10806=DIRECTION ( 'NONE',  ( 0.000000000000000000, 0.000000000000000000, 1.000000000000000000 ) ) ;
#10808=VERTEX_POINT ( 'NONE', #8967 ) ;
#10812=DIRECTION ( 'NONE',  ( 0.000000000000000000, 0.000000000000000000, 1.000000000000000000 ) ) ;
#10816=DIRECTION ( 'NONE',  ( 0.000000000000000000, -0.9876883405951358830, -0.1564344650402420822 ) ) ;
#10818=VERTEX_POINT ( 'NONE', #4691 ) ;
#10821=FACE_OUTER_BOUND ( 'NONE', #15946, .T. ) ;
#10823=AXIS2_PLACEMENT_3D ( 'NONE', #11812, #13150, #11432 ) ;
#10825=DIRECTION ( 'NONE',  ( -1.000000000000000000, -0.000000000000000000, -0.000000000000000000 ) ) ;
#10830=VERTEX_POINT ( 'NONE', #14610 ) ;
#10835=ORIENTED_EDGE ( 'NONE', *, *, #15403, .F. ) ;
#10845=CARTESIAN_POINT ( 'NONE',  ( 10.00000000000000000, 0.000000000000000000, 0.000000000000000000 ) ) ;
#10850=CARTESIAN_POINT ( 'NONE',  ( 0.000000000000000000, -13.79392154159179640, 61.47135697633775209 ) ) ;
#10851=ORIENTED_EDGE ( 'NONE', *, *, #1244, .F. ) ;
#10854=CIRCLE ( 'NONE', #14508, 24.00000000002399503 ) ;
#10857=LINE ( 'NONE', #15166, #6642 ) ;
#10859=CIRCLE ( 'NONE', #2662, 63.00000000006298961 ) ;
#10860=AXIS2_PLACEMENT_3D ( 'NONE', #1564, #7363, #5930 ) ;
#10864=ADVANCED_FACE ( 'NONE', ( #10598 ), #2122, .T. ) ;
#10869=EDGE_CURVE ( 'NONE', #3193, #9460, #9933, .T. ) ;
#10870=DIRECTION ( 'NONE',  ( -1.000000000000000000, 0.000000000000000000, 0.000000000000000000 ) ) ;
#10872=AXIS2_PLACEMENT_3D ( 'NONE', #3833, #12592, #15743 ) ;
#10873=CARTESIAN_POINT ( 'NONE',  ( -10.00000000000000000, -5.120903701083534543E-13, -42.35000000000000142 ) ) ;
#10876=FACE_OUTER_BOUND ( 'NONE', #4215, .T. ) ;
#10883=CYLINDRICAL_SURFACE ( 'NONE', #10748, 24.00000000002399503 ) ;
#10884=CARTESIAN_POINT ( 'NONE',  ( 10.00000000000000000, -39.14194549634393638, 40.58063702438330722 ) ) ;
#10886=ORIENTED_EDGE ( 'NONE', *, *, #14797, .T. ) ;
#10888=DIRECTION ( 'NONE',  ( 0.000000000000000000, 0.1564344650402312575, -0.9876883405951376593 ) ) ;
#10894=AXIS2_PLACEMENT_3D ( 'NONE', #18195, #1055, #5536 ) ;
#10895=EDGE_CURVE ( 'NONE', #3100, #18521, #15102, .T. ) ;
#10897=CARTESIAN_POINT ( 'NONE',  ( 10.00000000000000000, 42.79754323328179311, -16.55576474687299537 ) ) ;
#10900=EDGE_LOOP ( 'NONE', ( #4279, #16157, #17146, #2066 ) ) ;
#10901=CARTESIAN_POINT ( 'NONE',  ( 10.00000000000000000, 0.000000000000000000, 0.000000000000000000 ) ) ;
#10903=AXIS2_PLACEMENT_3D ( 'NONE', #10788, #18130, #6424 ) ;
#10905=VERTEX_POINT ( 'NONE', #18113 ) ;
#10913=DIRECTION ( 'NONE',  ( -1.000000000000000000, -0.000000000000000000, -0.000000000000000000 ) ) ;
#10914=ORIENTED_EDGE ( 'NONE', *, *, #7945, .F. ) ;
#10916=AXIS2_PLACEMENT_3D ( 'NONE', #311, #18199, #9622 ) ;
#10919=DIRECTION ( 'NONE',  ( -1.000000000000000000, 0.000000000000000000, 0.000000000000000000 ) ) ;
#10921=VERTEX_POINT ( 'NONE', #13653 ) ;
#10931=LINE ( 'NONE', #6656, #3926 ) ;
#10932=FACE_OUTER_BOUND ( 'NONE', #9824, .T. ) ;
#10934=VERTEX_POINT ( 'NONE', #15348 ) ;
#10937=ORIENTED_EDGE ( 'NONE', *, *, #3881, .T. ) ;
#10940=CIRCLE ( 'NONE', #3651, 24.00000000002399503 ) ;
#10941=CIRCLE ( 'NONE', #2748, 24.00000000002399148 ) ;
#10944=CARTESIAN_POINT ( 'NONE',  ( 0.000000000000000000, -31.97297851452457351, 46.27827401617392411 ) ) ;
#10949=FACE_OUTER_BOUND ( 'NONE', #7163, .T. ) ;
#10950=EDGE_LOOP ( 'NONE', ( #13946, #18430 ) ) ;
#10951=CIRCLE ( 'NONE', #12829, 24.00000000002399858 ) ;
#10953=VECTOR ( 'NONE', #16111, 1000.000000000000000 ) ;
#10971=CARTESIAN_POINT ( 'NONE',  ( 10.00000000000000000, -53.06836994729219725, -18.64666490672428623 ) ) ;
#10975=EDGE_CURVE ( 'NONE', #18363, #15353, #11460, .T. ) ;
#10976=CARTESIAN_POINT ( 'NONE',  ( 10.00000000000000000, -26.49895292618039377, 49.76630880786299826 ) ) ;
#10980=CARTESIAN_POINT ( 'NONE',  ( 10.00000000000000000, 0.000000000000000000, 0.000000000000000000 ) ) ;
#10982=DIRECTION ( 'NONE',  ( 1.000000000000000000, 0.000000000000000000, 0.000000000000000000 ) ) ;
#10984=EDGE_CURVE ( 'NONE', #12076, #3708, #1409, .T. ) ;
#10988=CARTESIAN_POINT ( 'NONE',  ( -10.00000000000000000, 0.000000000000000000, 0.000000000000000000 ) ) ;
#10991=ORIENTED_EDGE ( 'NONE', *, *, #13700, .T. ) ;
#10993=ORIENTED_EDGE ( 'NONE', *, *, #10975, .F. ) ;
#10996=CARTESIAN_POINT ( 'NONE',  ( 0.000000000000000000, 0.000000000000000000, 0.000000000000000000 ) ) ;
#10997=CARTESIAN_POINT ( 'NONE',  ( 0.000000000000000000, 49.76630880786347433, -26.49895292617950560 ) ) ;
#10998=CARTESIAN_POINT ( 'NONE',  ( 10.00000000000000000, 33.71303790549352186, -53.22058882792160261 ) ) ;
#10999=ORIENTED_EDGE ( 'NONE', *, *, #3061, .F. ) ;
#11004=CARTESIAN_POINT ( 'NONE',  ( 10.00000000000000000, -56.23315539212689629, -1.335003989222221410 ) ) ;
#11008=DIRECTION ( 'NONE',  ( 1.000000000000000000, 0.000000000000000000, 0.000000000000000000 ) ) ;
#11013=CARTESIAN_POINT ( 'NONE',  ( 0.000000000000000000, -9.823366686501049827, 55.51919907100648999 ) ) ;
#11015=DIRECTION ( 'NONE',  ( -1.000000000000000000, -0.000000000000000000, 0.000000000000000000 ) ) ;
#11024=DIRECTION ( 'NONE',  ( 0.000000000000000000, 0.000000000000000000, 1.000000000000000000 ) ) ;
#11029=DIRECTION ( 'NONE',  ( 0.000000000000000000, -0.3090169943749349057, -0.9510565162951576390 ) ) ;
#11030=AXIS2_PLACEMENT_3D ( 'NONE', #10013, #4480, #197 ) ;
#11031=EDGE_CURVE ( 'NONE', #3688, #3160, #6585, .T. ) ;
#11033=ADVANCED_FACE ( 'NONE', ( #12890 ), #6981, .T. ) ;
#11039=CARTESIAN_POINT ( 'NONE',  ( 0.000000000000000000, -24.33982105418938602, 50.71018745830434682 ) ) ;
#11040=DIRECTION ( 'NONE',  ( 0.000000000000000000, 0.000000000000000000, 1.000000000000000000 ) ) ;
#11042=CARTESIAN_POINT ( 'NONE',  ( 10.00000000000000000, 26.49895292618005271, 49.76630880786320432 ) ) ;
#11044=EDGE_LOOP ( 'NONE', ( #16078, #2763, #2653, #17554 ) ) ;
#11045=CARTESIAN_POINT ( 'NONE',  ( 10.00000000000000000, -50.71018745830427576, -24.33982105418956010 ) ) ;
#11046=CARTESIAN_POINT ( 'NONE',  ( 0.000000000000000000, 55.74967257055894265, -7.478235706488370660 ) ) ;
#11048=CIRCLE ( 'NONE', #2850, 56.24900000005624889 ) ;
#11050=VERTEX_POINT ( 'NONE', #1181 ) ;
#11051=ORIENTED_EDGE ( 'NONE', *, *, #17061, .F. ) ;
#11052=CARTESIAN_POINT ( 'NONE',  ( 10.00000000000000000, 53.06836994729258805, -18.64666490672316712 ) ) ;
#11054=CARTESIAN_POINT ( 'NONE',  ( 10.00000000000000000, 55.33199130079800199, -10.11537145609316646 ) ) ;
#11055=DIRECTION ( 'NONE',  ( 0.000000000000000000, 0.8910065241883690090, -0.4539904997395448616 ) ) ;
#11056=DIRECTION ( 'NONE',  ( 0.000000000000000000, 0.000000000000000000, 1.000000000000000000 ) ) ;
#11059=FACE_OUTER_BOUND ( 'NONE', #2396, .T. ) ;
#11064=DIRECTION ( 'NONE',  ( -1.000000000000000000, 0.000000000000000000, 0.000000000000000000 ) ) ;
#11066=ORIENTED_EDGE ( 'NONE', *, *, #9578, .F. ) ;
#11067=EDGE_LOOP ( 'NONE', ( #12757, #2128, #1185, #13218 ) ) ;
#11068=EDGE_CURVE ( 'NONE', #16413, #17793, #11355, .T. ) ;
#11071=DIRECTION ( 'NONE',  ( 0.000000000000000000, 0.3090169943749411785, 0.9510565162951556406 ) ) ;
#11073=EDGE_LOOP ( 'NONE', ( #13737, #10914, #4408, #8254 ) ) ;
#11076=ADVANCED_FACE ( 'NONE', ( #8224 ), #7066, .T. ) ;
#11077=CARTESIAN_POINT ( 'NONE',  ( 0.000000000000000000, -33.95787273855277988, 45.00825343885009033 ) ) ;
#11079=DIRECTION ( 'NONE',  ( -1.000000000000000000, -0.000000000000000000, -0.000000000000000000 ) ) ;
#11080=CYLINDRICAL_SURFACE ( 'NONE', #3084, 56.24900000005625600 ) ;
#11081=ADVANCED_FACE ( 'NONE', ( #6785 ), #4223, .T. ) ;
#11084=CARTESIAN_POINT ( 'NONE',  ( -10.00000000000000000, -42.79754323328189969, -13.90576474687263264 ) ) ;
#11085=VERTEX_POINT ( 'NONE', #18503 ) ;
#11087=DIRECTION ( 'NONE',  ( 0.000000000000000000, 0.000000000000000000, 1.000000000000000000 ) ) ;
#11089=LINE ( 'NONE', #14146, #11555 ) ;
#11093=VECTOR ( 'NONE', #12548, 1000.000000000000000 ) ;
#11094=EDGE_CURVE ( 'NONE', #12056, #12567, #3842, .T. ) ;
#11098=VERTEX_POINT ( 'NONE', #5254 ) ;
#11099=DIRECTION ( 'NONE',  ( -1.000000000000000000, 0.000000000000000000, 0.000000000000000000 ) ) ;
#11101=EDGE_CURVE ( 'NONE', #478, #5108, #18742, .T. ) ;
#11104=AXIS2_PLACEMENT_3D ( 'NONE', #12147, #2053, #11862 ) ;
#11106=AXIS2_PLACEMENT_3D ( 'NONE', #3836, #15352, #8125 ) ;
#11107=ORIENTED_EDGE ( 'NONE', *, *, #16689, .F. ) ;
#11110=CARTESIAN_POINT ( 'NONE',  ( 10.00000000000000000, 0.000000000000000000, 0.000000000000000000 ) ) ;
#11113=EDGE_LOOP ( 'NONE', ( #11339, #13768, #1247, #15161 ) ) ;
#11114=CARTESIAN_POINT ( 'NONE',  ( 10.00000000000000000, -15.61693798565454827, -61.03368945066451090 ) ) ;
#11115=ORIENTED_EDGE ( 'NONE', *, *, #4458, .T. ) ;
#11117=CARTESIAN_POINT ( 'NONE',  ( 10.00000000000000000, -31.97297851452390915, -46.27827401617439307 ) ) ;
#11121=VERTEX_POINT ( 'NONE', #29 ) ;
#11123=FACE_OUTER_BOUND ( 'NONE', #13799, .T. ) ;
#11124=CIRCLE ( 'NONE', #18745, 24.00000000002399858 ) ;
#11125=VECTOR ( 'NONE', #18098, 1000.000000000000000 ) ;
#11128=VERTEX_POINT ( 'NONE', #4672 ) ;
#11130=AXIS2_PLACEMENT_3D ( 'NONE', #45, #1473, #5842 ) ;
#11132=DIRECTION ( 'NONE',  ( -1.000000000000000000, 0.000000000000000000, 0.000000000000000000 ) ) ;
#11133=AXIS2_PLACEMENT_3D ( 'NONE', #6352, #7668, #13496 ) ;
#11137=PLANE ( 'NONE',  #16315 ) ;
#11139=CYLINDRICAL_SURFACE ( 'NONE', #4924, 63.00000000006298961 ) ;
#11143=DIRECTION ( 'NONE',  ( -1.000000000000000000, -0.000000000000000000, -0.000000000000000000 ) ) ;
#11145=LINE ( 'NONE', #4211, #18334 ) ;
#11146=AXIS2_PLACEMENT_3D ( 'NONE', #7225, #7320, #8477 ) ;
#11149=ORIENTED_EDGE ( 'NONE', *, *, #5790, .F. ) ;
#11150=AXIS2_PLACEMENT_3D ( 'NONE', #9736, #7827, #13651 ) ;
#11152=EDGE_CURVE ( 'NONE', #4158, #12684, #2014, .T. ) ;
#11153=ORIENTED_EDGE ( 'NONE', *, *, #15569, .T. ) ;
#11158=DIRECTION ( 'NONE',  ( 0.000000000000000000, -0.8910065241883722287, 0.4539904997395383113 ) ) ;
#11160=CARTESIAN_POINT ( 'NONE',  ( 10.00000000000000000, 55.74967257055883607, 7.478235706489176238 ) ) ;
#11161=DIRECTION ( 'NONE',  ( 1.000000000000000000, 0.000000000000000000, 0.000000000000000000 ) ) ;
#11162=CARTESIAN_POINT ( 'NONE',  ( 10.00000000000000000, -7.813799127873676476, 55.83748330407405547 ) ) ;
#11164=DIRECTION ( 'NONE',  ( -1.000000000000000000, 0.000000000000000000, 0.000000000000000000 ) ) ;
#11166=CIRCLE ( 'NONE', #5399, 63.00000000006298961 ) ;
#11168=ORIENTED_EDGE ( 'NONE', *, *, #13242, .T. ) ;
#11178=VERTEX_POINT ( 'NONE', #7429 ) ;
#11180=VECTOR ( 'NONE', #14325, 1000.000000000000000 ) ;
#11186=CYLINDRICAL_SURFACE ( 'NONE', #8530, 63.00000000006298961 ) ;
#11187=EDGE_CURVE ( 'NONE', #3106, #5418, #6104, .T. ) ;
#11188=AXIS2_PLACEMENT_3D ( 'NONE', #10802, #3681, #9766 ) ;
#11189=CARTESIAN_POINT ( 'NONE',  ( 0.000000000000000000, 58.55669782892461939, 23.24033432160458545 ) ) ;
#11191=AXIS2_PLACEMENT_3D ( 'NONE', #487, #16126, #8871 ) ;
#11192=CARTESIAN_POINT ( 'NONE',  ( 10.00000000000000000, -38.81885513160016643, 40.70683587897944022 ) ) ;
#11194=CARTESIAN_POINT ( 'NONE',  ( 10.00000000000000000, 5.876895005583349985, -62.72529079327799906 ) ) ;
#11195=AXIS2_PLACEMENT_3D ( 'NONE', #9164, #14787, #16416 ) ;
#11200=CARTESIAN_POINT ( 'NONE',  ( 0.000000000000000000, -46.27827401617379621, -31.97297851452475470 ) ) ;
#11202=VERTEX_POINT ( 'NONE', #17539 ) ;
#11205=CIRCLE ( 'NONE', #4235, 56.24900000005625600 ) ;
#11209=DIRECTION ( 'NONE',  ( 0.000000000000000000, 0.5877852522924741363, -0.8090169943749465631 ) ) ;
#11211=ORIENTED_EDGE ( 'NONE', *, *, #17189, .T. ) ;
#11215=ORIENTED_EDGE ( 'NONE', *, *, #5400, .F. ) ;
#11219=ORIENTED_EDGE ( 'NONE', *, *, #16677, .T. ) ;
#11220=CARTESIAN_POINT ( 'NONE',  ( 5.000000000000000000, -54.20017844242489247, -32.11449294037253566 ) ) ;
#11222=EDGE_CURVE ( 'NONE', #14229, #2916, #8701, .T. ) ;
#11223=CARTESIAN_POINT ( 'NONE',  ( 10.00000000000000000, 0.000000000000000000, 0.000000000000000000 ) ) ;
#11224=CARTESIAN_POINT ( 'NONE',  ( -10.00000000000000000, 0.000000000000000000, 0.000000000000000000 ) ) ;
#11225=VECTOR ( 'NONE', #5172, 1000.000000000000000 ) ;
#11227=ORIENTED_EDGE ( 'NONE', *, *, #4822, .F. ) ;
#11229=AXIS2_PLACEMENT_3D ( 'NONE', #11878, #8737, #4640 ) ;
#11235=CIRCLE ( 'NONE', #7574, 24.00000000002400213 ) ;
#11237=EDGE_CURVE ( 'NONE', #2561, #11050, #4450, .T. ) ;
#11238=AXIS2_PLACEMENT_3D ( 'NONE', #11388, #18541, #2732 ) ;
#11243=CARTESIAN_POINT ( 'NONE',  ( 10.00000000000000000, 40.19788616105679324, -48.50907078259339755 ) ) ;
#11249=EDGE_CURVE ( 'NONE', #6793, #3669, #8715, .T. ) ;
#11250=FACE_OUTER_BOUND ( 'NONE', #1529, .T. ) ;
#11253=CARTESIAN_POINT ( 'NONE',  ( 10.00000000000000000, 40.70683587898012235, -38.81885513159945589 ) ) ;
#11258=VERTEX_POINT ( 'NONE', #16016 ) ;
#11260=CARTESIAN_POINT ( 'NONE',  ( 0.000000000000000000, 0.000000000000000000, 0.000000000000000000 ) ) ;
#11266=CARTESIAN_POINT ( 'NONE',  ( 0.000000000000000000, 0.000000000000000000, 0.000000000000000000 ) ) ;
#11274=CARTESIAN_POINT ( 'NONE',  ( 10.00000000000000000, 40.58063702438344933, 39.14194549634378006 ) ) ;
#11278=FACE_OUTER_BOUND ( 'NONE', #14557, .T. ) ;
#11279=ORIENTED_EDGE ( 'NONE', *, *, #11793, .T. ) ;
#11280=EDGE_CURVE ( 'NONE', #2724, #16979, #16114, .T. ) ;
#11281=DIRECTION ( 'NONE',  ( -1.000000000000000000, -0.000000000000000000, -0.000000000000000000 ) ) ;
#11282=DIRECTION ( 'NONE',  ( -1.000000000000000000, 0.000000000000000000, -0.000000000000000000 ) ) ;
#11289=DIRECTION ( 'NONE',  ( 0.000000000000000000, 0.000000000000000000, 1.000000000000000000 ) ) ;
#11293=VERTEX_POINT ( 'NONE', #6481 ) ;
#11294=DIRECTION ( 'NONE',  ( 0.000000000000000000, 0.000000000000000000, 1.000000000000000000 ) ) ;
#11295=ORIENTED_EDGE ( 'NONE', *, *, #17390, .F. ) ;
#11300=ORIENTED_EDGE ( 'NONE', *, *, #17971, .F. ) ;
#11302=VECTOR ( 'NONE', #16400, 1000.000000000000000 ) ;
#11303=AXIS2_PLACEMENT_3D ( 'NONE', #18278, #5223, #9602 ) ;
#11304=ORIENTED_EDGE ( 'NONE', *, *, #9953, .F. ) ;
#11310=CARTESIAN_POINT ( 'NONE',  ( 0.000000000000000000, 55.83748330407397020, 7.813799127874245798 ) ) ;
#11311=ORIENTED_EDGE ( 'NONE', *, *, #5342, .F. ) ;
#11313=DIRECTION ( 'NONE',  ( -1.000000000000000000, -0.000000000000000000, -0.000000000000000000 ) ) ;
#11318=VERTEX_POINT ( 'NONE', #5040 ) ;
#11319=LINE ( 'NONE', #4282, #909 ) ;
#11320=CARTESIAN_POINT ( 'NONE',  ( 0.000000000000000000, 0.000000000000000000, 0.000000000000000000 ) ) ;
#11321=ADVANCED_FACE ( 'NONE', ( #6289 ), #3724, .T. ) ;
#11323=EDGE_CURVE ( 'NONE', #4962, #8010, #13444, .T. ) ;
#11326=EDGE_CURVE ( 'NONE', #18145, #9920, #17836, .T. ) ;
#11329=FACE_OUTER_BOUND ( 'NONE', #18108, .T. ) ;
#11332=CARTESIAN_POINT ( 'NONE',  ( 0.000000000000000000, 55.33199130079785277, 10.11537145609396404 ) ) ;
#11333=AXIS2_PLACEMENT_3D ( 'NONE', #2364, #11313, #8181 ) ;
#11334=EDGE_CURVE ( 'NONE', #11318, #18700, #9326, .T. ) ;
#11335=CYLINDRICAL_SURFACE ( 'NONE', #5730, 24.00000000002400213 ) ;
#11339=ORIENTED_EDGE ( 'NONE', *, *, #13101, .T. ) ;
#11343=CARTESIAN_POINT ( 'NONE',  ( 0.000000000000000000, 0.000000000000000000, 0.000000000000000000 ) ) ;
#11346=EDGE_CURVE ( 'NONE', #6188, #14229, #4758, .T. ) ;
#11351=EDGE_LOOP ( 'NONE', ( #13774, #9654, #13138, #6098 ) ) ;
#11353=FACE_OUTER_BOUND ( 'NONE', #3882, .T. ) ;
#11354=ORIENTED_EDGE ( 'NONE', *, *, #13415, .F. ) ;
#11355=LINE ( 'NONE', #17173, #4743 ) ;
#11356=CARTESIAN_POINT ( 'NONE',  ( 10.00000000000000000, 0.000000000000000000, 0.000000000000000000 ) ) ;
#11357=DIRECTION ( 'NONE',  ( -1.000000000000000000, 0.000000000000000000, 0.000000000000000000 ) ) ;
#11360=DIRECTION ( 'NONE',  ( 0.000000000000000000, 0.000000000000000000, 1.000000000000000000 ) ) ;
#11361=ORIENTED_EDGE ( 'NONE', *, *, #57, .F. ) ;
#11366=DIRECTION ( 'NONE',  ( -1.000000000000000000, 0.000000000000000000, 0.000000000000000000 ) ) ;
#11368=DIRECTION ( 'NONE',  ( 0.000000000000000000, 0.000000000000000000, 1.000000000000000000 ) ) ;
#11373=DIRECTION ( 'NONE',  ( -1.000000000000000000, 0.000000000000000000, 0.000000000000000000 ) ) ;
#11374=DIRECTION ( 'NONE',  ( -1.000000000000000000, -0.000000000000000000, 0.000000000000000000 ) ) ;
#11378=CARTESIAN_POINT ( 'NONE',  ( 10.00000000000000000, 53.29895248911675765, 18.38754094778260040 ) ) ;
#11379=CARTESIAN_POINT ( 'NONE',  ( 0.000000000000000000, 7.478235706488965739, 55.74967257055886449 ) ) ;
#11383=DIRECTION ( 'NONE',  ( 0.000000000000000000, 0.000000000000000000, 1.000000000000000000 ) ) ;
#11388=CARTESIAN_POINT ( 'NONE',  ( 10.00000000000000000, 0.000000000000000000, 0.000000000000000000 ) ) ;
#11394=ORIENTED_EDGE ( 'NONE', *, *, #3881, .F. ) ;
#11397=AXIS2_PLACEMENT_3D ( 'NONE', #16140, #8887, #11754 ) ;
#11414=VECTOR ( 'NONE', #15646, 1000.000000000000000 ) ;
#11417=VECTOR ( 'NONE', #3315, 1000.000000000000000 ) ;
#11420=DIRECTION ( 'NONE',  ( 0.000000000000000000, 0.4539904997395476927, -0.8910065241883673437 ) ) ;
#11424=EDGE_CURVE ( 'NONE', #13451, #16356, #17259, .T. ) ;
#11425=LINE ( 'NONE', #7413, #5740 ) ;
#11427=AXIS2_PLACEMENT_3D ( 'NONE', #17399, #5589, #11772 ) ;
#11432=DIRECTION ( 'NONE',  ( 0.000000000000000000, -0.9876883405951393247, 0.1564344650402205161 ) ) ;
#11440=AXIS2_PLACEMENT_3D ( 'NONE', #8517, #18704, #8695 ) ;
#11441=VECTOR ( 'NONE', #1778, 1000.000000000000000 ) ;
#11445=DIRECTION ( 'NONE',  ( 0.000000000000000000, 0.000000000000000000, 1.000000000000000000 ) ) ;
#11446=ORIENTED_EDGE ( 'NONE', *, *, #2087, .F. ) ;
#11451=EDGE_CURVE ( 'NONE', #16165, #5694, #13597, .T. ) ;
#11452=ADVANCED_FACE ( 'NONE', ( #17248, #1053, #8202, #18578, #6762, #5534, #4201 ), #11137, .F. ) ;
#11459=VERTEX_POINT ( 'NONE', #11332 ) ;
#11460=CIRCLE ( 'NONE', #12040, 24.00000000002399148 ) ;
#11467=CIRCLE ( 'NONE', #3244, 24.00000000002399858 ) ;
#11472=CIRCLE ( 'NONE', #7200, 24.00000000002399858 ) ;
#11474=CIRCLE ( 'NONE', #10539, 63.00000000006298961 ) ;
#11476=CYLINDRICAL_SURFACE ( 'NONE', #6383, 24.00000000002400213 ) ;
#11478=CIRCLE ( 'NONE', #1443, 24.00000000002400569 ) ;
#11480=CARTESIAN_POINT ( 'NONE',  ( 10.00000000000000000, 24.97244012287581683, -57.83923611457293390 ) ) ;
#11485=LINE ( 'NONE', #13106, #17455 ) ;
#11486=DIRECTION ( 'NONE',  ( -1.000000000000000000, 0.000000000000000000, -0.000000000000000000 ) ) ;
#11488=EDGE_LOOP ( 'NONE', ( #12537, #14444, #4991, #2976 ) ) ;
#11490=EDGE_CURVE ( 'NONE', #3688, #15880, #8110, .T. ) ;
#11491=CARTESIAN_POINT ( 'NONE',  ( 10.00000000000000000, 50.69000562871642046, 24.68609584167177218 ) ) ;
#11493=ORIENTED_EDGE ( 'NONE', *, *, #15543, .F. ) ;
#11494=AXIS2_PLACEMENT_3D ( 'NONE', #2520, #9855, #15664 ) ;
#11497=DIRECTION ( 'NONE',  ( -1.000000000000000000, -0.000000000000000000, -0.000000000000000000 ) ) ;
#11500=ORIENTED_EDGE ( 'NONE', *, *, #12607, .F. ) ;
#11504=ORIENTED_EDGE ( 'NONE', *, *, #5854, .F. ) ;
#11505=CIRCLE ( 'NONE', #3292, 24.00000000002399858 ) ;
#11508=CYLINDRICAL_SURFACE ( 'NONE', #1386, 24.00000000002399858 ) ;
#11512=ORIENTED_EDGE ( 'NONE', *, *, #5771, .T. ) ;
#11514=EDGE_CURVE ( 'NONE', #18225, #19, #14297, .T. ) ;
#11516=FILL_AREA_STYLE_COLOUR ( '', #7120 ) ;
#11520=CIRCLE ( 'NONE', #13342, 24.00000000002400569 ) ;
#11524=CARTESIAN_POINT ( 'NONE',  ( 4.999999999999999112, 13.79392154159135231, 61.47135697633785156 ) ) ;
#11529=CARTESIAN_POINT ( 'NONE',  ( 10.00000000000000000, 0.000000000000000000, 0.000000000000000000 ) ) ;
#11531=CARTESIAN_POINT ( 'NONE',  ( 0.000000000000000000, 55.83748330407408389, -7.813799127873475747 ) ) ;
#11533=CIRCLE ( 'NONE', #9082, 24.00000000002399858 ) ;
#11534=EDGE_CURVE ( 'NONE', #6648, #5427, #18458, .T. ) ;
#11536=DIRECTION ( 'NONE',  ( -1.000000000000000000, 0.000000000000000000, 0.000000000000000000 ) ) ;
#11537=CIRCLE ( 'NONE', #3322, 2.650000000000001243 ) ;
#11540=ORIENTED_EDGE ( 'NONE', *, *, #15276, .T. ) ;
#11543=ORIENTED_EDGE ( 'NONE', *, *, #11187, .F. ) ;
#11548=ORIENTED_EDGE ( 'NONE', *, *, #4811, .T. ) ;
#11550=DIRECTION ( 'NONE',  ( 0.000000000000000000, 0.000000000000000000, 1.000000000000000000 ) ) ;
#11551=VERTEX_POINT ( 'NONE', #878 ) ;
#11555=VECTOR ( 'NONE', #1112, 1000.000000000000000 ) ;
#11556=DIRECTION ( 'NONE',  ( 0.000000000000000000, 0.000000000000000000, 1.000000000000000000 ) ) ;
#11560=EDGE_LOOP ( 'NONE', ( #14739, #12964, #15771, #10260 ) ) ;
#11563=CARTESIAN_POINT ( 'NONE',  ( 10.00000000000000000, -1.017308535512791767, 56.37237871411032586 ) ) ;
#11567=EDGE_CURVE ( 'NONE', #12264, #17712, #4461, .T. ) ;
#11569=EDGE_CURVE ( 'NONE', #8684, #1351, #11474, .T. ) ;
#11571=VERTEX_POINT ( 'NONE', #11243 ) ;
#11572=CIRCLE ( 'NONE', #23, 24.00000000002399858 ) ;
#11577=CARTESIAN_POINT ( 'NONE',  ( 10.00000000000000000, 50.71018745830443919, 24.33982105418919417 ) ) ;
#11580=ORIENTED_EDGE ( 'NONE', *, *, #16099, .T. ) ;
#11583=CARTESIAN_POINT ( 'NONE',  ( 10.00000000000000000, 33.95787273855245303, 45.00825343885033192 ) ) ;
#11587=DIRECTION ( 'NONE',  ( -1.000000000000000000, -0.000000000000000000, -0.000000000000000000 ) ) ;
#11590=ORIENTED_EDGE ( 'NONE', *, *, #7263, .F. ) ;
#11592=EDGE_CURVE ( 'NONE', #10140, #11963, #2660, .T. ) ;
#11595=EDGE_CURVE ( 'NONE', #7581, #14103, #10854, .T. ) ;
#11596=VERTEX_POINT ( 'NONE', #17701 ) ;
#11598=CIRCLE ( 'NONE', #16456, 24.00000000002399858 ) ;
#11600=CARTESIAN_POINT ( 'NONE',  ( 0.000000000000000000, 10.11537145609457156, -55.33199130079773909 ) ) ;
#11602=ORIENTED_EDGE ( 'NONE', *, *, #1346, .F. ) ;
#11603=FACE_OUTER_BOUND ( 'NONE', #2725, .T. ) ;
#11605=ORIENTED_EDGE ( 'NONE', *, *, #1240, .F. ) ;
#11609=CARTESIAN_POINT ( 'NONE',  ( 10.00000000000000000, -33.71303790549235657, -53.22058882792234158 ) ) ;
#11610=CIRCLE ( 'NONE', #8263, 63.00000000006298961 ) ;
#11611=DIRECTION ( 'NONE',  ( -1.000000000000000000, 0.000000000000000000, 0.000000000000000000 ) ) ;
#11613=EDGE_CURVE ( 'NONE', #16829, #1379, #16351, .T. ) ;
#11614=EDGE_LOOP ( 'NONE', ( #2886, #3948, #1554, #12994 ) ) ;
#11615=ORIENTED_EDGE ( 'NONE', *, *, #10744, .T. ) ;
#11620=CARTESIAN_POINT ( 'NONE',  ( 0.000000000000000000, -45.00825343884996954, -33.95787273855293620 ) ) ;
#11627=CIRCLE ( 'NONE', #3409, 24.00000000002399858 ) ;
#11629=CARTESIAN_POINT ( 'NONE',  ( 5.000000000000000000, -23.24033432160398860, -58.55669782892485387 ) ) ;
#11634=AXIS2_PLACEMENT_3D ( 'NONE', #16848, #12754, #3795 ) ;
#11636=DIRECTION ( 'NONE',  ( 1.000000000000000000, 0.000000000000000000, 0.000000000000000000 ) ) ;
#11642=CARTESIAN_POINT ( 'NONE',  ( 10.00000000000000178, 0.000000000000000000, 0.000000000000000000 ) ) ;
#11643=ORIENTED_EDGE ( 'NONE', *, *, #803, .F. ) ;
#11648=DIRECTION ( 'NONE',  ( 0.000000000000000000, 0.000000000000000000, 1.000000000000000000 ) ) ;
#11653=CIRCLE ( 'NONE', #691, 63.00000000006298961 ) ;
#11656=CARTESIAN_POINT ( 'NONE',  ( 10.00000000000000000, 53.92768374110892893, -16.45250512421876010 ) ) ;
#11660=DIRECTION ( 'NONE',  ( -1.000000000000000000, 0.000000000000000000, 0.000000000000000000 ) ) ;
#11663=VERTEX_POINT ( 'NONE', #8930 ) ;
#11664=EDGE_CURVE ( 'NONE', #11128, #3467, #6296, .T. ) ;
#11667=DIRECTION ( 'NONE',  ( -1.000000000000000000, 0.000000000000000000, 0.000000000000000000 ) ) ;
#11671=CYLINDRICAL_SURFACE ( 'NONE', #15985, 24.00000000002399858 ) ;
#11674=ORIENTED_EDGE ( 'NONE', *, *, #13242, .F. ) ;
#11676=CIRCLE ( 'NONE', #412, 24.00000000002399858 ) ;
#11679=EDGE_CURVE ( 'NONE', #5010, #9182, #17556, .T. ) ;
#11680=DIRECTION ( 'NONE',  ( -1.000000000000000000, 0.000000000000000000, -0.000000000000000000 ) ) ;
#11681=ORIENTED_EDGE ( 'NONE', *, *, #3067, .T. ) ;
#11687=EDGE_CURVE ( 'NONE', #3393, #8632, #15128, .T. ) ;
#11688=ORIENTED_EDGE ( 'NONE', *, *, #10520, .F. ) ;
#11694=DIRECTION ( 'NONE',  ( 0.000000000000000000, 0.000000000000000000, 1.000000000000000000 ) ) ;
#11707=LINE ( 'NONE', #17610, #18470 ) ;
#11716=ORIENTED_EDGE ( 'NONE', *, *, #14450, .F. ) ;
#11718=DIRECTION ( 'NONE',  ( -0.000000000000000000, 0.000000000000000000, 1.000000000000000000 ) ) ;
#11724=CARTESIAN_POINT ( 'NONE',  ( 10.00000000000000000, -53.29895248911662264, -18.38754094778296277 ) ) ;
#11730=LINE ( 'NONE', #17637, #2683 ) ;
#11735=ORIENTED_EDGE ( 'NONE', *, *, #4927, .T. ) ;
#11739=AXIS2_PLACEMENT_3D ( 'NONE', #4426, #4340, #15868 ) ;
#11745=VECTOR ( 'NONE', #9239, 1000.000000000000000 ) ;
#11749=CARTESIAN_POINT ( 'NONE',  ( 10.00000000000000000, -4.007856633823827508, 62.87238730325619684 ) ) ;
#11753=DIRECTION ( 'NONE',  ( -1.000000000000000000, -0.000000000000000000, -0.000000000000000000 ) ) ;
#11754=DIRECTION ( 'NONE',  ( 0.000000000000000000, -0.3090169943749351278, -0.9510565162951575280 ) ) ;
#11757=ORIENTED_EDGE ( 'NONE', *, *, #2740, .T. ) ;
#11761=DIRECTION ( 'NONE',  ( -1.000000000000000000, -0.000000000000000000, -0.000000000000000000 ) ) ;
#11764=CARTESIAN_POINT ( 'NONE',  ( 0.000000000000000000, 62.87238730325621106, 4.007856633823609016 ) ) ;
#11768=AXIS2_PLACEMENT_3D ( 'NONE', #3034, #2655, #11694 ) ;
#11769=AXIS2_PLACEMENT_3D ( 'NONE', #3352, #10668, #10574 ) ;
#11772=DIRECTION ( 'NONE',  ( 0.000000000000000000, 0.9510565162951521989, 0.3090169943749515036 ) ) ;
#11774=DIRECTION ( 'NONE',  ( -1.000000000000000000, 0.000000000000000000, -0.000000000000000000 ) ) ;
#11777=AXIS2_PLACEMENT_3D ( 'NONE', #17425, #4376, #10179 ) ;
#11779=FACE_OUTER_BOUND ( 'NONE', #8741, .T. ) ;
#11786=VERTEX_POINT ( 'NONE', #9029 ) ;
#11790=DIRECTION ( 'NONE',  ( 0.000000000000000000, -0.5877852522924624790, -0.8090169943749551118 ) ) ;
#11793=EDGE_CURVE ( 'NONE', #7149, #18521, #1885, .T. ) ;
#11794=AXIS2_PLACEMENT_3D ( 'NONE', #1848, #7650, #13477 ) ;
#11800=EDGE_LOOP ( 'NONE', ( #1429, #15194, #9554, #2167 ) ) ;
#11801=CARTESIAN_POINT ( 'NONE',  ( 0.000000000000000000, 0.000000000000000000, 0.000000000000000000 ) ) ;
#11808=CIRCLE ( 'NONE', #6020, 24.00000000002399858 ) ;
#11812=CARTESIAN_POINT ( 'NONE',  ( 10.00000000000000000, 0.000000000000000000, 0.000000000000000000 ) ) ;
#11814=VERTEX_POINT ( 'NONE', #4847 ) ;
#11815=DIRECTION ( 'NONE',  ( 0.000000000000000000, 0.000000000000000000, -1.000000000000000000 ) ) ;
#11816=CARTESIAN_POINT ( 'NONE',  ( 10.00000000000000000, 0.000000000000000000, 0.000000000000000000 ) ) ;
#11818=AXIS2_PLACEMENT_3D ( 'NONE', #5145, #7999, #15249 ) ;
#11819=EDGE_CURVE ( 'NONE', #16951, #8859, #6617, .T. ) ;
#11820=ORIENTED_EDGE ( 'NONE', *, *, #4263, .F. ) ;
#11822=CARTESIAN_POINT ( 'NONE',  ( 0.000000000000000000, -62.72529079327802748, -5.876895005583096854 ) ) ;
#11826=CARTESIAN_POINT ( 'NONE',  ( 10.00000000000000000, -10.11537145609335830, -55.33199130079796646 ) ) ;
#11838=ORIENTED_EDGE ( 'NONE', *, *, #10018, .T. ) ;
#11843=DIRECTION ( 'NONE',  ( -1.000000000000000000, -0.000000000000000000, -0.000000000000000000 ) ) ;
#11845=CARTESIAN_POINT ( 'NONE',  ( 10.00000000000000000, -48.50907078259351835, -40.19788616105662982 ) ) ;
#11849=LINE ( 'NONE', #10604, #8789 ) ;
#11850=ORIENTED_EDGE ( 'NONE', *, *, #4240, .F. ) ;
#11851=CYLINDRICAL_SURFACE ( 'NONE', #1695, 24.00000000002399858 ) ;
#11858=VERTEX_POINT ( 'NONE', #658 ) ;
#11862=DIRECTION ( 'NONE',  ( 0.000000000000000000, 0.000000000000000000, 1.000000000000000000 ) ) ;
#11864=CARTESIAN_POINT ( 'NONE',  ( 10.00000000000000000, 0.000000000000000000, 0.000000000000000000 ) ) ;
#11869=FACE_OUTER_BOUND ( 'NONE', #8152, .T. ) ;
#11870=ORIENTED_EDGE ( 'NONE', *, *, #16685, .T. ) ;
#11871=AXIS2_PLACEMENT_3D ( 'NONE', #11260, #1539, #17632 ) ;
#11874=ORIENTED_EDGE ( 'NONE', *, *, #1066, .T. ) ;
#11876=DIRECTION ( 'NONE',  ( -1.000000000000000000, 0.000000000000000000, -0.000000000000000000 ) ) ;
#11878=CARTESIAN_POINT ( 'NONE',  ( 0.000000000000000000, 0.000000000000000000, 0.000000000000000000 ) ) ;
#11879=CIRCLE ( 'NONE', #3684, 2.649999999999999467 ) ;
#11882=ORIENTED_EDGE ( 'NONE', *, *, #112, .T. ) ;
#11884=LINE ( 'NONE', #14741, #3194 ) ;
#11885=CARTESIAN_POINT ( 'NONE',  ( 10.00000000000000000, 0.000000000000000000, 0.000000000000000000 ) ) ;
#11887=DIRECTION ( 'NONE',  ( -1.000000000000000000, 0.000000000000000000, -0.000000000000000000 ) ) ;
#11893=EDGE_CURVE ( 'NONE', #16334, #17597, #9591, .T. ) ;
#11897=ORIENTED_EDGE ( 'NONE', *, *, #18440, .T. ) ;
#11898=DIRECTION ( 'NONE',  ( 0.000000000000000000, -0.9510565162951565288, 0.3090169943749382364 ) ) ;
#11899=FACE_OUTER_BOUND ( 'NONE', #2101, .T. ) ;
#11902=EDGE_LOOP ( 'NONE', ( #15327, #10580, #3263, #7633 ) ) ;
#11908=DIRECTION ( 'NONE',  ( 0.000000000000000000, 0.000000000000000000, 1.000000000000000000 ) ) ;
#11909=VECTOR ( 'NONE', #11611, 1000.000000000000000 ) ;
#11911=CARTESIAN_POINT ( 'NONE',  ( 10.00000000000000000, -40.58063702438316511, -39.14194549634407139 ) ) ;
#11912=FACE_OUTER_BOUND ( 'NONE', #7373, .T. ) ;
#11913=DIRECTION ( 'NONE',  ( 0.000000000000000000, 0.000000000000000000, 1.000000000000000000 ) ) ;
#11916=ORIENTED_EDGE ( 'NONE', *, *, #18550, .F. ) ;
#11917=EDGE_CURVE ( 'NONE', #2800, #16028, #2546, .T. ) ;
#11920=CARTESIAN_POINT ( 'NONE',  ( 10.00000000000000000, 0.000000000000000000, 0.000000000000000000 ) ) ;
#11932=DIRECTION ( 'NONE',  ( -1.000000000000000000, -0.000000000000000000, -0.000000000000000000 ) ) ;
#11941=DIRECTION ( 'NONE',  ( 0.000000000000000000, -0.5877852522924801315, 0.8090169943749422332 ) ) ;
#11942=VERTEX_POINT ( 'NONE', #11114 ) ;
#11948=CARTESIAN_POINT ( 'NONE',  ( 5.000000000000000000, -62.87238730325618263, -4.007856633824053105 ) ) ;
#11951=AXIS2_PLACEMENT_3D ( 'NONE', #830, #2335, #2241 ) ;
#11952=FACE_OUTER_BOUND ( 'NONE', #15381, .T. ) ;
#11955=CARTESIAN_POINT ( 'NONE',  ( 10.00000000000000000, 16.45250512421934630, -53.92768374110874419 ) ) ;
#11957=FACE_OUTER_BOUND ( 'NONE', #17045, .T. ) ;
#11960=ORIENTED_EDGE ( 'NONE', *, *, #986, .T. ) ;
#11961=CYLINDRICAL_SURFACE ( 'NONE', #17823, 24.00000000002399858 ) ;
#11963=VERTEX_POINT ( 'NONE', #8274 ) ;
#11965=DIRECTION ( 'NONE',  ( -1.000000000000000000, 0.000000000000000000, 0.000000000000000000 ) ) ;
#11971=VERTEX_POINT ( 'NONE', #2645 ) ;
#11974=DIRECTION ( 'NONE',  ( 0.000000000000000000, 0.4539904997395412534, 0.8910065241883706744 ) ) ;
#11976=ORIENTED_EDGE ( 'NONE', *, *, #1727, .F. ) ;
#11978=CARTESIAN_POINT ( 'NONE',  ( 10.00000000000000000, 50.71018745830443919, 24.33982105418919417 ) ) ;
#11983=EDGE_CURVE ( 'NONE', #5722, #538, #10255, .T. ) ;
#11984=ORIENTED_EDGE ( 'NONE', *, *, #11613, .T. ) ;
#11985=CYLINDRICAL_SURFACE ( 'NONE', #6346, 24.00000000002399858 ) ;
#11986=DIRECTION ( 'NONE',  ( -1.000000000000000000, 0.000000000000000000, -0.000000000000000000 ) ) ;
#11987=ORIENTED_EDGE ( 'NONE', *, *, #18761, .T. ) ;
#11996=VECTOR ( 'NONE', #16380, 1000.000000000000000 ) ;
#12000=EDGE_LOOP ( 'NONE', ( #13419, #17633, #14106, #14542 ) ) ;
#12002=DIRECTION ( 'NONE',  ( -1.000000000000000000, 0.000000000000000000, 0.000000000000000000 ) ) ;
#12004=ORIENTED_EDGE ( 'NONE', *, *, #2141, .F. ) ;
#12010=ADVANCED_FACE ( 'NONE', ( #4792 ), #13471, .T. ) ;
#12012=DIRECTION ( 'NONE',  ( 1.000000000000000000, 0.000000000000000000, 0.000000000000000000 ) ) ;
#12017=CARTESIAN_POINT ( 'NONE',  ( 10.00000000000000000, 0.000000000000000000, 0.000000000000000000 ) ) ;
#12018=ADVANCED_FACE ( 'NONE', ( #7733 ), #11508, .T. ) ;
#12020=CARTESIAN_POINT ( 'NONE',  ( 0.000000000000000000, -55.51919907100660367, 9.823366686500467182 ) ) ;
#12024=EDGE_LOOP ( 'NONE', ( #15316, #17828, #7651, #18352 ) ) ;
#12029=VERTEX_POINT ( 'NONE', #8971 ) ;
#12031=VECTOR ( 'NONE', #4770, 1000.000000000000000 ) ;
#12032=CARTESIAN_POINT ( 'NONE',  ( 10.00000000000000000, 62.72529079327814117, -5.876895005581764586 ) ) ;
#12035=CYLINDRICAL_SURFACE ( 'NONE', #14366, 24.00000000002400213 ) ;
#12040=AXIS2_PLACEMENT_3D ( 'NONE', #16990, #5350, #11055 ) ;
#12041=DIRECTION ( 'NONE',  ( -1.000000000000000000, 0.000000000000000000, 0.000000000000000000 ) ) ;
#12042=DIRECTION ( 'NONE',  ( -1.000000000000000000, -0.000000000000000000, 0.000000000000000000 ) ) ;
#12043=CIRCLE ( 'NONE', #11440, 2.649999999999999467 ) ;
#12048=CARTESIAN_POINT ( 'NONE',  ( 10.00000000000000000, 40.58063702438344933, 39.14194549634378006 ) ) ;
#12050=CARTESIAN_POINT ( 'NONE',  ( 0.000000000000000000, 0.000000000000000000, 0.000000000000000000 ) ) ;
#12052=EDGE_CURVE ( 'NONE', #16334, #4819, #7759, .T. ) ;
#12053=FACE_OUTER_BOUND ( 'NONE', #7101, .T. ) ;
#12055=CIRCLE ( 'NONE', #10241, 56.24900000005625600 ) ;
#12056=VERTEX_POINT ( 'NONE', #17220 ) ;
#12058=AXIS2_PLACEMENT_3D ( 'NONE', #13895, #12364, #9703 ) ;
#12059=CARTESIAN_POINT ( 'NONE',  ( 10.00000000000000000, 0.000000000000000000, 0.000000000000000000 ) ) ;
#12063=DIRECTION ( 'NONE',  ( -1.000000000000000000, 0.000000000000000000, 0.000000000000000000 ) ) ;
#12064=AXIS2_PLACEMENT_3D ( 'NONE', #2208, #4964, #12496 ) ;
#12066=LINE ( 'NONE', #1969, #450 ) ;
#12067=CIRCLE ( 'NONE', #14809, 30.00000000000000000 ) ;
#12070=AXIS2_PLACEMENT_3D ( 'NONE', #6926, #1026, #11209 ) ;
#12071=ORIENTED_EDGE ( 'NONE', *, *, #4822, .T. ) ;
#12073=VECTOR ( 'NONE', #13379, 1000.000000000000000 ) ;
#12076=VERTEX_POINT ( 'NONE', #14439 ) ;
#12078=EDGE_CURVE ( 'NONE', #14399, #980, #9978, .T. ) ;
#12083=DIRECTION ( 'NONE',  ( -1.000000000000000000, 0.000000000000000000, 0.000000000000000000 ) ) ;
#12084=DIRECTION ( 'NONE',  ( -1.000000000000000000, -0.000000000000000000, -0.000000000000000000 ) ) ;
#12088=AXIS2_PLACEMENT_3D ( 'NONE', #1606, #7410, #14461 ) ;
#12090=AXIS2_PLACEMENT_3D ( 'NONE', #14532, #7948, #17955 ) ;
#12092=EDGE_CURVE ( 'NONE', #14358, #407, #17746, .T. ) ;
#12105=CARTESIAN_POINT ( 'NONE',  ( 10.00000000000000000, -61.03368945066424089, -15.61693798565562119 ) ) ;
#12109=ORIENTED_EDGE ( 'NONE', *, *, #4945, .T. ) ;
#12113=AXIS2_PLACEMENT_3D ( 'NONE', #6697, #6595, #11158 ) ;
#12119=DIRECTION ( 'NONE',  ( -1.000000000000000000, 0.000000000000000000, 0.000000000000000000 ) ) ;
#12120=CARTESIAN_POINT ( 'NONE',  ( 0.000000000000000000, 41.62350880771921169, 47.29147401531970019 ) ) ;
#12121=CARTESIAN_POINT ( 'NONE',  ( -10.00000000000000000, -5.120903701083534543E-13, -45.00000000000000000 ) ) ;
#12122=AXIS2_PLACEMENT_3D ( 'NONE', #17468, #6906, #8703 ) ;
#12128=AXIS2_PLACEMENT_3D ( 'NONE', #2657, #12853, #1145 ) ;
#12130=DIRECTION ( 'NONE',  ( -1.000000000000000000, 0.000000000000000000, 0.000000000000000000 ) ) ;
#12138=DIRECTION ( 'NONE',  ( 1.000000000000000000, 0.000000000000000000, -0.000000000000000000 ) ) ;
#12145=VECTOR ( 'NONE', #16830, 1000.000000000000000 ) ;
#12146=ADVANCED_FACE ( 'NONE', ( #9259 ), #606, .T. ) ;
#12147=CARTESIAN_POINT ( 'NONE',  ( -10.00000000000000000, 0.000000000000000000, 0.000000000000000000 ) ) ;
#12149=CARTESIAN_POINT ( 'NONE',  ( -10.00000000000000000, 42.79754323328179311, -13.90576474687299680 ) ) ;
#12150=ORIENTED_EDGE ( 'NONE', *, *, #9778, .T. ) ;
#12152=ADVANCED_FACE ( 'NONE', ( #10776 ), #16598, .T. ) ;
#12153=ORIENTED_EDGE ( 'NONE', *, *, #541, .T. ) ;
#12157=CARTESIAN_POINT ( 'NONE',  ( 0.000000000000000000, -57.83923611457302627, -24.97244012287563919 ) ) ;
#12162=DIRECTION ( 'NONE',  ( 0.000000000000000000, -0.8090169943749530024, 0.5877852522924653655 ) ) ;
#12165=ADVANCED_FACE ( 'NONE', ( #13746 ), #7838, .T. ) ;
#12166=VERTEX_POINT ( 'NONE', #5170 ) ;
#12168=EDGE_CURVE ( 'NONE', #11128, #10830, #5008, .T. ) ;
#12171=CIRCLE ( 'NONE', #16171, 63.00000000006298961 ) ;
#12188=FACE_OUTER_BOUND ( 'NONE', #5372, .T. ) ;
#12189=EDGE_CURVE ( 'NONE', #9984, #3645, #9543, .T. ) ;
#12192=CARTESIAN_POINT ( 'NONE',  ( 10.00000000000000000, 10.11537145609375798, 55.33199130079789541 ) ) ;
#12195=DIRECTION ( 'NONE',  ( -1.000000000000000000, 0.000000000000000000, 0.000000000000000000 ) ) ;
#12197=ORIENTED_EDGE ( 'NONE', *, *, #1777, .T. ) ;
#12201=ORIENTED_EDGE ( 'NONE', *, *, #14933, .F. ) ;
#12203=EDGE_CURVE ( 'NONE', #14748, #1691, #7447, .T. ) ;
#12204=VERTEX_POINT ( 'NONE', #2125 ) ;
#12205=AXIS2_PLACEMENT_3D ( 'NONE', #10527, #14631, #8998 ) ;
#12206=ORIENTED_EDGE ( 'NONE', *, *, #9515, .T. ) ;
#12207=ORIENTED_EDGE ( 'NONE', *, *, #15174, .F. ) ;
#12209=DIRECTION ( 'NONE',  ( 0.000000000000000000, 0.000000000000000000, 1.000000000000000000 ) ) ;
#12216=CARTESIAN_POINT ( 'NONE',  ( 0.000000000000000000, -16.45250512421895550, 53.92768374110886498 ) ) ;
#12218=CARTESIAN_POINT ( 'NONE',  ( 10.00000000000000000, 18.38754094778241210, 53.29895248911682870 ) ) ;
#12219=ORIENTED_EDGE ( 'NONE', *, *, #8560, .F. ) ;
#12226=DIRECTION ( 'NONE',  ( -1.000000000000000000, 0.000000000000000000, -0.000000000000000000 ) ) ;
#12230=DIRECTION ( 'NONE',  ( -1.000000000000000000, 0.000000000000000000, 0.000000000000000000 ) ) ;
#12237=EDGE_CURVE ( 'NONE', #18322, #8760, #7154, .T. ) ;
#12241=CYLINDRICAL_SURFACE ( 'NONE', #11188, 30.00000000000000000 ) ;
#12246=ORIENTED_EDGE ( 'NONE', *, *, #17614, .T. ) ;
#12247=ORIENTED_EDGE ( 'NONE', *, *, #14933, .T. ) ;
#12248=DIRECTION ( 'NONE',  ( 0.000000000000000000, 0.8090169943749486725, -0.5877852522924713607 ) ) ;
#12254=DIRECTION ( 'NONE',  ( -1.000000000000000000, 0.000000000000000000, -0.000000000000000000 ) ) ;
#12256=ORIENTED_EDGE ( 'NONE', *, *, #12394, .T. ) ;
#12262=CARTESIAN_POINT ( 'NONE',  ( 10.00000000000000000, 26.45033635316149301, 33.75576474687247241 ) ) ;
#12264=VERTEX_POINT ( 'NONE', #8020 ) ;
#12269=CYLINDRICAL_SURFACE ( 'NONE', #7985, 24.00000000002399858 ) ;
#12279=ORIENTED_EDGE ( 'NONE', *, *, #17063, .F. ) ;
#12280=ORIENTED_EDGE ( 'NONE', *, *, #1469, .F. ) ;
#12281=DIRECTION ( 'NONE',  ( 1.000000000000000000, 0.000000000000000000, 0.000000000000000000 ) ) ;
#12283=DIRECTION ( 'NONE',  ( -1.000000000000000000, -0.000000000000000000, -0.000000000000000000 ) ) ;
#12284=CARTESIAN_POINT ( 'NONE',  ( 4.999999999999999112, 13.79392154159224404, -61.47135697633764551 ) ) ;
#12297=DIRECTION ( 'NONE',  ( 0.000000000000000000, 0.000000000000000000, -1.000000000000000000 ) ) ;
#12302=DIRECTION ( 'NONE',  ( -1.000000000000000000, -0.000000000000000000, -0.000000000000000000 ) ) ;
#12309=DIRECTION ( 'NONE',  ( 0.000000000000000000, 0.000000000000000000, 1.000000000000000000 ) ) ;
#12312=EDGE_LOOP ( 'NONE', ( #17422, #7490 ) ) ;
#12313=DIRECTION ( 'NONE',  ( 0.000000000000000000, 0.000000000000000000, 1.000000000000000000 ) ) ;
#12316=FACE_OUTER_BOUND ( 'NONE', #4753, .T. ) ;
#12318=VECTOR ( 'NONE', #10429, 1000.000000000000000 ) ;
#12322=DIRECTION ( 'NONE',  ( -1.000000000000000000, 0.000000000000000000, 0.000000000000000000 ) ) ;
#12324=VECTOR ( 'NONE', #15701, 1000.000000000000000 ) ;
#12327=DIRECTION ( 'NONE',  ( 0.000000000000000000, 0.000000000000000000, 1.000000000000000000 ) ) ;
#12331=CARTESIAN_POINT ( 'NONE',  ( 10.00000000000000000, 10.11537145609375798, 55.33199130079789541 ) ) ;
#12332=VECTOR ( 'NONE', #586, 1000.000000000000000 ) ;
#12335=DIRECTION ( 'NONE',  ( 0.000000000000000000, 0.000000000000000000, 1.000000000000000000 ) ) ;
#12342=AXIS2_PLACEMENT_3D ( 'NONE', #11491, #18539, #5676 ) ;
#12347=DIRECTION ( 'NONE',  ( 0.000000000000000000, -0.4539904997395540764, 0.8910065241883640130 ) ) ;
#12348=ORIENTED_EDGE ( 'NONE', *, *, #9183, .T. ) ;
#12349=CIRCLE ( 'NONE', #3542, 24.00000000002400569 ) ;
#12350=ORIENTED_EDGE ( 'NONE', *, *, #648, .F. ) ;
#12352=CYLINDRICAL_SURFACE ( 'NONE', #10194, 24.00000000002399858 ) ;
#12353=DIRECTION ( 'NONE',  ( -1.000000000000000000, 0.000000000000000000, -0.000000000000000000 ) ) ;
#12354=CIRCLE ( 'NONE', #5965, 63.00000000006298961 ) ;
#12357=DIRECTION ( 'NONE',  ( 1.000000000000000000, 0.000000000000000000, 0.000000000000000000 ) ) ;
#12360=ORIENTED_EDGE ( 'NONE', *, *, #5385, .F. ) ;
#12364=DIRECTION ( 'NONE',  ( -1.000000000000000000, -0.000000000000000000, -0.000000000000000000 ) ) ;
#12369=EDGE_CURVE ( 'NONE', #11663, #13852, #12796, .T. ) ;
#12376=AXIS2_PLACEMENT_3D ( 'NONE', #18610, #18410, #4236 ) ;
#12377=ORIENTED_EDGE ( 'NONE', *, *, #5976, .T. ) ;
#12379=FACE_OUTER_BOUND ( 'NONE', #11113, .T. ) ;
#12381=DIRECTION ( 'NONE',  ( 0.000000000000000000, -0.8090169943749402348, -0.5877852522924830181 ) ) ;
#12382=DIRECTION ( 'NONE',  ( 0.000000000000000000, 0.000000000000000000, 1.000000000000000000 ) ) ;
#12383=EDGE_CURVE ( 'NONE', #12204, #11293, #14159, .T. ) ;
#12384=CARTESIAN_POINT ( 'NONE',  ( 10.00000000000000000, -56.23315539212691050, 1.335003989221430487 ) ) ;
#12387=ORIENTED_EDGE ( 'NONE', *, *, #5281, .T. ) ;
#12393=VECTOR ( 'NONE', #10328, 1000.000000000000000 ) ;
#12394=EDGE_CURVE ( 'NONE', #728, #6735, #4316, .T. ) ;
#12397=ORIENTED_EDGE ( 'NONE', *, *, #17845, .F. ) ;
#12401=CIRCLE ( 'NONE', #12712, 24.00000000002399858 ) ;
#12403=DIRECTION ( 'NONE',  ( 0.000000000000000000, 0.000000000000000000, -1.000000000000000000 ) ) ;
#12404=AXIS2_PLACEMENT_3D ( 'NONE', #15766, #1475, #7085 ) ;
#12405=CIRCLE ( 'NONE', #10872, 24.00000000002399858 ) ;
#12412=ORIENTED_EDGE ( 'NONE', *, *, #4143, .F. ) ;
#12420=CIRCLE ( 'NONE', #2372, 56.24900000005625600 ) ;
#12431=VERTEX_POINT ( 'NONE', #5355 ) ;
#12432=CARTESIAN_POINT ( 'NONE',  ( 10.00000000000000000, -18.64666490672410148, 53.06836994729227541 ) ) ;
#12433=AXIS2_PLACEMENT_3D ( 'NONE', #8301, #5817, #20 ) ;
#12436=UNCERTAINTY_MEASURE_WITH_UNIT (LENGTH_MEASURE( 1.000000000000000082E-05 ), #5426, 'distance_accuracy_value', 'NONE');
#12438=DIRECTION ( 'NONE',  ( -1.000000000000000000, -0.000000000000000000, -0.000000000000000000 ) ) ;
#12439=ORIENTED_EDGE ( 'NONE', *, *, #16807, .T. ) ;
#12441=LINE ( 'NONE', #9860, #17440 ) ;
#12443=ORIENTED_EDGE ( 'NONE', *, *, #15636, .T. ) ;
#12446=EDGE_CURVE ( 'NONE', #3960, #15091, #16909, .T. ) ;
#12447=VERTEX_POINT ( 'NONE', #2503 ) ;
#12449=CIRCLE ( 'NONE', #2412, 63.00000000006298961 ) ;
#12451=EDGE_CURVE ( 'NONE', #8692, #4390, #7465, .T. ) ;
#12456=CIRCLE ( 'NONE', #4856, 56.24900000005625600 ) ;
#12457=EDGE_LOOP ( 'NONE', ( #17215, #11984, #12470, #7262 ) ) ;
#12465=CARTESIAN_POINT ( 'NONE',  ( 5.000000000000000000, -13.79392154159090467, -61.47135697633794393 ) ) ;
#12470=ORIENTED_EDGE ( 'NONE', *, *, #9246, .F. ) ;
#12472=FACE_OUTER_BOUND ( 'NONE', #3728, .T. ) ;
#12477=DIRECTION ( 'NONE',  ( -1.000000000000000000, 0.000000000000000000, -0.000000000000000000 ) ) ;
#12484=LINE ( 'NONE', #1912, #12332 ) ;
#12495=CIRCLE ( 'NONE', #13417, 24.00000000002400569 ) ;
#12496=DIRECTION ( 'NONE',  ( 0.000000000000000000, 0.4539904997395479147, -0.8910065241883673437 ) ) ;
#12501=DIRECTION ( 'NONE',  ( 0.000000000000000000, 0.000000000000000000, 1.000000000000000000 ) ) ;
#12503=CARTESIAN_POINT ( 'NONE',  ( 0.000000000000000000, -45.00825343885045271, 33.95787273855228960 ) ) ;
#12504=CARTESIAN_POINT ( 'NONE',  ( 0.000000000000000000, 0.000000000000000000, 0.000000000000000000 ) ) ;
#12508=EDGE_LOOP ( 'NONE', ( #4846, #7329, #2137, #15867 ) ) ;
#12510=DIRECTION ( 'NONE',  ( 0.000000000000000000, 0.000000000000000000, -1.000000000000000000 ) ) ;
#12512=EDGE_LOOP ( 'NONE', ( #12803, #9361, #4824, #14059 ) ) ;
#12513=VERTEX_POINT ( 'NONE', #16401 ) ;
#12515=DIRECTION ( 'NONE',  ( -1.000000000000000000, -0.000000000000000000, -0.000000000000000000 ) ) ;
#12518=CARTESIAN_POINT ( 'NONE',  ( 0.000000000000000000, 15.61693798565496394, 61.03368945066441142 ) ) ;
#12526=CARTESIAN_POINT ( 'NONE',  ( 0.000000000000000000, -50.71018745830426866, -24.33982105418955655 ) ) ;
#12528=AXIS2_PLACEMENT_3D ( 'NONE', #11042, #3814, #14095 ) ;
#12529=CARTESIAN_POINT ( 'NONE',  ( 0.000000000000000000, 18.64666490672370713, 53.06836994729239620 ) ) ;
#12530=CYLINDRICAL_SURFACE ( 'NONE', #4947, 24.00000000002399503 ) ;
#12532=ORIENTED_EDGE ( 'NONE', *, *, #4122, .F. ) ;
#12533=ORIENTED_EDGE ( 'NONE', *, *, #15287, .T. ) ;
#12534=EDGE_CURVE ( 'NONE', #11963, #11942, #33, .T. ) ;
#12535=CARTESIAN_POINT ( 'NONE',  ( 10.00000000000000000, -18.38754094778278869, 53.29895248911668659 ) ) ;
#12537=ORIENTED_EDGE ( 'NONE', *, *, #17653, .F. ) ;
#12542=AXIS2_PLACEMENT_3D ( 'NONE', #7900, #6471, #12763 ) ;
#12547=DIRECTION ( 'NONE',  ( 0.000000000000000000, 0.000000000000000000, 1.000000000000000000 ) ) ;
#12548=DIRECTION ( 'NONE',  ( 1.000000000000000000, -0.000000000000000000, 0.000000000000000000 ) ) ;
#12553=CARTESIAN_POINT ( 'NONE',  ( 10.00000000000000000, -5.120903701083534543E-13, -45.00000000000000000 ) ) ;
#12555=ORIENTED_EDGE ( 'NONE', *, *, #5771, .F. ) ;
#12561=VECTOR ( 'NONE', #13185, 1000.000000000000000 ) ;
#12567=VERTEX_POINT ( 'NONE', #10206 ) ;
#12571=CYLINDRICAL_SURFACE ( 'NONE', #1142, 63.00000000006298961 ) ;
#12574=CARTESIAN_POINT ( 'NONE',  ( 0.000000000000000000, -53.22058882792172341, -33.71303790549333712 ) ) ;
#12575=CARTESIAN_POINT ( 'NONE',  ( -10.00000000000000000, 0.000000000000000000, 0.000000000000000000 ) ) ;
#12577=ORIENTED_EDGE ( 'NONE', *, *, #1376, .F. ) ;
#12579=CARTESIAN_POINT ( 'NONE',  ( 5.000000000000000000, -62.72529079327811274, 5.876895005582225551 ) ) ;
#12581=ORIENTED_EDGE ( 'NONE', *, *, #10018, .F. ) ;
#12582=VECTOR ( 'NONE', #4611, 1000.000000000000000 ) ;
#12583=EDGE_LOOP ( 'NONE', ( #13996, #8638, #14662, #17573 ) ) ;
#12587=CARTESIAN_POINT ( 'NONE',  ( 10.00000000000000000, 10.11537145609457156, -55.33199130079773909 ) ) ;
#12589=CARTESIAN_POINT ( 'NONE',  ( 10.00000000000000000, 24.33982105418901298, 50.71018745830453156 ) ) ;
#12592=DIRECTION ( 'NONE',  ( -1.000000000000000000, 0.000000000000000000, 0.000000000000000000 ) ) ;
#12595=ORIENTED_EDGE ( 'NONE', *, *, #13415, .T. ) ;
#12606=EDGE_CURVE ( 'NONE', #9916, #3285, #7167, .T. ) ;
#12607=EDGE_CURVE ( 'NONE', #10536, #1171, #5025, .T. ) ;
#12608=EDGE_CURVE ( 'NONE', #16951, #8709, #16020, .T. ) ;
#12610=CARTESIAN_POINT ( 'NONE',  ( 10.00000000000000000, 53.92768374110868734, 16.45250512421953459 ) ) ;
#12611=EDGE_CURVE ( 'NONE', #15930, #8606, #5940, .T. ) ;
#12620=EDGE_CURVE ( 'NONE', #3492, #2015, #12484, .T. ) ;
#12622=FACE_OUTER_BOUND ( 'NONE', #6503, .T. ) ;
#12623=DIRECTION ( 'NONE',  ( 0.000000000000000000, -0.9876883405951394357, 0.1564344650402205994 ) ) ;
#12628=CYLINDRICAL_SURFACE ( 'NONE', #474, 24.00000000002400213 ) ;
#12630=ORIENTED_EDGE ( 'NONE', *, *, #13674, .T. ) ;
#12635=AXIS2_PLACEMENT_3D ( 'NONE', #9275, #429, #246 ) ;
#12638=EDGE_CURVE ( 'NONE', #8411, #13451, #13811, .T. ) ;
#12641=VERTEX_POINT ( 'NONE', #14969 ) ;
#12643=DIRECTION ( 'NONE',  ( 0.000000000000000000, 0.000000000000000000, 1.000000000000000000 ) ) ;
#12645=ORIENTED_EDGE ( 'NONE', *, *, #9564, .F. ) ;
#12646=DIRECTION ( 'NONE',  ( 1.000000000000000000, 0.000000000000000000, 0.000000000000000000 ) ) ;
#12649=CARTESIAN_POINT ( 'NONE',  ( 0.000000000000000000, -4.007856633822952652, -62.87238730325625369 ) ) ;
#12651=ORIENTED_EDGE ( 'NONE', *, *, #3480, .F. ) ;
#12653=AXIS2_PLACEMENT_3D ( 'NONE', #2527, #2721, #11289 ) ;
#12655=ORIENTED_EDGE ( 'NONE', *, *, #1925, .T. ) ;
#12656=ORIENTED_EDGE ( 'NONE', *, *, #16442, .T. ) ;
#12659=CIRCLE ( 'NONE', #11130, 24.00000000002399858 ) ;
#12660=CIRCLE ( 'NONE', #18133, 56.24900000005625600 ) ;
#12661=CIRCLE ( 'NONE', #16312, 63.00000000006298961 ) ;
#12662=ADVANCED_FACE ( 'NONE', ( #10949 ), #6483, .T. ) ;
#12666=ORIENTED_EDGE ( 'NONE', *, *, #18788, .F. ) ;
#12667=DIRECTION ( 'NONE',  ( -1.000000000000000000, 0.000000000000000000, -0.000000000000000000 ) ) ;
#12670=DIRECTION ( 'NONE',  ( 0.000000000000000000, 0.1564344650402244297, 0.9876883405951387696 ) ) ;
#12673=DIRECTION ( 'NONE',  ( 1.000000000000000000, -0.000000000000000000, 0.000000000000000000 ) ) ;
#12675=DIRECTION ( 'NONE',  ( -1.000000000000000000, 0.000000000000000000, -0.000000000000000000 ) ) ;
#12679=DIRECTION ( 'NONE',  ( 0.000000000000000000, -0.8910065241883626808, -0.4539904997395571296 ) ) ;
#12680=CIRCLE ( 'NONE', #13290, 24.00000000002399858 ) ;
#12681=AXIS2_PLACEMENT_3D ( 'NONE', #14284, #8467, #7214 ) ;
#12684=VERTEX_POINT ( 'NONE', #10850 ) ;
#12686=AXIS2_PLACEMENT_3D ( 'NONE', #15435, #8201, #4951 ) ;
#12690=DIRECTION ( 'NONE',  ( -1.000000000000000000, -0.000000000000000000, 0.000000000000000000 ) ) ;
#12691=VECTOR ( 'NONE', #15134, 1000.000000000000000 ) ;
#12693=DIRECTION ( 'NONE',  ( 0.000000000000000000, 0.000000000000000000, 1.000000000000000000 ) ) ;
#12706=ORIENTED_EDGE ( 'NONE', *, *, #16565, .F. ) ;
#12707=DIRECTION ( 'NONE',  ( 0.000000000000000000, 0.000000000000000000, -1.000000000000000000 ) ) ;
#12710=VERTEX_POINT ( 'NONE', #3727 ) ;
#12712=AXIS2_PLACEMENT_3D ( 'NONE', #6886, #2314, #2509 ) ;
#12714=CARTESIAN_POINT ( 'NONE',  ( 0.000000000000000000, 0.000000000000000000, 0.000000000000000000 ) ) ;
#12716=FACE_OUTER_BOUND ( 'NONE', #2459, .T. ) ;
#12720=VERTEX_POINT ( 'NONE', #483 ) ;
#12722=EDGE_CURVE ( 'NONE', #9305, #16545, #3637, .T. ) ;
#12724=FACE_OUTER_BOUND ( 'NONE', #11067, .T. ) ;
#12725=DIRECTION ( 'NONE',  ( -1.000000000000000000, 0.000000000000000000, 0.000000000000000000 ) ) ;
#12727=ORIENTED_EDGE ( 'NONE', *, *, #18358, .T. ) ;
#12728=ORIENTED_EDGE ( 'NONE', *, *, #4811, .F. ) ;
#12735=EDGE_CURVE ( 'NONE', #9197, #1805, #6579, .T. ) ;
#12738=CARTESIAN_POINT ( 'NONE',  ( 5.000000000000000000, 4.007856633823394077, 62.87238730325622527 ) ) ;
#12739=EDGE_CURVE ( 'NONE', #7605, #16334, #4142, .T. ) ;
#12741=DIRECTION ( 'NONE',  ( -1.000000000000000000, 0.000000000000000000, 0.000000000000000000 ) ) ;
#12745=DIRECTION ( 'NONE',  ( 0.000000000000000000, 0.000000000000000000, 1.000000000000000000 ) ) ;
#12748=ORIENTED_EDGE ( 'NONE', *, *, #5431, .T. ) ;
#12751=ORIENTED_EDGE ( 'NONE', *, *, #18201, .T. ) ;
#12753=DIRECTION ( 'NONE',  ( -1.000000000000000000, 0.000000000000000000, 0.000000000000000000 ) ) ;
#12754=DIRECTION ( 'NONE',  ( -1.000000000000000000, -0.000000000000000000, 0.000000000000000000 ) ) ;
#12755=CIRCLE ( 'NONE', #5466, 63.00000000006298961 ) ;
#12757=ORIENTED_EDGE ( 'NONE', *, *, #8259, .T. ) ;
#12758=CARTESIAN_POINT ( 'NONE',  ( 10.00000000000000000, -7.813799127872885997, -55.83748330407415494 ) ) ;
#12761=ORIENTED_EDGE ( 'NONE', *, *, #18797, .F. ) ;
#12763=DIRECTION ( 'NONE',  ( 0.000000000000000000, 0.9876883405951371042, 0.1564344650402347547 ) ) ;
#12765=CIRCLE ( 'NONE', #7901, 56.24900000005626310 ) ;
#12769=CARTESIAN_POINT ( 'NONE',  ( 10.00000000000000000, -16.45250512421816680, -53.92768374110909235 ) ) ;
#12773=CARTESIAN_POINT ( 'NONE',  ( 0.000000000000000000, -4.007856633823831061, 62.87238730325619684 ) ) ;
#12776=ORIENTED_EDGE ( 'NONE', *, *, #12534, .F. ) ;
#12778=CARTESIAN_POINT ( 'NONE',  ( 10.00000000000000000, 0.000000000000000000, 0.000000000000000000 ) ) ;
#12779=DIRECTION ( 'NONE',  ( -1.000000000000000000, 0.000000000000000000, 0.000000000000000000 ) ) ;
#12780=CIRCLE ( 'NONE', #4552, 63.00000000006298961 ) ;
#12784=ORIENTED_EDGE ( 'NONE', *, *, #4160, .F. ) ;
#12785=ORIENTED_EDGE ( 'NONE', *, *, #7087, .F. ) ;
#12787=( NAMED_UNIT ( * ) SI_UNIT ( $, .STERADIAN. ) SOLID_ANGLE_UNIT ( ) );
#12792=DIRECTION ( 'NONE',  ( 0.000000000000000000, 0.000000000000000000, 1.000000000000000000 ) ) ;
#12794=DIRECTION ( 'NONE',  ( -1.000000000000000000, 0.000000000000000000, -0.000000000000000000 ) ) ;
#12795=LINE ( 'NONE', #18598, #4616 ) ;
#12796=LINE ( 'NONE', #5746, #11414 ) ;
#12799=ORIENTED_EDGE ( 'NONE', *, *, #6193, .T. ) ;
#12801=CARTESIAN_POINT ( 'NONE',  ( 0.000000000000000000, 0.000000000000000000, 0.000000000000000000 ) ) ;
#12803=ORIENTED_EDGE ( 'NONE', *, *, #291, .T. ) ;
#12804=FACE_OUTER_BOUND ( 'NONE', #11044, .T. ) ;
#12811=CARTESIAN_POINT ( 'NONE',  ( 10.00000000000000000, 53.06836994729233936, 18.64666490672390964 ) ) ;
#12814=DIRECTION ( 'NONE',  ( -1.000000000000000000, -0.000000000000000000, -0.000000000000000000 ) ) ;
#12815=ADVANCED_FACE ( 'NONE', ( #14008 ), #3816, .T. ) ;
#12818=CIRCLE ( 'NONE', #17384, 24.00000000002399503 ) ;
#12820=CARTESIAN_POINT ( 'NONE',  ( 0.000000000000000000, -26.71881558261766898, 49.49802920186213129 ) ) ;
#12821=DIRECTION ( 'NONE',  ( 0.000000000000000000, 0.000000000000000000, -1.000000000000000000 ) ) ;
#12826=ORIENTED_EDGE ( 'NONE', *, *, #3804, .T. ) ;
#12827=CARTESIAN_POINT ( 'NONE',  ( 0.000000000000000000, 57.83923611457320391, 24.97244012287522352 ) ) ;
#12829=AXIS2_PLACEMENT_3D ( 'NONE', #1292, #6124, #6213 ) ;
#12830=CYLINDRICAL_SURFACE ( 'NONE', #12955, 63.00000000006298961 ) ;
#12841=CARTESIAN_POINT ( 'NONE',  ( 0.000000000000000000, 53.89344778774834310, -16.10733642026427148 ) ) ;
#12844=ORIENTED_EDGE ( 'NONE', *, *, #1568, .F. ) ;
#12845=FACE_OUTER_BOUND ( 'NONE', #2322, .T. ) ;
#12853=DIRECTION ( 'NONE',  ( -1.000000000000000000, 0.000000000000000000, -0.000000000000000000 ) ) ;
#12854=CARTESIAN_POINT ( 'NONE',  ( 0.000000000000000000, 55.51919907100653973, 9.823366686500859757 ) ) ;
#12855=AXIS2_PLACEMENT_3D ( 'NONE', #1600, #4285, #1688 ) ;
#12860=EDGE_LOOP ( 'NONE', ( #4300, #10526 ) ) ;
#12861=EDGE_CURVE ( 'NONE', #475, #7605, #17072, .T. ) ;
#12865=CARTESIAN_POINT ( 'NONE',  ( 10.00000000000000000, -55.74967257055887870, 7.478235706488783663 ) ) ;
#12867=DIRECTION ( 'NONE',  ( -1.000000000000000000, -0.000000000000000000, -0.000000000000000000 ) ) ;
#12870=CARTESIAN_POINT ( 'NONE',  ( 10.00000000000000000, 49.49802920186223076, 26.71881558261748069 ) ) ;
#12873=ORIENTED_EDGE ( 'NONE', *, *, #7016, .F. ) ;
#12874=CARTESIAN_POINT ( 'NONE',  ( 0.000000000000000000, 0.000000000000000000, 0.000000000000000000 ) ) ;
#12878=CARTESIAN_POINT ( 'NONE',  ( 0.000000000000000000, 15.61693798565582547, -61.03368945066419826 ) ) ;
#12886=DIRECTION ( 'NONE',  ( 0.000000000000000000, -1.000000000000000000, -1.040834085585043434E-14 ) ) ;
#12888=CYLINDRICAL_SURFACE ( 'NONE', #18522, 24.00000000002400213 ) ;
#12889=EDGE_CURVE ( 'NONE', #5885, #3893, #6964, .T. ) ;
#12890=FACE_OUTER_BOUND ( 'NONE', #376, .T. ) ;
#12896=ORIENTED_EDGE ( 'NONE', *, *, #4709, .F. ) ;
#12902=DIRECTION ( 'NONE',  ( 0.000000000000000000, 0.4539904997395476927, -0.8910065241883673437 ) ) ;
#12904=DIRECTION ( 'NONE',  ( 0.000000000000000000, 0.4539904997395479147, -0.8910065241883673437 ) ) ;
#12905=CARTESIAN_POINT ( 'NONE',  ( 5.000000000000000000, 32.11449294037196722, 54.20017844242522642 ) ) ;
#12914=ORIENTED_EDGE ( 'NONE', *, *, #15541, .T. ) ;
#12933=DIRECTION ( 'NONE',  ( -1.000000000000000000, 0.000000000000000000, 0.000000000000000000 ) ) ;
#12934=DIRECTION ( 'NONE',  ( -1.000000000000000000, 0.000000000000000000, 0.000000000000000000 ) ) ;
#12935=ORIENTED_EDGE ( 'NONE', *, *, #1109, .F. ) ;
#12939=FACE_OUTER_BOUND ( 'NONE', #3990, .T. ) ;
#12941=PRODUCT_DEFINITION_FORMATION_WITH_SPECIFIED_SOURCE ( 'ANY', '', #9207, .NOT_KNOWN. ) ;
#12950=CARTESIAN_POINT ( 'NONE',  ( 10.00000000000000000, 47.29147401531953676, 41.62350880771938222 ) ) ;
#12953=LINE ( 'NONE', #188, #15162 ) ;
#12954=LINE ( 'NONE', #4562, #4032 ) ;
#12955=AXIS2_PLACEMENT_3D ( 'NONE', #7381, #14530, #5864 ) ;
#12957=ORIENTED_EDGE ( 'NONE', *, *, #2555, .F. ) ;
#12963=EDGE_CURVE ( 'NONE', #4060, #4800, #9571, .T. ) ;
#12964=ORIENTED_EDGE ( 'NONE', *, *, #7382, .T. ) ;
#12967=EDGE_CURVE ( 'NONE', #8010, #8173, #5038, .T. ) ;
#12968=ORIENTED_EDGE ( 'NONE', *, *, #9189, .T. ) ;
#12970=CIRCLE ( 'NONE', #12653, 63.00000000006298961 ) ;
#12973=AXIS2_PLACEMENT_3D ( 'NONE', #11077, #16725, #16901 ) ;
#12974=AXIS2_PLACEMENT_3D ( 'NONE', #17792, #10559, #6554 ) ;
#12976=DIRECTION ( 'NONE',  ( 0.000000000000000000, 0.000000000000000000, -1.000000000000000000 ) ) ;
#12977=CARTESIAN_POINT ( 'NONE',  ( 0.000000000000000000, 33.95787273855245303, 45.00825343885033192 ) ) ;
#12981=DIRECTION ( 'NONE',  ( -1.000000000000000000, 0.000000000000000000, -0.000000000000000000 ) ) ;
#12983=LINE ( 'NONE', #1275, #9160 ) ;
#12984=AXIS2_PLACEMENT_3D ( 'NONE', #13839, #10785, #12313 ) ;
#12985=DIRECTION ( 'NONE',  ( 1.000000000000000000, -0.000000000000000000, -0.000000000000000000 ) ) ;
#12986=ORIENTED_EDGE ( 'NONE', *, *, #3841, .F. ) ;
#12990=EDGE_CURVE ( 'NONE', #17686, #16356, #5950, .T. ) ;
#12992=DIRECTION ( 'NONE',  ( -1.000000000000000000, -0.000000000000000000, 0.000000000000000000 ) ) ;
#12994=ORIENTED_EDGE ( 'NONE', *, *, #740, .F. ) ;
#12998=AXIS2_PLACEMENT_3D ( 'NONE', #11620, #7324, #17516 ) ;
#13003=CARTESIAN_POINT ( 'NONE',  ( 0.000000000000000000, 53.29895248911700634, -18.38754094778185788 ) ) ;
#13004=DIRECTION ( 'NONE',  ( 0.000000000000000000, 0.000000000000000000, 1.000000000000000000 ) ) ;
#13007=CARTESIAN_POINT ( 'NONE',  ( 0.000000000000000000, -18.64666490672410148, 53.06836994729227541 ) ) ;
#13015=ORIENTED_EDGE ( 'NONE', *, *, #16389, .T. ) ;
#13016=CIRCLE ( 'NONE', #13323, 56.24900000005626310 ) ;
#13020=LINE ( 'NONE', #15789, #3887 ) ;
#13021=ORIENTED_EDGE ( 'NONE', *, *, #15860, .T. ) ;
#13023=VECTOR ( 'NONE', #3930, 1000.000000000000000 ) ;
#13024=CIRCLE ( 'NONE', #3910, 63.00000000006298961 ) ;
#13029=ORIENTED_EDGE ( 'NONE', *, *, #8474, .T. ) ;
#13033=VERTEX_POINT ( 'NONE', #4473 ) ;
#13034=ORIENTED_EDGE ( 'NONE', *, *, #9776, .T. ) ;
#13035=DIRECTION ( 'NONE',  ( -1.000000000000000000, -0.000000000000000000, 0.000000000000000000 ) ) ;
#13037=( NAMED_UNIT ( * ) SI_UNIT ( $, .STERADIAN. ) SOLID_ANGLE_UNIT ( ) );
#13040=CIRCLE ( 'NONE', #3602, 24.00000000002400569 ) ;
#13041=CIRCLE ( 'NONE', #16984, 24.00000000002400569 ) ;
#13049=DIRECTION ( 'NONE',  ( 0.000000000000000000, 0.000000000000000000, 1.000000000000000000 ) ) ;
#13052=DIRECTION ( 'NONE',  ( 0.000000000000000000, 0.8090169943749486725, -0.5877852522924714718 ) ) ;
#13057=LINE ( 'NONE', #13337, #8996 ) ;
#13059=DIRECTION ( 'NONE',  ( 0.000000000000000000, 0.000000000000000000, 1.000000000000000000 ) ) ;
#13065=AXIS2_PLACEMENT_3D ( 'NONE', #6768, #5148, #680 ) ;
#13066=AXIS2_PLACEMENT_3D ( 'NONE', #10444, #14550, #14733 ) ;
#13067=EDGE_CURVE ( 'NONE', #16371, #4390, #13057, .T. ) ;
#13068=ORIENTED_EDGE ( 'NONE', *, *, #11101, .T. ) ;
#13074=DIRECTION ( 'NONE',  ( -1.000000000000000000, 0.000000000000000000, 0.000000000000000000 ) ) ;
#13078=CARTESIAN_POINT ( 'NONE',  ( 10.00000000000000000, -55.33199130079790962, 10.11537145609357502 ) ) ;
#13079=DIRECTION ( 'NONE',  ( 1.000000000000000000, 0.000000000000000000, 0.000000000000000000 ) ) ;
#13082=ORIENTED_EDGE ( 'NONE', *, *, #3655, .T. ) ;
#13086=DIRECTION ( 'NONE',  ( 0.000000000000000000, 0.000000000000000000, 1.000000000000000000 ) ) ;
#13089=ORIENTED_EDGE ( 'NONE', *, *, #5110, .T. ) ;
#13090=EDGE_CURVE ( 'NONE', #15420, #9197, #810, .T. ) ;
#13091=CIRCLE ( 'NONE', #929, 63.00000000006298961 ) ;
#13099=DIRECTION ( 'NONE',  ( 1.000000000000000000, 0.000000000000000000, 0.000000000000000000 ) ) ;
#13100=DIRECTION ( 'NONE',  ( 0.000000000000000000, 0.000000000000000000, 1.000000000000000000 ) ) ;
#13101=EDGE_CURVE ( 'NONE', #10254, #3708, #7789, .T. ) ;
#13106=CARTESIAN_POINT ( 'NONE',  ( 5.000000000000000000, 47.29147401531955097, 41.62350880771938222 ) ) ;
#13108=EDGE_LOOP ( 'NONE', ( #15791, #1795, #14635, #5469 ) ) ;
#13115=DIRECTION ( 'NONE',  ( -1.000000000000000000, -0.000000000000000000, -0.000000000000000000 ) ) ;
#13119=VECTOR ( 'NONE', #6001, 1000.000000000000000 ) ;
#13122=VERTEX_POINT ( 'NONE', #4747 ) ;
#13123=EDGE_CURVE ( 'NONE', #5795, #4060, #13618, .T. ) ;
#13125=DIRECTION ( 'NONE',  ( 0.000000000000000000, 0.000000000000000000, -1.000000000000000000 ) ) ;
#13131=VERTEX_POINT ( 'NONE', #13796 ) ;
#13134=VECTOR ( 'NONE', #9925, 1000.000000000000000 ) ;
#13137=VERTEX_POINT ( 'NONE', #13516 ) ;
#13138=ORIENTED_EDGE ( 'NONE', *, *, #15543, .T. ) ;
#13150=DIRECTION ( 'NONE',  ( -1.000000000000000000, 0.000000000000000000, 0.000000000000000000 ) ) ;
#13160=CARTESIAN_POINT ( 'NONE',  ( 0.000000000000000000, 0.000000000000000000, 0.000000000000000000 ) ) ;
#13161=EDGE_LOOP ( 'NONE', ( #12666, #9735, #16716, #8468 ) ) ;
#13164=CYLINDRICAL_SURFACE ( 'NONE', #9659, 63.00000000006298961 ) ;
#13165=DIRECTION ( 'NONE',  ( -1.000000000000000000, 0.000000000000000000, -0.000000000000000000 ) ) ;
#13166=CARTESIAN_POINT ( 'NONE',  ( 10.00000000000000000, 0.000000000000000000, 0.000000000000000000 ) ) ;
#13169=EDGE_LOOP ( 'NONE', ( #1601, #13223, #10114, #1459, #5824, #16737, #1780, #9285, #692, #855, #13387, #2236, #14070, #3638, #12873, #4589, #4262, #3796, #13636, #5244, #150, #12784, #11493, #709, #17507, #17321, #10767, #17492, #4684, #17595, #15413, #2094, #11311, #17797, #14907, #1485, #13982, #8080, #16003, #11149, #15725, #11916, #10851, #5816, #14537, #7898, #11446, #4723, #15859, #13762, #8670, #16983, #14340, #13589, #14872, #12728, #6846, #13545, #8107, #18495, #17118, #11215, #5889, #10616, #18733, #13613, #14485, #9374, #13831, #12935, #11688, #1526, #7335, #14002, #15127, #11066, #16507, #14396, #17334, #16709, #8177, #15014, #8281, #10054, #11850, #370, #9367, #97, #1194, #3981, #8138, #9752, #1614, #18386, #11500, #1114, #18048, #6752, #7075, #16348, #10835, #17309, #11605, #15963, #15891, #5423, #4545, #15617, #9144, #4332, #12577, #7983, #6326, #3866, #10259, #12280, #6848, #5284, #14937, #8581, #17082, #13758, #14920, #9863, #13187, #15223, #10555, #9673, #5603, #17594, #5510, #12201, #2204, #670, #18398, #2506, #2444, #16381, #15301, #17544, #4339, #2234, #12896, #15802, #7407, #171, #10999, #16797, #13399, #10396, #15715, #17402, #10320, #16481, #14081, #2920, #1844, #9424, #14835, #17677, #7790, #2113, #3164, #11300, #1977 ) ) ;
#13171=DIRECTION ( 'NONE',  ( -1.000000000000000000, 0.000000000000000000, 0.000000000000000000 ) ) ;
#13172=DIRECTION ( 'NONE',  ( 0.000000000000000000, 0.3090169943749480619, -0.9510565162951533091 ) ) ;
#13177=AXIS2_PLACEMENT_3D ( 'NONE', #14016, #975, #12679 ) ;
#13178=DIRECTION ( 'NONE',  ( 0.000000000000000000, 0.9876883405951383255, -0.1564344650402276493 ) ) ;
#13180=EDGE_CURVE ( 'NONE', #18103, #2724, #6843, .T. ) ;
#13182=CARTESIAN_POINT ( 'NONE',  ( 10.00000000000000000, 0.000000000000000000, 0.000000000000000000 ) ) ;
#13183=CIRCLE ( 'NONE', #7703, 56.24900000005625600 ) ;
#13185=DIRECTION ( 'NONE',  ( -1.000000000000000000, 0.000000000000000000, 0.000000000000000000 ) ) ;
#13187=ORIENTED_EDGE ( 'NONE', *, *, #11819, .F. ) ;
#13193=ADVANCED_FACE ( 'NONE', ( #9097 ), #10521, .T. ) ;
#13194=EDGE_CURVE ( 'NONE', #13575, #3711, #247, .T. ) ;
#13197=EDGE_LOOP ( 'NONE', ( #8345, #15361, #8011, #6294 ) ) ;
#13202=CARTESIAN_POINT ( 'NONE',  ( 10.00000000000000000, 55.83748330407408389, -7.813799127873475747 ) ) ;
#13215=ADVANCED_FACE ( 'NONE', ( #16342 ), #1493, .T. ) ;
#13216=CARTESIAN_POINT ( 'NONE',  ( 0.000000000000000000, -1.335003989222025123, 56.23315539212689629 ) ) ;
#13217=( NAMED_UNIT ( * ) PLANE_ANGLE_UNIT ( ) SI_UNIT ( $, .RADIAN. ) );
#13218=ORIENTED_EDGE ( 'NONE', *, *, #9578, .T. ) ;
#13219=CARTESIAN_POINT ( 'NONE',  ( 10.00000000000000000, 0.000000000000000000, 0.000000000000000000 ) ) ;
#13223=ORIENTED_EDGE ( 'NONE', *, *, #13687, .F. ) ;
#13224=ORIENTED_EDGE ( 'NONE', *, *, #6313, .T. ) ;
#13227=CARTESIAN_POINT ( 'NONE',  ( 0.000000000000000000, 0.000000000000000000, 0.000000000000000000 ) ) ;
#13228=ORIENTED_EDGE ( 'NONE', *, *, #12861, .F. ) ;
#13229=DIRECTION ( 'NONE',  ( 1.000000000000000000, 0.000000000000000000, 0.000000000000000000 ) ) ;
#13231=CYLINDRICAL_SURFACE ( 'NONE', #2810, 56.24900000005625600 ) ;
#13235=CARTESIAN_POINT ( 'NONE',  ( 0.000000000000000000, 0.000000000000000000, 0.000000000000000000 ) ) ;
#13242=EDGE_CURVE ( 'NONE', #12431, #11050, #6240, .T. ) ;
#13244=DIRECTION ( 'NONE',  ( -1.000000000000000000, 0.000000000000000000, -0.000000000000000000 ) ) ;
#13245=CARTESIAN_POINT ( 'NONE',  ( 10.00000000000000000, -24.33982105418865061, -50.71018745830470920 ) ) ;
#13246=AXIS2_PLACEMENT_3D ( 'NONE', #7472, #13295, #10519 ) ;
#13251=DIRECTION ( 'NONE',  ( -1.000000000000000000, -0.000000000000000000, -0.000000000000000000 ) ) ;
#13260=EDGE_LOOP ( 'NONE', ( #4942, #10993, #16263, #2361 ) ) ;
#13265=CIRCLE ( 'NONE', #8112, 56.24900000005625600 ) ;
#13266=AXIS2_PLACEMENT_3D ( 'NONE', #14854, #369, #4381 ) ;
#13268=CARTESIAN_POINT ( 'NONE',  ( 0.000000000000000000, 50.69000562871642046, 24.68609584167177218 ) ) ;
#13283=DIRECTION ( 'NONE',  ( 0.000000000000000000, 0.4539904997395412534, 0.8910065241883705633 ) ) ;
#13284=VERTEX_POINT ( 'NONE', #5865 ) ;
#13287=CARTESIAN_POINT ( 'NONE',  ( 4.999999999999999112, -24.97244012287460535, -57.83923611457346681 ) ) ;
#13290=AXIS2_PLACEMENT_3D ( 'NONE', #15030, #9025, #182 ) ;
#13291=VECTOR ( 'NONE', #7034, 1000.000000000000000 ) ;
#13294=AXIS2_PLACEMENT_3D ( 'NONE', #18520, #14233, #12902 ) ;
#13295=DIRECTION ( 'NONE',  ( -1.000000000000000000, -0.000000000000000000, 0.000000000000000000 ) ) ;
#13304=DIRECTION ( 'NONE',  ( -1.000000000000000000, 0.000000000000000000, -0.000000000000000000 ) ) ;
#13311=EDGE_LOOP ( 'NONE', ( #11279, #16599, #5548, #7841 ) ) ;
#13313=CIRCLE ( 'NONE', #17561, 63.00000000006298961 ) ;
#13316=ORIENTED_EDGE ( 'NONE', *, *, #17653, .T. ) ;
#13317=CYLINDRICAL_SURFACE ( 'NONE', #282, 56.24900000005625600 ) ;
#13320=AXIS2_PLACEMENT_3D ( 'NONE', #3472, #16515, #9175 ) ;
#13322=CIRCLE ( 'NONE', #15761, 24.00000000002399858 ) ;
#13323=AXIS2_PLACEMENT_3D ( 'NONE', #18395, #12794, #5256 ) ;
#13326=EDGE_CURVE ( 'NONE', #11258, #11551, #10488, .T. ) ;
#13327=ORIENTED_EDGE ( 'NONE', *, *, #11451, .T. ) ;
#13328=CARTESIAN_POINT ( 'NONE',  ( 10.00000000000000000, 0.000000000000000000, 0.000000000000000000 ) ) ;
#13330=CARTESIAN_POINT ( 'NONE',  ( -10.00000000000000000, 42.79754323328179311, -16.55576474687299537 ) ) ;
#13333=EDGE_CURVE ( 'NONE', #5713, #5418, #6232, .T. ) ;
#13337=CARTESIAN_POINT ( 'NONE',  ( 5.000000000000000000, 33.71303790549275448, 53.22058882792209289 ) ) ;
#13342=AXIS2_PLACEMENT_3D ( 'NONE', #11274, #14499, #13172 ) ;
#13346=CIRCLE ( 'NONE', #13952, 56.24900000005625600 ) ;
#13349=CIRCLE ( 'NONE', #2706, 24.00000000002399858 ) ;
#13361=DIRECTION ( 'NONE',  ( 0.000000000000000000, 0.000000000000000000, 1.000000000000000000 ) ) ;
#13362=VERTEX_POINT ( 'NONE', #16366 ) ;
#13369=ORIENTED_EDGE ( 'NONE', *, *, #12534, .T. ) ;
#13371=ADVANCED_FACE ( 'NONE', ( #4925 ), #5005, .T. ) ;
#13376=DIRECTION ( 'NONE',  ( -1.000000000000000000, -0.000000000000000000, -0.000000000000000000 ) ) ;
#13379=DIRECTION ( 'NONE',  ( 1.000000000000000000, -0.000000000000000000, -0.000000000000000000 ) ) ;
#13380=CARTESIAN_POINT ( 'NONE',  ( 10.00000000000000000, 42.79754323328179311, -11.25576474687299644 ) ) ;
#13384=CYLINDRICAL_SURFACE ( 'NONE', #17819, 63.00000000006298961 ) ;
#13387=ORIENTED_EDGE ( 'NONE', *, *, #13674, .F. ) ;
#13389=CARTESIAN_POINT ( 'NONE',  ( 0.000000000000000000, -26.45033635316118747, 39.05576474687271116 ) ) ;
#13391=DIRECTION ( 'NONE',  ( -1.000000000000000000, 0.000000000000000000, -0.000000000000000000 ) ) ;
#13394=VECTOR ( 'NONE', #10134, 1000.000000000000000 ) ;
#13395=EDGE_CURVE ( 'NONE', #8897, #3688, #449, .T. ) ;
#13399=ORIENTED_EDGE ( 'NONE', *, *, #16189, .F. ) ;
#13400=DIRECTION ( 'NONE',  ( 0.000000000000000000, -0.9876883405951359940, -0.1564344650402419989 ) ) ;
#13401=EDGE_CURVE ( 'NONE', #538, #1960, #14840, .T. ) ;
#13406=AXIS2_PLACEMENT_3D ( 'NONE', #7171, #7640, #3554 ) ;
#13409=ORIENTED_EDGE ( 'NONE', *, *, #8193, .T. ) ;
#13410=ORIENTED_EDGE ( 'NONE', *, *, #10591, .T. ) ;
#13413=ORIENTED_EDGE ( 'NONE', *, *, #11346, .F. ) ;
#13414=CARTESIAN_POINT ( 'NONE',  ( 10.00000000000000000, 55.51919907100666762, -9.823366686500051514 ) ) ;
#13415=EDGE_CURVE ( 'NONE', #10818, #17139, #12066, .T. ) ;
#13417=AXIS2_PLACEMENT_3D ( 'NONE', #10113, #17714, #15922 ) ;
#13418=DIRECTION ( 'NONE',  ( -1.000000000000000000, -0.000000000000000000, -0.000000000000000000 ) ) ;
#13419=ORIENTED_EDGE ( 'NONE', *, *, #1360, .T. ) ;
#13420=EDGE_LOOP ( 'NONE', ( #10131, #12219, #10592, #3318 ) ) ;
#13423=LINE ( 'NONE', #10733, #4481 ) ;
#13424=ORIENTED_EDGE ( 'NONE', *, *, #16455, .F. ) ;
#13433=DIRECTION ( 'NONE',  ( -1.000000000000000000, -0.000000000000000000, 0.000000000000000000 ) ) ;
#13436=EDGE_CURVE ( 'NONE', #12710, #4722, #15962, .T. ) ;
#13438=EDGE_CURVE ( 'NONE', #15353, #16371, #4117, .T. ) ;
#13441=CARTESIAN_POINT ( 'NONE',  ( 0.000000000000000000, -5.120903701083534543E-13, -45.00000000000000000 ) ) ;
#13444=LINE ( 'NONE', #18193, #216 ) ;
#13451=VERTEX_POINT ( 'NONE', #6925 ) ;
#13455=CARTESIAN_POINT ( 'NONE',  ( 10.00000000000000000, 26.49895292618076326, -49.76630880786279931 ) ) ;
#13461=CIRCLE ( 'NONE', #10111, 24.00000000002399858 ) ;
#13463=EDGE_CURVE ( 'NONE', #3123, #7777, #2889, .T. ) ;
#13464=ORIENTED_EDGE ( 'NONE', *, *, #5234, .F. ) ;
#13467=DIRECTION ( 'NONE',  ( -1.000000000000000000, 0.000000000000000000, 0.000000000000000000 ) ) ;
#13469=LINE ( 'NONE', #6410, #1150 ) ;
#13471=CYLINDRICAL_SURFACE ( 'NONE', #10489, 24.00000000002400213 ) ;
#13475=DIRECTION ( 'NONE',  ( -1.000000000000000000, -0.000000000000000000, 0.000000000000000000 ) ) ;
#13477=DIRECTION ( 'NONE',  ( 0.000000000000000000, 0.000000000000000000, 1.000000000000000000 ) ) ;
#13483=CARTESIAN_POINT ( 'NONE',  ( 10.00000000000000000, 7.813799127873274131, 55.83748330407410521 ) ) ;
#13488=DIRECTION ( 'NONE',  ( 0.000000000000000000, 0.000000000000000000, 1.000000000000000000 ) ) ;
#13490=DIRECTION ( 'NONE',  ( -1.000000000000000000, -0.000000000000000000, 0.000000000000000000 ) ) ;
#13492=DIRECTION ( 'NONE',  ( -1.000000000000000000, 0.000000000000000000, 0.000000000000000000 ) ) ;
#13496=DIRECTION ( 'NONE',  ( 0.000000000000000000, 0.000000000000000000, 1.000000000000000000 ) ) ;
#13497=DIRECTION ( 'NONE',  ( -1.000000000000000000, 0.000000000000000000, 0.000000000000000000 ) ) ;
#13500=EDGE_CURVE ( 'NONE', #7210, #16278, #7747, .T. ) ;
#13504=EDGE_CURVE ( 'NONE', #6017, #17166, #15307, .T. ) ;
#13506=ORIENTED_EDGE ( 'NONE', *, *, #383, .T. ) ;
#13510=CARTESIAN_POINT ( 'NONE',  ( 10.00000000000000000, 50.71018745830478736, -24.33982105418846942 ) ) ;
#13511=DIRECTION ( 'NONE',  ( -1.000000000000000000, 0.000000000000000000, -0.000000000000000000 ) ) ;
#13515=FACE_OUTER_BOUND ( 'NONE', #15471, .T. ) ;
#13516=CARTESIAN_POINT ( 'NONE',  ( 0.000000000000000000, -5.876895005582878362, 62.72529079327805590 ) ) ;
#13518=DIRECTION ( 'NONE',  ( 0.000000000000000000, -0.9510565162951565288, 0.3090169943749382364 ) ) ;
#13520=VERTEX_POINT ( 'NONE', #6821 ) ;
#13521=CARTESIAN_POINT ( 'NONE',  ( 0.000000000000000000, -55.83748330407401284, -7.813799127873885197 ) ) ;
#13522=LINE ( 'NONE', #15044, #14395 ) ;
#13530=EDGE_CURVE ( 'NONE', #16959, #14039, #9682, .T. ) ;
#13535=VECTOR ( 'NONE', #9018, 1000.000000000000000 ) ;
#13536=CARTESIAN_POINT ( 'NONE',  ( 10.00000000000000000, 56.37237871411035428, -1.017308535511785683 ) ) ;
#13537=ORIENTED_EDGE ( 'NONE', *, *, #8130, .T. ) ;
#13542=CYLINDRICAL_SURFACE ( 'NONE', #14177, 2.649999999999999467 ) ;
#13543=ORIENTED_EDGE ( 'NONE', *, *, #3309, .T. ) ;
#13545=ORIENTED_EDGE ( 'NONE', *, *, #17599, .F. ) ;
#13548=ORIENTED_EDGE ( 'NONE', *, *, #15764, .F. ) ;
#13550=CIRCLE ( 'NONE', #13246, 56.24900000005625600 ) ;
#13554=DIRECTION ( 'NONE',  ( -1.000000000000000000, 0.000000000000000000, 0.000000000000000000 ) ) ;
#13555=DIRECTION ( 'NONE',  ( 0.000000000000000000, 0.000000000000000000, 1.000000000000000000 ) ) ;
#13560=CIRCLE ( 'NONE', #6565, 24.00000000002399858 ) ;
#13561=DIRECTION ( 'NONE',  ( -1.000000000000000000, 0.000000000000000000, 0.000000000000000000 ) ) ;
#13564=ORIENTED_EDGE ( 'NONE', *, *, #2646, .F. ) ;
#13565=CARTESIAN_POINT ( 'NONE',  ( 0.000000000000000000, 0.000000000000000000, 0.000000000000000000 ) ) ;
#13568=VECTOR ( 'NONE', #4409, 1000.000000000000000 ) ;
#13571=ADVANCED_FACE ( 'NONE', ( #14430 ), #12830, .T. ) ;
#13574=DIRECTION ( 'NONE',  ( 0.000000000000000000, 0.9876883405951371042, 0.1564344650402347547 ) ) ;
#13575=VERTEX_POINT ( 'NONE', #4431 ) ;
#13580=FACE_OUTER_BOUND ( 'NONE', #14269, .T. ) ;
#13586=DIRECTION ( 'NONE',  ( 0.000000000000000000, 0.000000000000000000, 1.000000000000000000 ) ) ;
#13588=LINE ( 'NONE', #10530, #17002 ) ;
#13589=ORIENTED_EDGE ( 'NONE', *, *, #1066, .F. ) ;
#13591=CARTESIAN_POINT ( 'NONE',  ( 0.000000000000000000, -26.45033635316118747, 36.40576474687271258 ) ) ;
#13595=EDGE_CURVE ( 'NONE', #478, #11596, #7197, .T. ) ;
#13596=FACE_OUTER_BOUND ( 'NONE', #452, .T. ) ;
#13597=CIRCLE ( 'NONE', #9022, 56.24900000005625600 ) ;
#13601=CIRCLE ( 'NONE', #5073, 24.00000000002399858 ) ;
#13610=VECTOR ( 'NONE', #3464, 1000.000000000000000 ) ;
#13612=DIRECTION ( 'NONE',  ( 0.000000000000000000, -0.9876883405951358830, -0.1564344650402420822 ) ) ;
#13613=ORIENTED_EDGE ( 'NONE', *, *, #10454, .F. ) ;
#13618=LINE ( 'NONE', #9311, #11996 ) ;
#13622=FACE_OUTER_BOUND ( 'NONE', #10298, .T. ) ;
#13624=AXIS2_PLACEMENT_3D ( 'NONE', #17786, #4738, #10554 ) ;
#13625=AXIS2_PLACEMENT_3D ( 'NONE', #8976, #7844, #13666 ) ;
#13628=ORIENTED_EDGE ( 'NONE', *, *, #14720, .T. ) ;
#13629=AXIS2_PLACEMENT_3D ( 'NONE', #18424, #5283, #13964 ) ;
#13632=VECTOR ( 'NONE', #15253, 1000.000000000000000 ) ;
#13636=ORIENTED_EDGE ( 'NONE', *, *, #10063, .F. ) ;
#13638=FACE_OUTER_BOUND ( 'NONE', #3512, .T. ) ;
#13641=EDGE_LOOP ( 'NONE', ( #6081, #11874, #2780, #17868 ) ) ;
#13646=EDGE_CURVE ( 'NONE', #11202, #3100, #4730, .T. ) ;
#13651=DIRECTION ( 'NONE',  ( 0.000000000000000000, 0.000000000000000000, 1.000000000000000000 ) ) ;
#13653=CARTESIAN_POINT ( 'NONE',  ( 0.000000000000000000, -33.71303790549234947, -53.22058882792234158 ) ) ;
#13654=CARTESIAN_POINT ( 'NONE',  ( 5.000000000000000000, 53.22058882792246237, -33.71303790549217183 ) ) ;
#13656=VECTOR ( 'NONE', #9435, 1000.000000000000000 ) ;
#13658=CARTESIAN_POINT ( 'NONE',  ( 0.000000000000000000, 55.51919907100666762, -9.823366686500051514 ) ) ;
#13663=FACE_OUTER_BOUND ( 'NONE', #1067, .T. ) ;
#13665=DIRECTION ( 'NONE',  ( 0.000000000000000000, 1.000000000000000000, 3.491481338843133355E-15 ) ) ;
#13666=DIRECTION ( 'NONE',  ( 0.000000000000000000, 0.3090169943749411785, 0.9510565162951555296 ) ) ;
#13668=ORIENTED_EDGE ( 'NONE', *, *, #10693, .T. ) ;
#13672=DIRECTION ( 'NONE',  ( -1.000000000000000000, 0.000000000000000000, -0.000000000000000000 ) ) ;
#13673=ORIENTED_EDGE ( 'NONE', *, *, #7230, .T. ) ;
#13674=EDGE_CURVE ( 'NONE', #10426, #7667, #17805, .T. ) ;
#13677=CARTESIAN_POINT ( 'NONE',  ( 0.000000000000000000, 0.000000000000000000, 0.000000000000000000 ) ) ;
#13679=DIRECTION ( 'NONE',  ( -1.000000000000000000, -0.000000000000000000, -0.000000000000000000 ) ) ;
#13680=CYLINDRICAL_SURFACE ( 'NONE', #10567, 63.00000000006298961 ) ;
#13685=CYLINDRICAL_SURFACE ( 'NONE', #9066, 63.00000000006298961 ) ;
#13687=EDGE_CURVE ( 'NONE', #4094, #13520, #14467, .T. ) ;
#13689=CARTESIAN_POINT ( 'NONE',  ( -10.00000000000000000, 0.000000000000000000, 0.000000000000000000 ) ) ;
#13692=DIRECTION ( 'NONE',  ( -1.000000000000000000, 0.000000000000000000, -0.000000000000000000 ) ) ;
#13695=ORIENTED_EDGE ( 'NONE', *, *, #7945, .T. ) ;
#13700=EDGE_CURVE ( 'NONE', #7777, #451, #5938, .T. ) ;
#13705=CARTESIAN_POINT ( 'NONE',  ( 5.000000000000000000, -48.50907078259351835, -40.19788616105663692 ) ) ;
#13709=FACE_OUTER_BOUND ( 'NONE', #5158, .T. ) ;
#13713=FACE_OUTER_BOUND ( 'NONE', #7746, .T. ) ;
#13714=ORIENTED_EDGE ( 'NONE', *, *, #1469, .T. ) ;
#13715=CARTESIAN_POINT ( 'NONE',  ( 10.00000000000000000, -53.89344778774823652, 16.10733642026462675 ) ) ;
#13716=CARTESIAN_POINT ( 'NONE',  ( 10.00000000000000000, 55.51919907100666762, -9.823366686500051514 ) ) ;
#13719=ORIENTED_EDGE ( 'NONE', *, *, #6693, .F. ) ;
#13720=ORIENTED_EDGE ( 'NONE', *, *, #18022, .T. ) ;
#13725=AXIS2_PLACEMENT_3D ( 'NONE', #6431, #9383, #6720 ) ;
#13726=FACE_OUTER_BOUND ( 'NONE', #13641, .T. ) ;
#13731=LINE ( 'NONE', #16869, #13023 ) ;
#13732=ORIENTED_EDGE ( 'NONE', *, *, #16329, .T. ) ;
#13733=EDGE_CURVE ( 'NONE', #1152, #9197, #471, .T. ) ;
#13735=CIRCLE ( 'NONE', #14314, 2.649999999999999467 ) ;
#13736=ADVANCED_FACE ( 'NONE', ( #15103 ), #16526, .T. ) ;
#13737=ORIENTED_EDGE ( 'NONE', *, *, #2199, .F. ) ;
#13739=VECTOR ( 'NONE', #15351, 1000.000000000000000 ) ;
#13744=CARTESIAN_POINT ( 'NONE',  ( -10.00000000000000000, 42.79754323328179311, -11.25576474687299644 ) ) ;
#13746=FACE_OUTER_BOUND ( 'NONE', #356, .T. ) ;
#13750=FACE_OUTER_BOUND ( 'NONE', #2293, .T. ) ;
#13751=CARTESIAN_POINT ( 'NONE',  ( 10.00000000000000000, -16.10733642026522006, 53.89344778774807310 ) ) ;
#13753=VERTEX_POINT ( 'NONE', #8991 ) ;
#13758=ORIENTED_EDGE ( 'NONE', *, *, #4067, .F. ) ;
#13761=CARTESIAN_POINT ( 'NONE',  ( 0.000000000000000000, -24.97244012287543669, 57.83923611457311154 ) ) ;
#13762=ORIENTED_EDGE ( 'NONE', *, *, #7962, .F. ) ;
#13763=DIRECTION ( 'NONE',  ( -1.000000000000000000, -0.000000000000000000, -0.000000000000000000 ) ) ;
#13767=DIRECTION ( 'NONE',  ( -1.000000000000000000, -0.000000000000000000, 0.000000000000000000 ) ) ;
#13768=ORIENTED_EDGE ( 'NONE', *, *, #14064, .T. ) ;
#13770=EDGE_CURVE ( 'NONE', #6237, #10072, #175, .T. ) ;
#13771=ADVANCED_FACE ( 'NONE', ( #4814 ), #4904, .T. ) ;
#13772=CARTESIAN_POINT ( 'NONE',  ( 0.000000000000000000, -18.64666490672335186, -53.06836994729252410 ) ) ;
#13774=ORIENTED_EDGE ( 'NONE', *, *, #14142, .F. ) ;
#13775=ORIENTED_EDGE ( 'NONE', *, *, #17061, .T. ) ;
#13776=DIRECTION ( 'NONE',  ( -1.000000000000000000, 0.000000000000000000, 0.000000000000000000 ) ) ;
#13777=ADVANCED_FACE ( 'NONE', ( #10343 ), #10618, .T. ) ;
#13779=CYLINDRICAL_SURFACE ( 'NONE', #918, 63.00000000006298961 ) ;
#13782=ADVANCED_FACE ( 'NONE', ( #11952 ), #8904, .F. ) ;
#13785=ORIENTED_EDGE ( 'NONE', *, *, #1538, .T. ) ;
#13788=LINE ( 'NONE', #15313, #537 ) ;
#13792=AXIS2_PLACEMENT_3D ( 'NONE', #15267, #3953, #9651 ) ;
#13793=DIRECTION ( 'NONE',  ( -1.000000000000000000, 0.000000000000000000, -0.000000000000000000 ) ) ;
#13794=DIRECTION ( 'NONE',  ( -1.000000000000000000, -0.000000000000000000, 0.000000000000000000 ) ) ;
#13796=CARTESIAN_POINT ( 'NONE',  ( 10.00000000000000000, -57.83923611457338154, 24.97244012287480430 ) ) ;
#13799=EDGE_LOOP ( 'NONE', ( #8051, #5951, #12109, #16086 ) ) ;
#13801=DIRECTION ( 'NONE',  ( -1.000000000000000000, 0.000000000000000000, 0.000000000000000000 ) ) ;
#13802=EDGE_CURVE ( 'NONE', #12684, #11971, #16243, .T. ) ;
#13805=ORIENTED_EDGE ( 'NONE', *, *, #10156, .T. ) ;
#13807=CARTESIAN_POINT ( 'NONE',  ( 10.00000000000000000, -53.89344778774800915, -16.10733642026540480 ) ) ;
#13808=CARTESIAN_POINT ( 'NONE',  ( 0.000000000000000000, 49.49802920186223076, 26.71881558261748069 ) ) ;
#13810=FACE_OUTER_BOUND ( 'NONE', #4873, .T. ) ;
#13811=LINE ( 'NONE', #5043, #11125 ) ;
#13814=CARTESIAN_POINT ( 'NONE',  ( 0.000000000000000000, 26.45033635316149301, 39.05576474687247668 ) ) ;
#13819=ORIENTED_EDGE ( 'NONE', *, *, #2087, .T. ) ;
#13820=VERTEX_POINT ( 'NONE', #4710 ) ;
#13828=CARTESIAN_POINT ( 'NONE',  ( 10.00000000000000000, -23.24033432160398505, -58.55669782892484676 ) ) ;
#13829=LINE ( 'NONE', #9452, #13739 ) ;
#13831=ORIENTED_EDGE ( 'NONE', *, *, #4023, .F. ) ;
#13833=EDGE_LOOP ( 'NONE', ( #18166, #15955, #7764, #13714 ) ) ;
#13834=EDGE_CURVE ( 'NONE', #3113, #2015, #13550, .T. ) ;
#13835=CYLINDRICAL_SURFACE ( 'NONE', #13792, 24.00000000002400213 ) ;
#13837=ORIENTED_EDGE ( 'NONE', *, *, #7263, .T. ) ;
#13838=ORIENTED_EDGE ( 'NONE', *, *, #1664, .T. ) ;
#13839=CARTESIAN_POINT ( 'NONE',  ( -10.00000000000000000, 0.000000000000000000, 0.000000000000000000 ) ) ;
#13844=AXIS2_PLACEMENT_3D ( 'NONE', #9580, #1025, #16929 ) ;
#13848=DIRECTION ( 'NONE',  ( -1.000000000000000000, 0.000000000000000000, 0.000000000000000000 ) ) ;
#13852=VERTEX_POINT ( 'NONE', #17674 ) ;
#13853=CYLINDRICAL_SURFACE ( 'NONE', #8751, 2.649999999999999467 ) ;
#13854=AXIS2_PLACEMENT_3D ( 'NONE', #8408, #11164, #16995 ) ;
#13855=EDGE_LOOP ( 'NONE', ( #14879, #218, #1814, #8323 ) ) ;
#13857=DIRECTION ( 'NONE',  ( 0.000000000000000000, 0.000000000000000000, 1.000000000000000000 ) ) ;
#13858=CARTESIAN_POINT ( 'NONE',  ( 10.00000000000000000, -10.11537145609416122, 55.33199130079781014 ) ) ;
#13859=ORIENTED_EDGE ( 'NONE', *, *, #889, .T. ) ;
#13864=CARTESIAN_POINT ( 'NONE',  ( 10.00000000000000000, 55.51919907100653973, 9.823366686500859757 ) ) ;
#13867=AXIS2_PLACEMENT_3D ( 'NONE', #2300, #5163, #6497 ) ;
#13868=CIRCLE ( 'NONE', #2616, 63.00000000006298961 ) ;
#13873=ADVANCED_FACE ( 'NONE', ( #14915 ), #16341, .T. ) ;
#13876=DIRECTION ( 'NONE',  ( 1.000000000000000000, 0.000000000000000000, 0.000000000000000000 ) ) ;
#13882=CARTESIAN_POINT ( 'NONE',  ( 10.00000000000000000, -1.335003989222025123, 56.23315539212689629 ) ) ;
#13889=CARTESIAN_POINT ( 'NONE',  ( 0.000000000000000000, -42.79754323328189969, -16.55576474687263300 ) ) ;
#13890=CARTESIAN_POINT ( 'NONE',  ( 0.000000000000000000, 0.000000000000000000, 0.000000000000000000 ) ) ;
#13891=CIRCLE ( 'NONE', #10542, 24.00000000002400213 ) ;
#13893=VERTEX_POINT ( 'NONE', #13954 ) ;
#13895=CARTESIAN_POINT ( 'NONE',  ( 0.000000000000000000, 0.000000000000000000, 0.000000000000000000 ) ) ;
#13898=DIRECTION ( 'NONE',  ( -1.000000000000000000, 0.000000000000000000, 0.000000000000000000 ) ) ;
#13899=CARTESIAN_POINT ( 'NONE',  ( 0.000000000000000000, 57.83923611457355918, -24.97244012287440285 ) ) ;
#13901=AXIS2_PLACEMENT_3D ( 'NONE', #18372, #12281, #18282 ) ;
#13902=ADVANCED_FACE ( 'NONE', ( #919 ), #18326, .T. ) ;
#13903=AXIS2_PLACEMENT_3D ( 'NONE', #4863, #6577, #12382 ) ;
#13904=ADVANCED_FACE ( 'NONE', ( #2229 ), #8243, .T. ) ;
#13905=CIRCLE ( 'NONE', #17858, 24.00000000002399503 ) ;
#13908=EDGE_CURVE ( 'NONE', #7103, #4060, #4746, .T. ) ;
#13910=CARTESIAN_POINT ( 'NONE',  ( 10.00000000000000000, -49.49802920186242972, 26.71881558261712186 ) ) ;
#13913=EDGE_CURVE ( 'NONE', #9460, #538, #15394, .T. ) ;
#13914=CARTESIAN_POINT ( 'NONE',  ( 0.000000000000000000, 0.000000000000000000, 0.000000000000000000 ) ) ;
#13916=CIRCLE ( 'NONE', #12088, 24.00000000002400213 ) ;
#13920=VECTOR ( 'NONE', #6372, 1000.000000000000000 ) ;
#13923=CIRCLE ( 'NONE', #15129, 24.00000000002399858 ) ;
#13928=VERTEX_POINT ( 'NONE', #3857 ) ;
#13931=CARTESIAN_POINT ( 'NONE',  ( 10.00000000000000000, -40.58063702438372644, 39.14194549634347453 ) ) ;
#13932=AXIS2_PLACEMENT_3D ( 'NONE', #10409, #2025, #14695 ) ;
#13936=DIRECTION ( 'NONE',  ( -1.000000000000000000, -0.000000000000000000, -0.000000000000000000 ) ) ;
#13942=EDGE_LOOP ( 'NONE', ( #5910, #7491, #7820, #2492 ) ) ;
#13945=ORIENTED_EDGE ( 'NONE', *, *, #13500, .T. ) ;
#13946=ORIENTED_EDGE ( 'NONE', *, *, #4807, .F. ) ;
#13952=AXIS2_PLACEMENT_3D ( 'NONE', #6784, #5461, #3557 ) ;
#13954=CARTESIAN_POINT ( 'NONE',  ( 10.00000000000000000, 40.70683587898012235, -38.81885513159945589 ) ) ;
#13956=FACE_OUTER_BOUND ( 'NONE', #17025, .T. ) ;
#13964=DIRECTION ( 'NONE',  ( 0.000000000000000000, 0.000000000000000000, 1.000000000000000000 ) ) ;
#13966=DIRECTION ( 'NONE',  ( 1.000000000000000000, -0.000000000000000000, -0.000000000000000000 ) ) ;
#13968=LINE ( 'NONE', #13858, #2741 ) ;
#13971=DIRECTION ( 'NONE',  ( -1.000000000000000000, -0.000000000000000000, 0.000000000000000000 ) ) ;
#13974=DIRECTION ( 'NONE',  ( 0.000000000000000000, 0.000000000000000000, 1.000000000000000000 ) ) ;
#13975=EDGE_CURVE ( 'NONE', #1379, #8411, #11124, .T. ) ;
#13982=ORIENTED_EDGE ( 'NONE', *, *, #7624, .F. ) ;
#13983=CARTESIAN_POINT ( 'NONE',  ( 0.000000000000000000, -50.71018745830461683, 24.33982105418882469 ) ) ;
#13984=CARTESIAN_POINT ( 'NONE',  ( 4.999999999999999112, 62.72529079327815538, -5.876895005581753928 ) ) ;
#13989=AXIS2_PLACEMENT_3D ( 'NONE', #13864, #12063, #10812 ) ;
#13990=CARTESIAN_POINT ( 'NONE',  ( 0.000000000000000000, 49.49802920186260735, -26.71881558261677370 ) ) ;
#13991=FACE_OUTER_BOUND ( 'NONE', #14170, .T. ) ;
#13993=ORIENTED_EDGE ( 'NONE', *, *, #1827, .T. ) ;
#13996=ORIENTED_EDGE ( 'NONE', *, *, #2849, .T. ) ;
#14002=ORIENTED_EDGE ( 'NONE', *, *, #15758, .F. ) ;
#14006=DIRECTION ( 'NONE',  ( 0.000000000000000000, 0.000000000000000000, 1.000000000000000000 ) ) ;
#14007=FACE_OUTER_BOUND ( 'NONE', #953, .T. ) ;
#14008=FACE_OUTER_BOUND ( 'NONE', #3386, .T. ) ;
#14014=EDGE_CURVE ( 'NONE', #2916, #5427, #2518, .T. ) ;
#14015=DIRECTION ( 'NONE',  ( 0.000000000000000000, -0.9876883405951393247, 0.1564344650402205439 ) ) ;
#14016=CARTESIAN_POINT ( 'NONE',  ( 10.00000000000000000, 1.017308535513159695, -56.37237871411032586 ) ) ;
#14019=EDGE_CURVE ( 'NONE', #5875, #15951, #6271, .T. ) ;
#14022=ORIENTED_EDGE ( 'NONE', *, *, #13194, .F. ) ;
#14026=CYLINDRICAL_SURFACE ( 'NONE', #9759, 24.00000000002400213 ) ;
#14030=DIRECTION ( 'NONE',  ( 0.000000000000000000, 0.000000000000000000, 1.000000000000000000 ) ) ;
#14033=EDGE_LOOP ( 'NONE', ( #14310, #4520, #3955, #13805 ) ) ;
#14034=DIRECTION ( 'NONE',  ( -1.000000000000000000, -0.000000000000000000, -0.000000000000000000 ) ) ;
#14039=VERTEX_POINT ( 'NONE', #4144 ) ;
#14040=ORIENTED_EDGE ( 'NONE', *, *, #2281, .F. ) ;
#14041=CYLINDRICAL_SURFACE ( 'NONE', #12984, 63.00000000006298961 ) ;
#14056=DIRECTION ( 'NONE',  ( -1.000000000000000000, 0.000000000000000000, 0.000000000000000000 ) ) ;
#14057=CARTESIAN_POINT ( 'NONE',  ( 10.00000000000000000, 44.70888270294211253, -34.13306034420136825 ) ) ;
#14059=ORIENTED_EDGE ( 'NONE', *, *, #15191, .T. ) ;
#14064=EDGE_CURVE ( 'NONE', #3708, #13893, #18423, .T. ) ;
#14065=AXIS2_PLACEMENT_3D ( 'NONE', #7981, #1980, #16657 ) ;
#14067=DIRECTION ( 'NONE',  ( -1.000000000000000000, -0.000000000000000000, 0.000000000000000000 ) ) ;
#14070=ORIENTED_EDGE ( 'NONE', *, *, #7382, .F. ) ;
#14074=EDGE_CURVE ( 'NONE', #7406, #13131, #13868, .T. ) ;
#14075=VERTEX_POINT ( 'NONE', #4244 ) ;
#14080=VERTEX_POINT ( 'NONE', #8795 ) ;
#14081=ORIENTED_EDGE ( 'NONE', *, *, #2620, .F. ) ;
#14083=EDGE_CURVE ( 'NONE', #18209, #9028, #10218, .T. ) ;
#14085=LINE ( 'NONE', #8370, #14285 ) ;
#14087=CARTESIAN_POINT ( 'NONE',  ( 10.00000000000000000, 38.81885513160045065, -40.70683587897917022 ) ) ;
#14091=CARTESIAN_POINT ( 'NONE',  ( 10.00000000000000000, 0.000000000000000000, 0.000000000000000000 ) ) ;
#14094=DIRECTION ( 'NONE',  ( -1.000000000000000000, -0.000000000000000000, 0.000000000000000000 ) ) ;
#14095=DIRECTION ( 'NONE',  ( 0.000000000000000000, 0.000000000000000000, 1.000000000000000000 ) ) ;
#14099=FACE_OUTER_BOUND ( 'NONE', #18295, .T. ) ;
#14101=ORIENTED_EDGE ( 'NONE', *, *, #7270, .F. ) ;
#14103=VERTEX_POINT ( 'NONE', #1373 ) ;
#14104=ORIENTED_EDGE ( 'NONE', *, *, #1925, .F. ) ;
#14106=ORIENTED_EDGE ( 'NONE', *, *, #14936, .F. ) ;
#14107=DIRECTION ( 'NONE',  ( 1.000000000000000000, 0.000000000000000000, 0.000000000000000000 ) ) ;
#14108=EDGE_CURVE ( 'NONE', #10818, #6404, #12043, .T. ) ;
#14111=DIRECTION ( 'NONE',  ( 0.000000000000000000, 0.000000000000000000, 1.000000000000000000 ) ) ;
#14122=CARTESIAN_POINT ( 'NONE',  ( 10.00000000000000000, 13.79392154159223693, -61.47135697633763129 ) ) ;
#14125=DIRECTION ( 'NONE',  ( 0.000000000000000000, 0.000000000000000000, 1.000000000000000000 ) ) ;
#14129=EDGE_CURVE ( 'NONE', #1653, #18126, #8398, .T. ) ;
#14130=STYLED_ITEM ( 'NONE', ( #14643 ), #8303 ) ;
#14132=EDGE_CURVE ( 'NONE', #15913, #9305, #12659, .T. ) ;
#14134=EDGE_CURVE ( 'NONE', #10364, #17129, #17463, .T. ) ;
#14135=DIRECTION ( 'NONE',  ( 0.000000000000000000, 0.000000000000000000, 1.000000000000000000 ) ) ;
#14141=ORIENTED_EDGE ( 'NONE', *, *, #14129, .T. ) ;
#14142=EDGE_CURVE ( 'NONE', #15913, #18678, #4150, .T. ) ;
#14144=CYLINDRICAL_SURFACE ( 'NONE', #2317, 24.00000000002399503 ) ;
#14145=DIRECTION ( 'NONE',  ( -1.000000000000000000, -0.000000000000000000, -0.000000000000000000 ) ) ;
#14146=CARTESIAN_POINT ( 'NONE',  ( 4.999999999999999112, 61.47135697633778051, 13.79392154159156370 ) ) ;
#14147=EDGE_LOOP ( 'NONE', ( #15283, #8591, #16361, #16461 ) ) ;
#14151=DIRECTION ( 'NONE',  ( 0.000000000000000000, 0.000000000000000000, 1.000000000000000000 ) ) ;
#14159=CIRCLE ( 'NONE', #1107, 24.00000000002399858 ) ;
#14161=CYLINDRICAL_SURFACE ( 'NONE', #663, 24.00000000002399503 ) ;
#14162=ORIENTED_EDGE ( 'NONE', *, *, #524, .T. ) ;
#14167=ORIENTED_EDGE ( 'NONE', *, *, #5395, .F. ) ;
#14170=EDGE_LOOP ( 'NONE', ( #18572, #15020, #8924, #14752 ) ) ;
#14177=AXIS2_PLACEMENT_3D ( 'NONE', #4872, #3450, #3258 ) ;
#14185=VECTOR ( 'NONE', #9314, 1000.000000000000000 ) ;
#14188=AXIS2_PLACEMENT_3D ( 'NONE', #14217, #6874, #12693 ) ;
#14189=VECTOR ( 'NONE', #10870, 1000.000000000000000 ) ;
#14193=DIRECTION ( 'NONE',  ( -1.000000000000000000, -0.000000000000000000, -0.000000000000000000 ) ) ;
#14195=DIRECTION ( 'NONE',  ( -1.000000000000000000, 0.000000000000000000, -0.000000000000000000 ) ) ;
#14197=DIRECTION ( 'NONE',  ( -1.000000000000000000, 0.000000000000000000, 0.000000000000000000 ) ) ;
#14198=DIRECTION ( 'NONE',  ( 0.000000000000000000, 0.000000000000000000, 1.000000000000000000 ) ) ;
#14201=CARTESIAN_POINT ( 'NONE',  ( 10.00000000000000000, 0.000000000000000000, 0.000000000000000000 ) ) ;
#14208=VECTOR ( 'NONE', #16063, 1000.000000000000000 ) ;
#14209=AXIS2_PLACEMENT_3D ( 'NONE', #9848, #17008, #11368 ) ;
#14214=CIRCLE ( 'NONE', #7810, 63.00000000006298961 ) ;
#14217=CARTESIAN_POINT ( 'NONE',  ( 10.00000000000000000, 24.68609584167230153, -50.69000562871616467 ) ) ;
#14219=DIRECTION ( 'NONE',  ( -1.000000000000000000, 0.000000000000000000, 0.000000000000000000 ) ) ;
#14221=AXIS2_PLACEMENT_3D ( 'NONE', #17863, #10706, #8995 ) ;
#14222=DIRECTION ( 'NONE',  ( -1.000000000000000000, -0.000000000000000000, -0.000000000000000000 ) ) ;
#14223=ORIENTED_EDGE ( 'NONE', *, *, #14083, .T. ) ;
#14224=VECTOR ( 'NONE', #3091, 1000.000000000000000 ) ;
#14227=DIRECTION ( 'NONE',  ( 0.000000000000000000, 0.000000000000000000, 1.000000000000000000 ) ) ;
#14229=VERTEX_POINT ( 'NONE', #14692 ) ;
#14231=DIRECTION ( 'NONE',  ( -1.000000000000000000, -0.000000000000000000, -0.000000000000000000 ) ) ;
#14233=DIRECTION ( 'NONE',  ( -1.000000000000000000, 0.000000000000000000, -0.000000000000000000 ) ) ;
#14235=ORIENTED_EDGE ( 'NONE', *, *, #15764, .T. ) ;
#14238=AXIS2_PLACEMENT_3D ( 'NONE', #9253, #11843, #15076 ) ;
#14244=EDGE_CURVE ( 'NONE', #18322, #18738, #13265, .T. ) ;
#14246=ORIENTED_EDGE ( 'NONE', *, *, #4832, .T. ) ;
#14248=DIRECTION ( 'NONE',  ( -1.000000000000000000, 0.000000000000000000, 0.000000000000000000 ) ) ;
#14249=DIRECTION ( 'NONE',  ( 0.000000000000000000, 0.000000000000000000, 1.000000000000000000 ) ) ;
#14251=VECTOR ( 'NONE', #9352, 1000.000000000000000 ) ;
#14253=EDGE_LOOP ( 'NONE', ( #13228, #8346, #897, #15199 ) ) ;
#14259=ORIENTED_EDGE ( 'NONE', *, *, #1244, .T. ) ;
#14264=CIRCLE ( 'NONE', #12433, 24.00000000002399858 ) ;
#14269=EDGE_LOOP ( 'NONE', ( #16433, #11304, #15703, #15697 ) ) ;
#14271=ADVANCED_FACE ( 'NONE', ( #4882 ), #499, .T. ) ;
#14272=ORIENTED_EDGE ( 'NONE', *, *, #6779, .F. ) ;
#14274=DIRECTION ( 'NONE',  ( 0.000000000000000000, 0.000000000000000000, 1.000000000000000000 ) ) ;
#14275=CYLINDRICAL_SURFACE ( 'NONE', #17880, 24.00000000002399858 ) ;
#14278=ORIENTED_EDGE ( 'NONE', *, *, #11237, .F. ) ;
#14279=CYLINDRICAL_SURFACE ( 'NONE', #5458, 24.00000000002400213 ) ;
#14281=ORIENTED_EDGE ( 'NONE', *, *, #17971, .T. ) ;
#14283=EDGE_CURVE ( 'NONE', #17827, #5885, #17839, .T. ) ;
#14284=CARTESIAN_POINT ( 'NONE',  ( 0.000000000000000000, -1.017308535512791767, 56.37237871411032586 ) ) ;
#14285=VECTOR ( 'NONE', #8282, 1000.000000000000000 ) ;
#14288=DIRECTION ( 'NONE',  ( 0.000000000000000000, 0.000000000000000000, -1.000000000000000000 ) ) ;
#14293=VERTEX_POINT ( 'NONE', #12587 ) ;
#14294=DIRECTION ( 'NONE',  ( 0.000000000000000000, 0.1564344650402312298, -0.9876883405951376593 ) ) ;
#14295=DIRECTION ( 'NONE',  ( -1.000000000000000000, -0.000000000000000000, 0.000000000000000000 ) ) ;
#14297=LINE ( 'NONE', #4010, #5066 ) ;
#14299=DIRECTION ( 'NONE',  ( 0.000000000000000000, -0.7071067811865389130, -0.7071067811865561215 ) ) ;
#14303=LINE ( 'NONE', #12579, #7173 ) ;
#14306=DIRECTION ( 'NONE',  ( -1.000000000000000000, -0.000000000000000000, 0.000000000000000000 ) ) ;
#14309=ADVANCED_FACE ( 'NONE', ( #16985 ), #6781, .T. ) ;
#14310=ORIENTED_EDGE ( 'NONE', *, *, #2726, .T. ) ;
#14314=AXIS2_PLACEMENT_3D ( 'NONE', #229, #4413, #411 ) ;
#14315=LINE ( 'NONE', #4035, #3010 ) ;
#14317=CARTESIAN_POINT ( 'NONE',  ( 10.00000000000000000, -34.13306034420153168, -44.70888270294199884 ) ) ;
#14323=EDGE_CURVE ( 'NONE', #872, #18209, #1418, .T. ) ;
#14324=DIRECTION ( 'NONE',  ( 0.000000000000000000, 0.000000000000000000, 1.000000000000000000 ) ) ;
#14325=DIRECTION ( 'NONE',  ( -1.000000000000000000, -0.000000000000000000, 0.000000000000000000 ) ) ;
#14327=EDGE_CURVE ( 'NONE', #17735, #8855, #18301, .T. ) ;
#14329=EDGE_LOOP ( 'NONE', ( #12256, #9169, #13029, #12153 ) ) ;
#14330=CARTESIAN_POINT ( 'NONE',  ( 0.000000000000000000, 56.37237871411034007, 1.017308535512583711 ) ) ;
#14335=ORIENTED_EDGE ( 'NONE', *, *, #7147, .T. ) ;
#14337=CYLINDRICAL_SURFACE ( 'NONE', #16601, 24.00000000002400213 ) ;
#14339=CARTESIAN_POINT ( 'NONE',  ( 0.000000000000000000, 23.24033432160521429, -58.55669782892436359 ) ) ;
#14340=ORIENTED_EDGE ( 'NONE', *, *, #4649, .F. ) ;
#14350=CARTESIAN_POINT ( 'NONE',  ( 0.000000000000000000, -7.478235706488566059, -55.74967257055892134 ) ) ;
#14351=AXIS2_PLACEMENT_3D ( 'NONE', #12504, #3657, #2213 ) ;
#14353=CIRCLE ( 'NONE', #7056, 24.00000000002399858 ) ;
#14357=DIRECTION ( 'NONE',  ( -1.000000000000000000, -0.000000000000000000, 0.000000000000000000 ) ) ;
#14358=VERTEX_POINT ( 'NONE', #11052 ) ;
#14359=EDGE_CURVE ( 'NONE', #18225, #18700, #1711, .T. ) ;
#14361=CARTESIAN_POINT ( 'NONE',  ( 10.00000000000000000, 0.000000000000000000, 0.000000000000000000 ) ) ;
#14366=AXIS2_PLACEMENT_3D ( 'NONE', #13483, #10615, #17757 ) ;
#14367=ORIENTED_EDGE ( 'NONE', *, *, #14327, .F. ) ;
#14379=DIRECTION ( 'NONE',  ( -1.000000000000000000, -0.000000000000000000, -0.000000000000000000 ) ) ;
#14380=AXIS2_PLACEMENT_3D ( 'NONE', #11224, #18362, #17224 ) ;
#14382=FACE_OUTER_BOUND ( 'NONE', #4451, .T. ) ;
#14385=ORIENTED_EDGE ( 'NONE', *, *, #3017, .F. ) ;
#14389=EDGE_CURVE ( 'NONE', #13928, #18209, #9348, .T. ) ;
#14390=ORIENTED_EDGE ( 'NONE', *, *, #8347, .T. ) ;
#14395=VECTOR ( 'NONE', #17799, 1000.000000000000000 ) ;
#14396=ORIENTED_EDGE ( 'NONE', *, *, #17614, .F. ) ;
#14398=DIRECTION ( 'NONE',  ( -1.000000000000000000, 0.000000000000000000, 0.000000000000000000 ) ) ;
#14399=VERTEX_POINT ( 'NONE', #8220 ) ;
#14401=CARTESIAN_POINT ( 'NONE',  ( 10.00000000000000000, 46.20417134726178432, -32.31183295104722220 ) ) ;
#14405=ORIENTED_EDGE ( 'NONE', *, *, #18656, .T. ) ;
#14407=ORIENTED_EDGE ( 'NONE', *, *, #12451, .T. ) ;
#14410=FACE_OUTER_BOUND ( 'NONE', #15493, .T. ) ;
#14414=AXIS2_PLACEMENT_3D ( 'NONE', #6707, #997, #12510 ) ;
#14415=EDGE_CURVE ( 'NONE', #11596, #1683, #2946, .T. ) ;
#14418=CYLINDRICAL_SURFACE ( 'NONE', #7535, 56.24900000005625600 ) ;
#14423=CARTESIAN_POINT ( 'NONE',  ( 10.00000000000000000, 0.000000000000000000, 0.000000000000000000 ) ) ;
#14425=DIRECTION ( 'NONE',  ( 0.000000000000000000, 0.4539904997395479147, -0.8910065241883673437 ) ) ;
#14430=FACE_OUTER_BOUND ( 'NONE', #5689, .T. ) ;
#14438=ORIENTED_EDGE ( 'NONE', *, *, #14389, .T. ) ;
#14439=CARTESIAN_POINT ( 'NONE',  ( 10.00000000000000000, 48.50907078259439942, -40.19788616105556400 ) ) ;
#14441=DIRECTION ( 'NONE',  ( 0.000000000000000000, 0.000000000000000000, 1.000000000000000000 ) ) ;
#14444=ORIENTED_EDGE ( 'NONE', *, *, #12963, .F. ) ;
#14445=CARTESIAN_POINT ( 'NONE',  ( 10.00000000000000000, -50.69000562871624993, -24.68609584167212745 ) ) ;
#14450=EDGE_CURVE ( 'NONE', #12264, #10921, #13891, .T. ) ;
#14451=AXIS2_PLACEMENT_3D ( 'NONE', #15140, #13115, #14815 ) ;
#14452=AXIS2_PLACEMENT_3D ( 'NONE', #13658, #5258, #2214 ) ;
#14455=ORIENTED_EDGE ( 'NONE', *, *, #4149, .T. ) ;
#14457=CIRCLE ( 'NONE', #796, 24.00000000002399148 ) ;
#14458=ORIENTED_EDGE ( 'NONE', *, *, #14589, .T. ) ;
#14461=DIRECTION ( 'NONE',  ( 0.000000000000000000, 0.000000000000000000, -1.000000000000000000 ) ) ;
#14463=DIRECTION ( 'NONE',  ( 0.000000000000000000, 0.000000000000000000, -1.000000000000000000 ) ) ;
#14466=CARTESIAN_POINT ( 'NONE',  ( 10.00000000000000000, 0.000000000000000000, 0.000000000000000000 ) ) ;
#14467=CIRCLE ( 'NONE', #10200, 56.24900000005625600 ) ;
#14476=ORIENTED_EDGE ( 'NONE', *, *, #15298, .F. ) ;
#14479=AXIS2_PLACEMENT_3D ( 'NONE', #5742, #6005, #1451 ) ;
#14481=VECTOR ( 'NONE', #5089, 1000.000000000000000 ) ;
#14484=ADVANCED_FACE ( 'NONE', ( #5634 ), #2872, .T. ) ;
#14485=ORIENTED_EDGE ( 'NONE', *, *, #3183, .F. ) ;
#14488=ORIENTED_EDGE ( 'NONE', *, *, #9183, .F. ) ;
#14491=LINE ( 'NONE', #1545, #10085 ) ;
#14495=VECTOR ( 'NONE', #14574, 1000.000000000000000 ) ;
#14499=DIRECTION ( 'NONE',  ( -1.000000000000000000, 0.000000000000000000, -0.000000000000000000 ) ) ;
#14500=ORIENTED_EDGE ( 'NONE', *, *, #14415, .F. ) ;
#14502=CIRCLE ( 'NONE', #16950, 24.00000000002400569 ) ;
#14508=AXIS2_PLACEMENT_3D ( 'NONE', #17612, #11887, #13052 ) ;
#14516=CARTESIAN_POINT ( 'NONE',  ( 0.000000000000000000, -62.87238730325618263, -4.007856633824049553 ) ) ;
#14518=LINE ( 'NONE', #4422, #2439 ) ;
#14525=ORIENTED_EDGE ( 'NONE', *, *, #17636, .T. ) ;
#14527=VECTOR ( 'NONE', #6482, 1000.000000000000000 ) ;
#14530=DIRECTION ( 'NONE',  ( -1.000000000000000000, -0.000000000000000000, -0.000000000000000000 ) ) ;
#14532=CARTESIAN_POINT ( 'NONE',  ( 10.00000000000000000, 0.000000000000000000, 0.000000000000000000 ) ) ;
#14536=AXIS2_PLACEMENT_3D ( 'NONE', #3459, #323, #18019 ) ;
#14537=ORIENTED_EDGE ( 'NONE', *, *, #10607, .F. ) ;
#14542=ORIENTED_EDGE ( 'NONE', *, *, #2828, .T. ) ;
#14543=CARTESIAN_POINT ( 'NONE',  ( 10.00000000000000000, 0.000000000000000000, 0.000000000000000000 ) ) ;
#14546=ORIENTED_EDGE ( 'NONE', *, *, #16547, .T. ) ;
#14550=DIRECTION ( 'NONE',  ( 1.000000000000000000, 0.000000000000000000, 0.000000000000000000 ) ) ;
#14554=AXIS2_PLACEMENT_3D ( 'NONE', #8118, #7924, #9637 ) ;
#14555=AXIS2_PLACEMENT_3D ( 'NONE', #11223, #13793, #755 ) ;
#14557=EDGE_LOOP ( 'NONE', ( #12004, #3455, #7741, #639 ) ) ;
#14561=DIRECTION ( 'NONE',  ( 1.000000000000000000, 0.000000000000000000, 0.000000000000000000 ) ) ;
#14566=EDGE_CURVE ( 'NONE', #8186, #3193, #5055, .T. ) ;
#14568=DIRECTION ( 'NONE',  ( 0.000000000000000000, -0.7071067811865535679, 0.7071067811865413555 ) ) ;
#14572=CIRCLE ( 'NONE', #6362, 24.00000000002399503 ) ;
#14574=DIRECTION ( 'NONE',  ( -1.000000000000000000, 0.000000000000000000, 0.000000000000000000 ) ) ;
#14582=CARTESIAN_POINT ( 'NONE',  ( 10.00000000000000000, 18.64666490672447097, -53.06836994729213330 ) ) ;
#14583=DIRECTION ( 'NONE',  ( -1.000000000000000000, 0.000000000000000000, 0.000000000000000000 ) ) ;
#14589=EDGE_CURVE ( 'NONE', #3492, #18225, #18754, .T. ) ;
#14603=ORIENTED_EDGE ( 'NONE', *, *, #9564, .T. ) ;
#14610=CARTESIAN_POINT ( 'NONE',  ( 0.000000000000000000, 53.22058882792246237, -33.71303790549217183 ) ) ;
#14612=CARTESIAN_POINT ( 'NONE',  ( 10.00000000000000000, -32.11449294037235092, 54.20017844242499905 ) ) ;
#14614=CARTESIAN_POINT ( 'NONE',  ( 0.000000000000000000, -7.478235706489372525, 55.74967257055880054 ) ) ;
#14615=ORIENTED_EDGE ( 'NONE', *, *, #14566, .T. ) ;
#14630=ORIENTED_EDGE ( 'NONE', *, *, #9888, .T. ) ;
#14631=DIRECTION ( 'NONE',  ( 1.000000000000000000, 0.000000000000000000, 0.000000000000000000 ) ) ;
#14632=CIRCLE ( 'NONE', #16149, 63.00000000006298961 ) ;
#14635=ORIENTED_EDGE ( 'NONE', *, *, #4240, .T. ) ;
#14640=ORIENTED_EDGE ( 'NONE', *, *, #2665, .F. ) ;
#14642=DIRECTION ( 'NONE',  ( -1.000000000000000000, 0.000000000000000000, -0.000000000000000000 ) ) ;
#14643=PRESENTATION_STYLE_ASSIGNMENT (( #14833 ) ) ;
#14646=CIRCLE ( 'NONE', #5523, 56.24900000005625600 ) ;
#14650=ORIENTED_EDGE ( 'NONE', *, *, #12168, .F. ) ;
#14651=EDGE_CURVE ( 'NONE', #3993, #13575, #13905, .T. ) ;
#14662=ORIENTED_EDGE ( 'NONE', *, *, #8659, .F. ) ;
#14665=EDGE_CURVE ( 'NONE', #6377, #3113, #6539, .T. ) ;
#14666=ORIENTED_EDGE ( 'NONE', *, *, #66, .F. ) ;
#14672=CARTESIAN_POINT ( 'NONE',  ( 0.000000000000000000, 55.83748330407408389, 16.18620087215052195 ) ) ;
#14677=LINE ( 'NONE', #7431, #14527 ) ;
#14682=ORIENTED_EDGE ( 'NONE', *, *, #8088, .F. ) ;
#14687=CIRCLE ( 'NONE', #11951, 63.00000000006298961 ) ;
#14688=ORIENTED_EDGE ( 'NONE', *, *, #7494, .T. ) ;
#14689=AXIS2_PLACEMENT_3D ( 'NONE', #888, #6686, #2488 ) ;
#14692=CARTESIAN_POINT ( 'NONE',  ( 0.000000000000000000, -61.03368945066424800, -15.61693798565561409 ) ) ;
#14695=DIRECTION ( 'NONE',  ( 0.000000000000000000, 0.000000000000000000, 1.000000000000000000 ) ) ;
#14696=DIRECTION ( 'NONE',  ( 0.000000000000000000, 0.000000000000000000, 1.000000000000000000 ) ) ;
#14698=CIRCLE ( 'NONE', #8009, 24.00000000002399858 ) ;
#14700=DIRECTION ( 'NONE',  ( -1.000000000000000000, -0.000000000000000000, -0.000000000000000000 ) ) ;
#14705=DIRECTION ( 'NONE',  ( 0.000000000000000000, -0.8910065241883722287, 0.4539904997395383113 ) ) ;
#14720=EDGE_CURVE ( 'NONE', #10905, #10374, #1139, .T. ) ;
#14721=ORIENTED_EDGE ( 'NONE', *, *, #4000, .T. ) ;
#14724=DIRECTION ( 'NONE',  ( -1.000000000000000000, -0.000000000000000000, -0.000000000000000000 ) ) ;
#14727=FACE_OUTER_BOUND ( 'NONE', #15811, .T. ) ;
#14730=ORIENTED_EDGE ( 'NONE', *, *, #11237, .T. ) ;
#14733=DIRECTION ( 'NONE',  ( 0.000000000000000000, 0.000000000000000000, -1.000000000000000000 ) ) ;
#14739=ORIENTED_EDGE ( 'NONE', *, *, #1231, .F. ) ;
#14740=CYLINDRICAL_SURFACE ( 'NONE', #18780, 56.24900000005625600 ) ;
#14741=CARTESIAN_POINT ( 'NONE',  ( 5.000000000000000000, 5.876895005583342879, -62.72529079327799906 ) ) ;
#14742=DIRECTION ( 'NONE',  ( -1.000000000000000000, 0.000000000000000000, 0.000000000000000000 ) ) ;
#14746=FACE_OUTER_BOUND ( 'NONE', #9653, .T. ) ;
#14748=VERTEX_POINT ( 'NONE', #115 ) ;
#14752=ORIENTED_EDGE ( 'NONE', *, *, #3683, .F. ) ;
#14754=PLANE ( 'NONE',  #711 ) ;
#14755=AXIS2_PLACEMENT_3D ( 'NONE', #2075, #12254, #7881 ) ;
#14758=EDGE_CURVE ( 'NONE', #15167, #445, #15122, .T. ) ;
#14759=AXIS2_PLACEMENT_3D ( 'NONE', #1984, #14642, #17414 ) ;
#14763=VECTOR ( 'NONE', #10919, 1000.000000000000000 ) ;
#14764=VERTEX_POINT ( 'NONE', #6734 ) ;
#14769=DIRECTION ( 'NONE',  ( -1.000000000000000000, -0.000000000000000000, 0.000000000000000000 ) ) ;
#14772=ORIENTED_EDGE ( 'NONE', *, *, #2971, .T. ) ;
#14774=ORIENTED_EDGE ( 'NONE', *, *, #4757, .F. ) ;
#14776=EDGE_CURVE ( 'NONE', #5713, #11318, #5398, .T. ) ;
#14779=CIRCLE ( 'NONE', #8417, 56.24900000005626310 ) ;
#14780=EDGE_CURVE ( 'NONE', #16544, #3711, #9949, .T. ) ;
#14783=CARTESIAN_POINT ( 'NONE',  ( -10.00000000000000000, 0.000000000000000000, 0.000000000000000000 ) ) ;
#14784=DIRECTION ( 'NONE',  ( 0.000000000000000000, 0.000000000000000000, 1.000000000000000000 ) ) ;
#14785=AXIS2_PLACEMENT_3D ( 'NONE', #5565, #14231, #12707 ) ;
#14787=DIRECTION ( 'NONE',  ( -1.000000000000000000, 0.000000000000000000, 0.000000000000000000 ) ) ;
#14790=CARTESIAN_POINT ( 'NONE',  ( 10.00000000000000000, 7.813799127873274131, 55.83748330407410521 ) ) ;
#14792=AXIS2_PLACEMENT_3D ( 'NONE', #5251, #6405, #12209 ) ;
#14797=EDGE_CURVE ( 'NONE', #4490, #11098, #3980, .T. ) ;
#14798=EDGE_CURVE ( 'NONE', #2015, #19, #1730, .T. ) ;
#14799=CARTESIAN_POINT ( 'NONE',  ( 10.00000000000000000, -48.50907078259410099, 40.19788616105592638 ) ) ;
#14800=DIRECTION ( 'NONE',  ( 0.000000000000000000, 0.000000000000000000, 1.000000000000000000 ) ) ;
#14802=ORIENTED_EDGE ( 'NONE', *, *, #4089, .T. ) ;
#14803=VERTEX_POINT ( 'NONE', #3696 ) ;
#14804=CARTESIAN_POINT ( 'NONE',  ( 10.00000000000000000, -45.00825343885045271, 33.95787273855228960 ) ) ;
#14809=AXIS2_PLACEMENT_3D ( 'NONE', #18190, #5438, #15329 ) ;
#14814=DIRECTION ( 'NONE',  ( 0.000000000000000000, 0.000000000000000000, 1.000000000000000000 ) ) ;
#14815=DIRECTION ( 'NONE',  ( 0.000000000000000000, 0.000000000000000000, 1.000000000000000000 ) ) ;
#14817=EDGE_LOOP ( 'NONE', ( #9558, #16608, #11227, #17926 ) ) ;
#14819=ORIENTED_EDGE ( 'NONE', *, *, #8423, .F. ) ;
#14820=DIRECTION ( 'NONE',  ( -1.000000000000000000, 0.000000000000000000, 0.000000000000000000 ) ) ;
#14821=EDGE_LOOP ( 'NONE', ( #908, #14438, #4939, #9044 ) ) ;
#14826=CARTESIAN_POINT ( 'NONE',  ( 10.00000000000000000, 46.20417134726178432, -32.31183295104722220 ) ) ;
#14827=DIRECTION ( 'NONE',  ( -1.000000000000000000, -0.000000000000000000, -0.000000000000000000 ) ) ;
#14833=SURFACE_STYLE_USAGE ( .BOTH. , #6068 ) ;
#14835=ORIENTED_EDGE ( 'NONE', *, *, #2252, .F. ) ;
#14840=LINE ( 'NONE', #7595, #3500 ) ;
#14842=AXIS2_PLACEMENT_3D ( 'NONE', #11266, #8227, #14030 ) ;
#14845=CARTESIAN_POINT ( 'NONE',  ( 10.00000000000000000, -5.120903701083534543E-13, -42.35000000000000142 ) ) ;
#14850=EDGE_CURVE ( 'NONE', #13753, #8186, #15592, .T. ) ;
#14852=CARTESIAN_POINT ( 'NONE',  ( 10.00000000000000000, -33.95787273855213328, -45.00825343885058061 ) ) ;
#14854=CARTESIAN_POINT ( 'NONE',  ( 0.000000000000000000, 0.000000000000000000, 0.000000000000000000 ) ) ;
#14858=AXIS2_PLACEMENT_3D ( 'NONE', #2795, #8414, #11648 ) ;
#14859=EDGE_LOOP ( 'NONE', ( #7079, #18556, #595, #11219 ) ) ;
#14860=CARTESIAN_POINT ( 'NONE',  ( 10.00000000000000000, 55.33199130079785277, 10.11537145609396404 ) ) ;
#14863=AXIS2_PLACEMENT_3D ( 'NONE', #1158, #14094, #4013 ) ;
#14872=ORIENTED_EDGE ( 'NONE', *, *, #18200, .F. ) ;
#14873=AXIS2_PLACEMENT_3D ( 'NONE', #1698, #7512, #1886 ) ;
#14879=ORIENTED_EDGE ( 'NONE', *, *, #13770, .T. ) ;
#14881=ORIENTED_EDGE ( 'NONE', *, *, #14798, .T. ) ;
#14889=EDGE_LOOP ( 'NONE', ( #6398, #6447 ) ) ;
#14890=ORIENTED_EDGE ( 'NONE', *, *, #14083, .F. ) ;
#14892=DIRECTION ( 'NONE',  ( 0.000000000000000000, 0.000000000000000000, -1.000000000000000000 ) ) ;
#14893=AXIS2_PLACEMENT_3D ( 'NONE', #4852, #12725, #12623 ) ;
#14894=DIRECTION ( 'NONE',  ( -1.000000000000000000, -0.000000000000000000, -0.000000000000000000 ) ) ;
#14898=DIRECTION ( 'NONE',  ( 0.000000000000000000, 0.000000000000000000, 1.000000000000000000 ) ) ;
#14899=CARTESIAN_POINT ( 'NONE',  ( 0.000000000000000000, -1.017308535511979972, -56.37237871411034718 ) ) ;
#14902=VERTEX_POINT ( 'NONE', #5404 ) ;
#14904=LINE ( 'NONE', #14993, #3524 ) ;
#14906=CYLINDRICAL_SURFACE ( 'NONE', #11794, 56.24900000005625600 ) ;
#14907=ORIENTED_EDGE ( 'NONE', *, *, #7494, .F. ) ;
#14915=FACE_OUTER_BOUND ( 'NONE', #9507, .T. ) ;
#14917=FACE_OUTER_BOUND ( 'NONE', #15952, .T. ) ;
#14919=CARTESIAN_POINT ( 'NONE',  ( 10.00000000000000000, -41.62350880771888484, -47.29147401531998440 ) ) ;
#14920=ORIENTED_EDGE ( 'NONE', *, *, #10755, .F. ) ;
#14923=CIRCLE ( 'NONE', #13406, 24.00000000002399858 ) ;
#14925=DIRECTION ( 'NONE',  ( 0.000000000000000000, 0.000000000000000000, 1.000000000000000000 ) ) ;
#14931=DIRECTION ( 'NONE',  ( -1.000000000000000000, 0.000000000000000000, -0.000000000000000000 ) ) ;
#14933=EDGE_CURVE ( 'NONE', #4445, #380, #3563, .T. ) ;
#14934=AXIS2_PLACEMENT_3D ( 'NONE', #13160, #10199, #16012 ) ;
#14936=EDGE_CURVE ( 'NONE', #8859, #2515, #4435, .T. ) ;
#14937=ORIENTED_EDGE ( 'NONE', *, *, #729, .F. ) ;
#14938=EDGE_CURVE ( 'NONE', #10240, #9460, #13020, .T. ) ;
#14942=FACE_OUTER_BOUND ( 'NONE', #13833, .T. ) ;
#14950=CIRCLE ( 'NONE', #3392, 24.00000000002399858 ) ;
#14951=DIRECTION ( 'NONE',  ( -1.000000000000000000, -0.000000000000000000, -0.000000000000000000 ) ) ;
#14952=EDGE_LOOP ( 'NONE', ( #12207, #12968, #6259, #3456 ) ) ;
#14959=EDGE_CURVE ( 'NONE', #6509, #11571, #4265, .T. ) ;
#14962=ORIENTED_EDGE ( 'NONE', *, *, #1661, .F. ) ;
#14969=CARTESIAN_POINT ( 'NONE',  ( 0.000000000000000000, 24.97244012287502102, 57.83923611457328207 ) ) ;
#14970=ORIENTED_EDGE ( 'NONE', *, *, #9641, .T. ) ;
#14973=AXIS2_PLACEMENT_3D ( 'NONE', #15366, #10982, #3756 ) ;
#14993=CARTESIAN_POINT ( 'NONE',  ( 10.00000000000000000, 53.89344778774812994, 16.10733642026502466 ) ) ;
#14994=CARTESIAN_POINT ( 'NONE',  ( 0.000000000000000000, 23.24033432160437584, 58.55669782892469755 ) ) ;
#15006=ADVANCED_FACE ( 'NONE', ( #5949 ), #8626, .T. ) ;
#15012=ORIENTED_EDGE ( 'NONE', *, *, #16270, .F. ) ;
#15014=ORIENTED_EDGE ( 'NONE', *, *, #8041, .F. ) ;
#15015=LINE ( 'NONE', #2060, #10589 ) ;
#15018=CYLINDRICAL_SURFACE ( 'NONE', #9826, 63.00000000006298961 ) ;
#15020=ORIENTED_EDGE ( 'NONE', *, *, #14074, .T. ) ;
#15030=CARTESIAN_POINT ( 'NONE',  ( 10.00000000000000000, -32.31183295104805353, 46.20417134726119457 ) ) ;
#15033=ORIENTED_EDGE ( 'NONE', *, *, #4668, .F. ) ;
#15036=CYLINDRICAL_SURFACE ( 'NONE', #14065, 63.00000000006298961 ) ;
#15038=ORIENTED_EDGE ( 'NONE', *, *, #9720, .T. ) ;
#15043=DIRECTION ( 'NONE',  ( 0.000000000000000000, 0.3090169943749481174, -0.9510565162951533091 ) ) ;
#15044=CARTESIAN_POINT ( 'NONE',  ( 4.999999999999999112, -62.72529079327802748, -5.876895005583096854 ) ) ;
#15049=DIRECTION ( 'NONE',  ( 0.000000000000000000, 0.000000000000000000, -1.000000000000000000 ) ) ;
#15051=ORIENTED_EDGE ( 'NONE', *, *, #12092, .T. ) ;
#15052=LINE ( 'NONE', #12192, #10610 ) ;
#15056=CARTESIAN_POINT ( 'NONE',  ( 5.000000000000000000, -58.55669782892479702, 23.24033432160415913 ) ) ;
#15059=EDGE_LOOP ( 'NONE', ( #14682, #14546, #15255, #5189 ) ) ;
#15066=ORIENTED_EDGE ( 'NONE', *, *, #7377, .F. ) ;
#15067=EDGE_CURVE ( 'NONE', #6939, #14764, #5710, .T. ) ;
#15070=AXIS2_PLACEMENT_3D ( 'NONE', #6142, #1857, #7660 ) ;
#15076=DIRECTION ( 'NONE',  ( 0.000000000000000000, 0.000000000000000000, 1.000000000000000000 ) ) ;
#15078=DIRECTION ( 'NONE',  ( 1.000000000000000000, -0.000000000000000000, 0.000000000000000000 ) ) ;
#15081=CIRCLE ( 'NONE', #11739, 24.00000000002399858 ) ;
#15084=CARTESIAN_POINT ( 'NONE',  ( 5.000000000000000000, 57.83923611457320391, 24.97244012287522352 ) ) ;
#15089=DIRECTION ( 'NONE',  ( 0.000000000000000000, 0.1564344650402312298, -0.9876883405951376593 ) ) ;
#15091=VERTEX_POINT ( 'NONE', #4906 ) ;
#15094=VECTOR ( 'NONE', #883, 1000.000000000000000 ) ;
#15095=DIRECTION ( 'NONE',  ( -1.000000000000000000, 0.000000000000000000, 0.000000000000000000 ) ) ;
#15097=CARTESIAN_POINT ( 'NONE',  ( 10.00000000000000000, 16.45250512421856470, 53.92768374110897156 ) ) ;
#15099=ADVANCED_FACE ( 'NONE', ( #16343 ), #6429, .T. ) ;
#15102=CIRCLE ( 'NONE', #2312, 24.00000000002400213 ) ;
#15103=FACE_OUTER_BOUND ( 'NONE', #14147, .T. ) ;
#15106=AXIS2_PLACEMENT_3D ( 'NONE', #14826, #4632, #16447 ) ;
#15109=DIRECTION ( 'NONE',  ( 0.000000000000000000, 0.000000000000000000, 1.000000000000000000 ) ) ;
#15110=EDGE_LOOP ( 'NONE', ( #9065, #212, #9343, #6639 ) ) ;
#15114=DIRECTION ( 'NONE',  ( -1.000000000000000000, 0.000000000000000000, -0.000000000000000000 ) ) ;
#15116=ORIENTED_EDGE ( 'NONE', *, *, #7257, .T. ) ;
#15119=AXIS2_PLACEMENT_3D ( 'NONE', #9721, #1157, #4099 ) ;
#15120=ORIENTED_EDGE ( 'NONE', *, *, #5338, .T. ) ;
#15121=FACE_OUTER_BOUND ( 'NONE', #6209, .T. ) ;
#15122=CIRCLE ( 'NONE', #12070, 24.00000000002400213 ) ;
#15124=EDGE_CURVE ( 'NONE', #3205, #980, #15447, .T. ) ;
#15126=CIRCLE ( 'NONE', #9330, 24.00000000002399858 ) ;
#15127=ORIENTED_EDGE ( 'NONE', *, *, #3460, .F. ) ;
#15128=CIRCLE ( 'NONE', #3580, 24.00000000002399858 ) ;
#15129=AXIS2_PLACEMENT_3D ( 'NONE', #3200, #10523, #4818 ) ;
#15131=DIRECTION ( 'NONE',  ( 0.000000000000000000, -6.938893903900288768E-15, 1.000000000000000000 ) ) ;
#15132=AXIS2_PLACEMENT_3D ( 'NONE', #17565, #11753, #12745 ) ;
#15134=DIRECTION ( 'NONE',  ( -1.000000000000000000, -0.000000000000000000, -0.000000000000000000 ) ) ;
#15135=ADVANCED_FACE ( 'NONE', ( #16528 ), #13680, .T. ) ;
#15137=DIRECTION ( 'NONE',  ( 0.000000000000000000, 0.000000000000000000, -1.000000000000000000 ) ) ;
#15140=CARTESIAN_POINT ( 'NONE',  ( 0.000000000000000000, 0.000000000000000000, 0.000000000000000000 ) ) ;
#15141=ORIENTED_EDGE ( 'NONE', *, *, #14665, .F. ) ;
#15150=AXIS2_PLACEMENT_3D ( 'NONE', #16487, #12195, #3353 ) ;
#15153=VERTEX_POINT ( 'NONE', #627 ) ;
#15157=CIRCLE ( 'NONE', #9067, 56.24900000005625600 ) ;
#15161=ORIENTED_EDGE ( 'NONE', *, *, #15519, .T. ) ;
#15162=VECTOR ( 'NONE', #18762, 1000.000000000000000 ) ;
#15166=CARTESIAN_POINT ( 'NONE',  ( 4.999999999999999112, -15.61693798565540270, 61.03368945066429774 ) ) ;
#15167=VERTEX_POINT ( 'NONE', #10620 ) ;
#15168=VERTEX_POINT ( 'NONE', #6342 ) ;
#15170=AXIS2_PLACEMENT_3D ( 'NONE', #7899, #9419, #5222 ) ;
#15173=EDGE_CURVE ( 'NONE', #6648, #14229, #18045, .T. ) ;
#15174=EDGE_CURVE ( 'NONE', #380, #8389, #4711, .T. ) ;
#15177=ADVANCED_FACE ( 'NONE', ( #14917 ), #3483, .F. ) ;
#15180=DIRECTION ( 'NONE',  ( 0.000000000000000000, 0.9510565162951545304, -0.3090169943749446202 ) ) ;
#15189=ORIENTED_EDGE ( 'NONE', *, *, #18202, .T. ) ;
#15191=EDGE_CURVE ( 'NONE', #5117, #7622, #13923, .T. ) ;
#15194=ORIENTED_EDGE ( 'NONE', *, *, #8212, .F. ) ;
#15195=ORIENTED_EDGE ( 'NONE', *, *, #5499, .F. ) ;
#15199=ORIENTED_EDGE ( 'NONE', *, *, #6714, .T. ) ;
#15204=CARTESIAN_POINT ( 'NONE',  ( -10.00000000000000000, 0.000000000000000000, 0.000000000000000000 ) ) ;
#15205=ORIENTED_EDGE ( 'NONE', *, *, #396, .T. ) ;
#15210=ADVANCED_FACE ( 'NONE', ( #345 ), #6144, .T. ) ;
#15212=CYLINDRICAL_SURFACE ( 'NONE', #1610, 24.00000000002400213 ) ;
#15216=VECTOR ( 'NONE', #18218, 1000.000000000000000 ) ;
#15221=AXIS2_PLACEMENT_3D ( 'NONE', #13182, #17834, #14696 ) ;
#15223=ORIENTED_EDGE ( 'NONE', *, *, #18677, .F. ) ;
#15231=LINE ( 'NONE', #18459, #268 ) ;
#15237=DIRECTION ( 'NONE',  ( -1.000000000000000000, -0.000000000000000000, 0.000000000000000000 ) ) ;
#15239=CIRCLE ( 'NONE', #1259, 24.00000000002400213 ) ;
#15243=VERTEX_POINT ( 'NONE', #13761 ) ;
#15249=DIRECTION ( 'NONE',  ( 0.000000000000000000, 0.000000000000000000, 1.000000000000000000 ) ) ;
#15253=DIRECTION ( 'NONE',  ( -1.000000000000000000, 0.000000000000000000, 0.000000000000000000 ) ) ;
#15255=ORIENTED_EDGE ( 'NONE', *, *, #12722, .F. ) ;
#15260=CARTESIAN_POINT ( 'NONE',  ( 0.000000000000000000, 0.000000000000000000, 0.000000000000000000 ) ) ;
#15263=DIRECTION ( 'NONE',  ( -1.000000000000000000, 0.000000000000000000, -0.000000000000000000 ) ) ;
#15265=CARTESIAN_POINT ( 'NONE',  ( 5.000000000000000000, -40.19788616105574164, -48.50907078259425731 ) ) ;
#15267=CARTESIAN_POINT ( 'NONE',  ( 10.00000000000000000, 45.00825343885021113, 33.95787273855260935 ) ) ;
#15272=FACE_OUTER_BOUND ( 'NONE', #4880, .T. ) ;
#15275=CYLINDRICAL_SURFACE ( 'NONE', #10198, 24.00000000002399858 ) ;
#15276=EDGE_CURVE ( 'NONE', #417, #8897, #17560, .T. ) ;
#15278=EDGE_CURVE ( 'NONE', #7239, #3393, #10859, .T. ) ;
#15283=ORIENTED_EDGE ( 'NONE', *, *, #13975, .T. ) ;
#15287=EDGE_CURVE ( 'NONE', #12513, #18363, #8338, .T. ) ;
#15289=ORIENTED_EDGE ( 'NONE', *, *, #10975, .T. ) ;
#15291=FACE_OUTER_BOUND ( 'NONE', #13855, .T. ) ;
#15292=EDGE_LOOP ( 'NONE', ( #13732, #4596, #11543, #9288 ) ) ;
#15293=DIRECTION ( 'NONE',  ( -1.000000000000000000, 0.000000000000000000, 0.000000000000000000 ) ) ;
#15294=CARTESIAN_POINT ( 'NONE',  ( 10.00000000000000000, 15.61693798565582902, -61.03368945066418405 ) ) ;
#15298=EDGE_CURVE ( 'NONE', #5739, #18350, #2613, .T. ) ;
#15299=CARTESIAN_POINT ( 'NONE',  ( 10.00000000000000000, 0.000000000000000000, 0.000000000000000000 ) ) ;
#15301=ORIENTED_EDGE ( 'NONE', *, *, #16180, .F. ) ;
#15304=ADVANCED_FACE ( 'NONE', ( #12716 ), #6518, .T. ) ;
#15305=CIRCLE ( 'NONE', #14689, 24.00000000002399858 ) ;
#15307=LINE ( 'NONE', #15591, #10790 ) ;
#15311=CARTESIAN_POINT ( 'NONE',  ( 10.00000000000000000, 0.000000000000000000, 0.000000000000000000 ) ) ;
#15312=CARTESIAN_POINT ( 'NONE',  ( 10.00000000000000000, 32.31183295104839459, -46.20417134726096009 ) ) ;
#15313=CARTESIAN_POINT ( 'NONE',  ( 10.00000000000000000, -44.70888270294135936, -34.13306034420235591 ) ) ;
#15316=ORIENTED_EDGE ( 'NONE', *, *, #8537, .F. ) ;
#15322=LINE ( 'NONE', #169, #12324 ) ;
#15325=CARTESIAN_POINT ( 'NONE',  ( 0.000000000000000000, -56.37237871411034718, 1.017308535512174261 ) ) ;
#15327=ORIENTED_EDGE ( 'NONE', *, *, #3479, .T. ) ;
#15329=DIRECTION ( 'NONE',  ( 0.000000000000000000, 0.000000000000000000, 1.000000000000000000 ) ) ;
#15333=DIRECTION ( 'NONE',  ( -1.000000000000000000, 0.000000000000000000, 0.000000000000000000 ) ) ;
#15336=DIRECTION ( 'NONE',  ( -1.000000000000000000, -0.000000000000000000, 0.000000000000000000 ) ) ;
#15338=CARTESIAN_POINT ( 'NONE',  ( 10.00000000000000000, 55.83748330407408389, 16.18620087215052195 ) ) ;
#15348=CARTESIAN_POINT ( 'NONE',  ( 10.00000000000000000, -15.61693798565540625, 61.03368945066429774 ) ) ;
#15349=LINE ( 'NONE', #13654, #10032 ) ;
#15351=DIRECTION ( 'NONE',  ( -1.000000000000000000, 0.000000000000000000, 0.000000000000000000 ) ) ;
#15352=DIRECTION ( 'NONE',  ( -1.000000000000000000, 0.000000000000000000, 0.000000000000000000 ) ) ;
#15353=VERTEX_POINT ( 'NONE', #2329 ) ;
#15355=ORIENTED_EDGE ( 'NONE', *, *, #8875, .F. ) ;
#15358=DIRECTION ( 'NONE',  ( -1.000000000000000000, 0.000000000000000000, 0.000000000000000000 ) ) ;
#15361=ORIENTED_EDGE ( 'NONE', *, *, #10266, .T. ) ;
#15366=CARTESIAN_POINT ( 'NONE',  ( 0.000000000000000000, 24.68609584167230153, -50.69000562871616467 ) ) ;
#15370=CARTESIAN_POINT ( 'NONE',  ( 10.00000000000000000, 32.31183295104772668, 46.20417134726143615 ) ) ;
#15374=ORIENTED_EDGE ( 'NONE', *, *, #7805, .T. ) ;
#15376=ADVANCED_FACE ( 'NONE', ( #13956 ), #18329, .F. ) ;
#15381=EDGE_LOOP ( 'NONE', ( #3768, #14405, #156, #12532 ) ) ;
#15382=PRODUCT_DEFINITION ( 'UNKNOWN', '', #12941, #6933 ) ;
#15387=ORIENTED_EDGE ( 'NONE', *, *, #10342, .T. ) ;
#15391=AXIS2_PLACEMENT_3D ( 'NONE', #4636, #11876, #4920 ) ;
#15392=AXIS2_PLACEMENT_3D ( 'NONE', #12778, #4107, #7842 ) ;
#15393=AXIS2_PLACEMENT_3D ( 'NONE', #9638, #15459, #11908 ) ;
#15394=CIRCLE ( 'NONE', #3232, 63.00000000006298961 ) ;
#15401=EDGE_CURVE ( 'NONE', #18678, #4356, #9350, .T. ) ;
#15403=EDGE_CURVE ( 'NONE', #13362, #9382, #7854, .T. ) ;
#15404=EDGE_CURVE ( 'NONE', #451, #12684, #13024, .T. ) ;
#15406=ORIENTED_EDGE ( 'NONE', *, *, #18085, .T. ) ;
#15408=CYLINDRICAL_SURFACE ( 'NONE', #7437, 56.24900000005625600 ) ;
#15411=ORIENTED_EDGE ( 'NONE', *, *, #729, .T. ) ;
#15413=ORIENTED_EDGE ( 'NONE', *, *, #3309, .F. ) ;
#15417=CARTESIAN_POINT ( 'NONE',  ( 0.000000000000000000, 53.06836994729233936, 18.64666490672390964 ) ) ;
#15420=VERTEX_POINT ( 'NONE', #1561 ) ;
#15423=ORIENTED_EDGE ( 'NONE', *, *, #717, .F. ) ;
#15430=ORIENTED_EDGE ( 'NONE', *, *, #5976, .F. ) ;
#15431=EDGE_CURVE ( 'NONE', #7464, #10253, #18616, .T. ) ;
#15433=DIRECTION ( 'NONE',  ( -1.000000000000000000, 0.000000000000000000, 0.000000000000000000 ) ) ;
#15434=DIRECTION ( 'NONE',  ( 0.000000000000000000, 0.000000000000000000, 1.000000000000000000 ) ) ;
#15435=CARTESIAN_POINT ( 'NONE',  ( 10.00000000000000000, 0.000000000000000000, 0.000000000000000000 ) ) ;
#15437=LINE ( 'NONE', #12870, #16190 ) ;
#15438=CIRCLE ( 'NONE', #3870, 56.24900000005625600 ) ;
#15441=CARTESIAN_POINT ( 'NONE',  ( 10.00000000000000000, 0.000000000000000000, 0.000000000000000000 ) ) ;
#15443=CYLINDRICAL_SURFACE ( 'NONE', #5945, 56.24900000005625600 ) ;
#15445=CARTESIAN_POINT ( 'NONE',  ( 0.000000000000000000, 26.71881558261799228, -49.49802920186195365 ) ) ;
#15447=CIRCLE ( 'NONE', #14221, 56.24900000005625600 ) ;
#15452=AXIS2_PLACEMENT_3D ( 'NONE', #8272, #12353, #3701 ) ;
#15454=AXIS2_PLACEMENT_3D ( 'NONE', #18102, #18382, #14015 ) ;
#15456=CYLINDRICAL_SURFACE ( 'NONE', #17964, 24.00000000002399858 ) ;
#15457=VECTOR ( 'NONE', #15333, 1000.000000000000000 ) ;
#15459=DIRECTION ( 'NONE',  ( 1.000000000000000000, 0.000000000000000000, 0.000000000000000000 ) ) ;
#15461=CARTESIAN_POINT ( 'NONE',  ( 0.000000000000000000, 54.20017844242511273, 32.11449294037214486 ) ) ;
#15462=DIRECTION ( 'NONE',  ( -1.000000000000000000, 0.000000000000000000, 0.000000000000000000 ) ) ;
#15463=CARTESIAN_POINT ( 'NONE',  ( 10.00000000000000000, -18.38754094778278869, 53.29895248911668659 ) ) ;
#15466=ORIENTED_EDGE ( 'NONE', *, *, #5026, .T. ) ;
#15471=EDGE_LOOP ( 'NONE', ( #2526, #10650, #6247, #2215 ) ) ;
#15475=DIRECTION ( 'NONE',  ( -1.000000000000000000, -0.000000000000000000, -0.000000000000000000 ) ) ;
#15479=DIRECTION ( 'NONE',  ( 0.000000000000000000, 0.3090169943749411785, 0.9510565162951556406 ) ) ;
#15488=ORIENTED_EDGE ( 'NONE', *, *, #3198, .F. ) ;
#15490=CARTESIAN_POINT ( 'NONE',  ( 5.000000000000000000, -33.71303790549312396, 53.22058882792185841 ) ) ;
#15491=DIRECTION ( 'NONE',  ( -1.000000000000000000, -0.000000000000000000, 0.000000000000000000 ) ) ;
#15493=EDGE_LOOP ( 'NONE', ( #6653, #7783, #3619, #11548 ) ) ;
#15498=CIRCLE ( 'NONE', #7879, 2.649999999999999467 ) ;
#15499=DIRECTION ( 'NONE',  ( -1.000000000000000000, 0.000000000000000000, 0.000000000000000000 ) ) ;
#15502=LINE ( 'NONE', #1994, #5814 ) ;
#15503=AXIS2_PLACEMENT_3D ( 'NONE', #18536, #2440, #16825 ) ;
#15506=DIRECTION ( 'NONE',  ( -1.000000000000000000, -0.000000000000000000, -0.000000000000000000 ) ) ;
#15510=ORIENTED_EDGE ( 'NONE', *, *, #14134, .F. ) ;
#15515=DIRECTION ( 'NONE',  ( -1.000000000000000000, 0.000000000000000000, -0.000000000000000000 ) ) ;
#15519=EDGE_CURVE ( 'NONE', #5833, #10254, #13322, .T. ) ;
#15520=ADVANCED_FACE ( 'NONE', ( #2999 ), #14418, .T. ) ;
#15523=AXIS2_PLACEMENT_3D ( 'NONE', #16902, #18417, #18526 ) ;
#15525=EDGE_LOOP ( 'NONE', ( #6986, #15141, #17171, #10531 ) ) ;
#15530=DIRECTION ( 'NONE',  ( -1.000000000000000000, 0.000000000000000000, 0.000000000000000000 ) ) ;
#15533=DIRECTION ( 'NONE',  ( -1.000000000000000000, -0.000000000000000000, 0.000000000000000000 ) ) ;
#15536=VERTEX_POINT ( 'NONE', #11749 ) ;
#15540=CARTESIAN_POINT ( 'NONE',  ( 10.00000000000000000, -26.71881558261695133, -49.49802920186252209 ) ) ;
#15541=EDGE_CURVE ( 'NONE', #407, #13852, #869, .T. ) ;
#15543=EDGE_CURVE ( 'NONE', #11178, #2985, #3594, .T. ) ;
#15544=ORIENTED_EDGE ( 'NONE', *, *, #9480, .T. ) ;
#15551=DIRECTION ( 'NONE',  ( 0.000000000000000000, -0.8910065241883721177, 0.4539904997395383113 ) ) ;
#15555=DIRECTION ( 'NONE',  ( -1.000000000000000000, -0.000000000000000000, 0.000000000000000000 ) ) ;
#15569=EDGE_CURVE ( 'NONE', #11858, #6887, #9973, .T. ) ;
#15573=DIRECTION ( 'NONE',  ( 0.000000000000000000, 0.000000000000000000, 1.000000000000000000 ) ) ;
#15576=ORIENTED_EDGE ( 'NONE', *, *, #2615, .T. ) ;
#15579=LINE ( 'NONE', #18339, #10721 ) ;
#15585=EDGE_CURVE ( 'NONE', #1536, #5770, #1759, .T. ) ;
#15586=ORIENTED_EDGE ( 'NONE', *, *, #16180, .T. ) ;
#15588=EDGE_CURVE ( 'NONE', #15536, #11085, #5101, .T. ) ;
#15591=CARTESIAN_POINT ( 'NONE',  ( 5.000000000000000000, -23.24033432160480217, 58.55669782892453412 ) ) ;
#15592=LINE ( 'NONE', #15683, #4778 ) ;
#15597=CARTESIAN_POINT ( 'NONE',  ( 0.000000000000000000, -32.11449294037235802, 54.20017844242499905 ) ) ;
#15600=ORIENTED_EDGE ( 'NONE', *, *, #14959, .T. ) ;
#15608=CYLINDRICAL_SURFACE ( 'NONE', #1415, 24.00000000002399503 ) ;
#15611=DIRECTION ( 'NONE',  ( -1.000000000000000000, -0.000000000000000000, 0.000000000000000000 ) ) ;
#15612=CIRCLE ( 'NONE', #7677, 63.00000000006298961 ) ;
#15613=DIRECTION ( 'NONE',  ( 1.000000000000000000, 0.000000000000000000, 0.000000000000000000 ) ) ;
#15615=ORIENTED_EDGE ( 'NONE', *, *, #4668, .T. ) ;
#15616=CIRCLE ( 'NONE', #1333, 63.00000000006298961 ) ;
#15617=ORIENTED_EDGE ( 'NONE', *, *, #7944, .F. ) ;
#15618=LINE ( 'NONE', #5036, #7501 ) ;
#15620=DIRECTION ( 'NONE',  ( 0.000000000000000000, -0.8090169943749531134, 0.5877852522924654766 ) ) ;
#15621=CARTESIAN_POINT ( 'NONE',  ( 10.00000000000000000, 0.000000000000000000, 0.000000000000000000 ) ) ;
#15624=CYLINDRICAL_SURFACE ( 'NONE', #10581, 24.00000000002400213 ) ;
#15629=DIRECTION ( 'NONE',  ( 0.000000000000000000, -0.4539904997395540764, 0.8910065241883640130 ) ) ;
#15635=VERTEX_POINT ( 'NONE', #16313 ) ;
#15636=EDGE_CURVE ( 'NONE', #1864, #6177, #6634, .T. ) ;
#15642=ADVANCED_FACE ( 'NONE', ( #8966 ), #1838, .F. ) ;
#15643=ADVANCED_FACE ( 'NONE', ( #3273 ), #3088, .T. ) ;
#15646=DIRECTION ( 'NONE',  ( -1.000000000000000000, 0.000000000000000000, -0.000000000000000000 ) ) ;
#15647=EDGE_LOOP ( 'NONE', ( #16730, #1982, #4187, #12533 ) ) ;
#15652=FACE_OUTER_BOUND ( 'NONE', #11614, .T. ) ;
#15657=LINE ( 'NONE', #6996, #8853 ) ;
#15659=ADVANCED_FACE ( 'NONE', ( #6028 ), #7553, .T. ) ;
#15661=AXIS2_PLACEMENT_3D ( 'NONE', #18576, #14193, #17066 ) ;
#15664=DIRECTION ( 'NONE',  ( 0.000000000000000000, -6.938893903900289557E-15, 1.000000000000000000 ) ) ;
#15669=CARTESIAN_POINT ( 'NONE',  ( 10.00000000000000000, -1.017308535512791767, 56.37237871411032586 ) ) ;
#15670=DIRECTION ( 'NONE',  ( -1.000000000000000000, -0.000000000000000000, 0.000000000000000000 ) ) ;
#15673=AXIS2_PLACEMENT_3D ( 'NONE', #9401, #271, #10816 ) ;
#15675=AXIS2_PLACEMENT_3D ( 'NONE', #6603, #16794, #17938 ) ;
#15677=FACE_OUTER_BOUND ( 'NONE', #1716, .T. ) ;
#15681=CARTESIAN_POINT ( 'NONE',  ( 10.00000000000000000, 0.000000000000000000, 0.000000000000000000 ) ) ;
#15682=VECTOR ( 'NONE', #11497, 1000.000000000000000 ) ;
#15683=CARTESIAN_POINT ( 'NONE',  ( 10.00000000000000000, 55.74967257055894265, -7.478235706488370660 ) ) ;
#15686=CARTESIAN_POINT ( 'NONE',  ( -10.00000000000000000, -42.79754323328189969, -11.25576474687263229 ) ) ;
#15690=CARTESIAN_POINT ( 'NONE',  ( 10.00000000000000000, -55.33199130079790962, 10.11537145609357502 ) ) ;
#15694=DIRECTION ( 'NONE',  ( 1.000000000000000000, -0.000000000000000000, -0.000000000000000000 ) ) ;
#15697=ORIENTED_EDGE ( 'NONE', *, *, #14019, .T. ) ;
#15698=VERTEX_POINT ( 'NONE', #11054 ) ;
#15701=DIRECTION ( 'NONE',  ( -1.000000000000000000, 0.000000000000000000, -0.000000000000000000 ) ) ;
#15703=ORIENTED_EDGE ( 'NONE', *, *, #15982, .F. ) ;
#15715=ORIENTED_EDGE ( 'NONE', *, *, #4003, .F. ) ;
#15716=FACE_OUTER_BOUND ( 'NONE', #10406, .T. ) ;
#15720=CARTESIAN_POINT ( 'NONE',  ( 0.000000000000000000, 0.000000000000000000, 0.000000000000000000 ) ) ;
#15725=ORIENTED_EDGE ( 'NONE', *, *, #11451, .F. ) ;
#15739=EDGE_LOOP ( 'NONE', ( #17946, #9544, #8973, #8421 ) ) ;
#15741=DIRECTION ( 'NONE',  ( -1.000000000000000000, 0.000000000000000000, -0.000000000000000000 ) ) ;
#15742=VECTOR ( 'NONE', #7027, 1000.000000000000000 ) ;
#15743=DIRECTION ( 'NONE',  ( 0.000000000000000000, -0.9876883405951394357, 0.1564344650402205994 ) ) ;
#15749=ORIENTED_EDGE ( 'NONE', *, *, #11187, .T. ) ;
#15751=DIRECTION ( 'NONE',  ( -1.000000000000000000, 0.000000000000000000, 0.000000000000000000 ) ) ;
#15752=CARTESIAN_POINT ( 'NONE',  ( -10.00000000000000000, 0.000000000000000000, 0.000000000000000000 ) ) ;
#15757=EDGE_CURVE ( 'NONE', #13284, #79, #13346, .T. ) ;
#15758=EDGE_CURVE ( 'NONE', #7847, #16606, #1484, .T. ) ;
#15760=EDGE_CURVE ( 'NONE', #12166, #7753, #18391, .T. ) ;
#15761=AXIS2_PLACEMENT_3D ( 'NONE', #13003, #13099, #8432 ) ;
#15763=DIRECTION ( 'NONE',  ( -1.000000000000000000, 0.000000000000000000, -0.000000000000000000 ) ) ;
#15764=EDGE_CURVE ( 'NONE', #5108, #1683, #5349, .T. ) ;
#15765=DIRECTION ( 'NONE',  ( -1.000000000000000000, 0.000000000000000000, 0.000000000000000000 ) ) ;
#15766=CARTESIAN_POINT ( 'NONE',  ( -10.00000000000000000, -26.45033635316118747, 36.40576474687271258 ) ) ;
#15769=AXIS2_PLACEMENT_3D ( 'NONE', #16625, #3865, #3590 ) ;
#15771=ORIENTED_EDGE ( 'NONE', *, *, #13504, .F. ) ;
#15773=CARTESIAN_POINT ( 'NONE',  ( 0.000000000000000000, 24.97244012287581327, -57.83923611457294101 ) ) ;
#15774=EDGE_CURVE ( 'NONE', #18250, #5010, #5738, .T. ) ;
#15775=CARTESIAN_POINT ( 'NONE',  ( 10.00000000000000000, 49.76630880786347433, -26.49895292617950560 ) ) ;
#15777=ORIENTED_EDGE ( 'NONE', *, *, #8767, .T. ) ;
#15783=AXIS2_PLACEMENT_3D ( 'NONE', #8231, #14034, #2216 ) ;
#15788=VECTOR ( 'NONE', #3337, 1000.000000000000000 ) ;
#15789=CARTESIAN_POINT ( 'NONE',  ( 4.999999999999999112, 61.47135697633798657, -13.79392154159068618 ) ) ;
#15790=EDGE_CURVE ( 'NONE', #3687, #2800, #1177, .T. ) ;
#15791=ORIENTED_EDGE ( 'NONE', *, *, #15569, .F. ) ;
#15792=CARTESIAN_POINT ( 'NONE',  ( 10.00000000000000000, -16.45250512421895550, 53.92768374110886498 ) ) ;
#15793=ORIENTED_EDGE ( 'NONE', *, *, #6922, .T. ) ;
#15797=ORIENTED_EDGE ( 'NONE', *, *, #16542, .T. ) ;
#15798=CYLINDRICAL_SURFACE ( 'NONE', #17913, 24.00000000002399858 ) ;
#15800=CIRCLE ( 'NONE', #13065, 24.00000000002400213 ) ;
#15802=ORIENTED_EDGE ( 'NONE', *, *, #14758, .F. ) ;
#15807=DIRECTION ( 'NONE',  ( 1.000000000000000000, 0.000000000000000000, 0.000000000000000000 ) ) ;
#15809=AXIS2_PLACEMENT_3D ( 'NONE', #17522, #7236, #10286 ) ;
#15811=EDGE_LOOP ( 'NONE', ( #10274, #2160, #13859, #8651 ) ) ;
#15812=AXIS2_PLACEMENT_3D ( 'NONE', #5294, #11099, #16922 ) ;
#15814=ORIENTED_EDGE ( 'NONE', *, *, #14132, .F. ) ;
#15815=CYLINDRICAL_SURFACE ( 'NONE', #210, 24.00000000002399858 ) ;
#15816=CARTESIAN_POINT ( 'NONE',  ( 10.00000000000000000, 0.000000000000000000, 0.000000000000000000 ) ) ;
#15818=DIRECTION ( 'NONE',  ( 0.000000000000000000, -6.982962677686266711E-15, 1.000000000000000000 ) ) ;
#15831=ORIENTED_EDGE ( 'NONE', *, *, #6322, .F. ) ;
#15832=ADVANCED_FACE ( 'NONE', ( #17446 ), #12888, .T. ) ;
#15836=DIRECTION ( 'NONE',  ( 0.000000000000000000, 0.000000000000000000, 1.000000000000000000 ) ) ;
#15838=CARTESIAN_POINT ( 'NONE',  ( 0.000000000000000000, 0.000000000000000000, 0.000000000000000000 ) ) ;
#15839=CARTESIAN_POINT ( 'NONE',  ( 10.00000000000000000, -24.97244012287543313, 57.83923611457311154 ) ) ;
#15842=DIRECTION ( 'NONE',  ( 0.000000000000000000, 0.000000000000000000, 1.000000000000000000 ) ) ;
#15843=ORIENTED_EDGE ( 'NONE', *, *, #13504, .T. ) ;
#15853=ORIENTED_EDGE ( 'NONE', *, *, #18307, .F. ) ;
#15854=CARTESIAN_POINT ( 'NONE',  ( 10.00000000000000000, 53.29895248911700634, -18.38754094778185788 ) ) ;
#15855=CARTESIAN_POINT ( 'NONE',  ( 10.00000000000000000, 33.95787273855245303, 45.00825343885033192 ) ) ;
#15856=CARTESIAN_POINT ( 'NONE',  ( 10.00000000000000000, -7.478235706488566059, -55.74967257055892134 ) ) ;
#15857=CARTESIAN_POINT ( 'NONE',  ( 10.00000000000000000, -16.45250512421816680, -53.92768374110909235 ) ) ;
#15859=ORIENTED_EDGE ( 'NONE', *, *, #8193, .F. ) ;
#15860=EDGE_CURVE ( 'NONE', #9916, #7866, #14315, .T. ) ;
#15861=CIRCLE ( 'NONE', #9463, 63.00000000006298961 ) ;
#15863=CYLINDRICAL_SURFACE ( 'NONE', #16924, 63.00000000006298961 ) ;
#15864=DIRECTION ( 'NONE',  ( -1.000000000000000000, 0.000000000000000000, -0.000000000000000000 ) ) ;
#15867=ORIENTED_EDGE ( 'NONE', *, *, #6488, .T. ) ;
#15868=DIRECTION ( 'NONE',  ( 0.000000000000000000, 0.5877852522924685852, 0.8090169943749506709 ) ) ;
#15880=VERTEX_POINT ( 'NONE', #28 ) ;
#15885=FACE_OUTER_BOUND ( 'NONE', #18769, .T. ) ;
#15886=DIRECTION ( 'NONE',  ( 0.000000000000000000, -6.938893903900288768E-15, 1.000000000000000000 ) ) ;
#15887=ORIENTED_EDGE ( 'NONE', *, *, #2849, .F. ) ;
#15891=ORIENTED_EDGE ( 'NONE', *, *, #5295, .F. ) ;
#15892=CARTESIAN_POINT ( 'NONE',  ( 0.000000000000000000, 56.23315539212690339, 1.335003989221828835 ) ) ;
#15901=CARTESIAN_POINT ( 'NONE',  ( 10.00000000000000000, 0.000000000000000000, 0.000000000000000000 ) ) ;
#15912=DIRECTION ( 'NONE',  ( 0.000000000000000000, 0.000000000000000000, 1.000000000000000000 ) ) ;
#15913=VERTEX_POINT ( 'NONE', #17537 ) ;
#15915=CYLINDRICAL_SURFACE ( 'NONE', #11030, 63.00000000006298961 ) ;
#15918=CIRCLE ( 'NONE', #8903, 24.00000000002399503 ) ;
#15922=DIRECTION ( 'NONE',  ( 0.000000000000000000, 0.9876883405951382144, -0.1564344650402274828 ) ) ;
#15929=CYLINDRICAL_SURFACE ( 'NONE', #3328, 56.24900000005625600 ) ;
#15930=VERTEX_POINT ( 'NONE', #3066 ) ;
#15932=DIRECTION ( 'NONE',  ( -1.000000000000000000, 0.000000000000000000, 0.000000000000000000 ) ) ;
#15933=FACE_OUTER_BOUND ( 'NONE', #5191, .T. ) ;
#15934=VERTEX_POINT ( 'NONE', #11826 ) ;
#15936=ADVANCED_FACE ( 'NONE', ( #10386 ), #10305, .F. ) ;
#15940=DIRECTION ( 'NONE',  ( -1.000000000000000000, 0.000000000000000000, 0.000000000000000000 ) ) ;
#15942=DIRECTION ( 'NONE',  ( 0.000000000000000000, 0.000000000000000000, 1.000000000000000000 ) ) ;
#15943=EDGE_CURVE ( 'NONE', #7149, #10237, #17017, .T. ) ;
#15946=EDGE_LOOP ( 'NONE', ( #9955, #893, #15586, #13410 ) ) ;
#15948=CARTESIAN_POINT ( 'NONE',  ( 0.000000000000000000, 53.29895248911675765, 18.38754094778260040 ) ) ;
#15951=VERTEX_POINT ( 'NONE', #206 ) ;
#15952=EDGE_LOOP ( 'NONE', ( #7305, #9840, #2586, #7222 ) ) ;
#15955=ORIENTED_EDGE ( 'NONE', *, *, #15541, .F. ) ;
#15958=DIRECTION ( 'NONE',  ( 0.000000000000000000, 0.000000000000000000, 1.000000000000000000 ) ) ;
#15960=ORIENTED_EDGE ( 'NONE', *, *, #17636, .F. ) ;
#15962=CIRCLE ( 'NONE', #17800, 56.24900000005625600 ) ;
#15963=ORIENTED_EDGE ( 'NONE', *, *, #17395, .F. ) ;
#15965=CIRCLE ( 'NONE', #3494, 63.00000000006298961 ) ;
#15966=ORIENTED_EDGE ( 'NONE', *, *, #767, .T. ) ;
#15967=ORIENTED_EDGE ( 'NONE', *, *, #8039, .F. ) ;
#15971=ORIENTED_EDGE ( 'NONE', *, *, #10295, .F. ) ;
#15982=EDGE_CURVE ( 'NONE', #5875, #18738, #15052, .T. ) ;
#15985=AXIS2_PLACEMENT_3D ( 'NONE', #2908, #2727, #11383 ) ;
#15988=DIRECTION ( 'NONE',  ( -1.000000000000000000, 0.000000000000000000, -0.000000000000000000 ) ) ;
#15994=DIRECTION ( 'NONE',  ( 0.000000000000000000, 0.000000000000000000, 1.000000000000000000 ) ) ;
#16003=ORIENTED_EDGE ( 'NONE', *, *, #11613, .F. ) ;
#16004=DIRECTION ( 'NONE',  ( 1.000000000000000000, 0.000000000000000000, 0.000000000000000000 ) ) ;
#16012=DIRECTION ( 'NONE',  ( 0.000000000000000000, 0.000000000000000000, 1.000000000000000000 ) ) ;
#16013=ORIENTED_EDGE ( 'NONE', *, *, #14134, .T. ) ;
#16016=CARTESIAN_POINT ( 'NONE',  ( 0.000000000000000000, 31.97297851452424311, 46.27827401617415148 ) ) ;
#16017=CARTESIAN_POINT ( 'NONE',  ( 10.00000000000000000, -56.37237871411034718, 1.017308535512174261 ) ) ;
#16019=CIRCLE ( 'NONE', #7799, 24.00000000002399503 ) ;
#16020=LINE ( 'NONE', #1546, #2607 ) ;
#16022=CARTESIAN_POINT ( 'NONE',  ( 10.00000000000000000, 0.000000000000000000, 0.000000000000000000 ) ) ;
#16024=ORIENTED_EDGE ( 'NONE', *, *, #14798, .F. ) ;
#16025=AXIS2_PLACEMENT_3D ( 'NONE', #4766, #6191, #1908 ) ;
#16027=CARTESIAN_POINT ( 'NONE',  ( 0.000000000000000000, -55.33199130079790962, 10.11537145609357502 ) ) ;
#16028=VERTEX_POINT ( 'NONE', #6674 ) ;
#16039=DIRECTION ( 'NONE',  ( 0.000000000000000000, -0.8090169943749402348, -0.5877852522924829071 ) ) ;
#16041=DIRECTION ( 'NONE',  ( -1.000000000000000000, 0.000000000000000000, 0.000000000000000000 ) ) ;
#16044=FACE_OUTER_BOUND ( 'NONE', #8770, .T. ) ;
#16046=DIRECTION ( 'NONE',  ( -1.000000000000000000, 0.000000000000000000, 0.000000000000000000 ) ) ;
#16063=DIRECTION ( 'NONE',  ( -1.000000000000000000, 0.000000000000000000, 0.000000000000000000 ) ) ;
#16064=VERTEX_POINT ( 'NONE', #13807 ) ;
#16072=ORIENTED_EDGE ( 'NONE', *, *, #16455, .T. ) ;
#16074=CARTESIAN_POINT ( 'NONE',  ( 0.000000000000000000, -50.69000562871659810, 24.68609584167141691 ) ) ;
#16076=ORIENTED_EDGE ( 'NONE', *, *, #9943, .F. ) ;
#16078=ORIENTED_EDGE ( 'NONE', *, *, #13194, .T. ) ;
#16082=AXIS2_PLACEMENT_3D ( 'NONE', #6084, #16468, #17615 ) ;
#16084=ORIENTED_EDGE ( 'NONE', *, *, #6917, .T. ) ;
#16086=ORIENTED_EDGE ( 'NONE', *, *, #4005, .T. ) ;
#16091=DIRECTION ( 'NONE',  ( -1.000000000000000000, -0.000000000000000000, 0.000000000000000000 ) ) ;
#16094=CARTESIAN_POINT ( 'NONE',  ( 10.00000000000000000, 0.000000000000000000, 0.000000000000000000 ) ) ;
#16096=ORIENTED_EDGE ( 'NONE', *, *, #6488, .F. ) ;
#16097=AXIS2_PLACEMENT_3D ( 'NONE', #14543, #4114, #4180 ) ;
#16098=DIRECTION ( 'NONE',  ( 0.000000000000000000, -0.1564344650402381964, 0.9876883405951365491 ) ) ;
#16099=EDGE_CURVE ( 'NONE', #18692, #16028, #8793, .T. ) ;
#16109=VERTEX_POINT ( 'NONE', #6850 ) ;
#16111=DIRECTION ( 'NONE',  ( -1.000000000000000000, -0.000000000000000000, 0.000000000000000000 ) ) ;
#16112=ADVANCED_FACE ( 'NONE', ( #17246 ), #8, .T. ) ;
#16114=LINE ( 'NONE', #3068, #6598 ) ;
#16117=FACE_OUTER_BOUND ( 'NONE', #18681, .T. ) ;
#16120=DIRECTION ( 'NONE',  ( -1.000000000000000000, -0.000000000000000000, 0.000000000000000000 ) ) ;
#16123=CIRCLE ( 'NONE', #17952, 63.00000000006298961 ) ;
#16126=DIRECTION ( 'NONE',  ( -1.000000000000000000, 0.000000000000000000, -0.000000000000000000 ) ) ;
#16130=ORIENTED_EDGE ( 'NONE', *, *, #11592, .T. ) ;
#16140=CARTESIAN_POINT ( 'NONE',  ( 10.00000000000000000, 55.83748330407397020, 7.813799127874245798 ) ) ;
#16144=CARTESIAN_POINT ( 'NONE',  ( 0.000000000000000000, 62.72529079327807011, 5.876895005582658982 ) ) ;
#16146=EDGE_LOOP ( 'NONE', ( #1444, #798, #3853, #12706 ) ) ;
#16149=AXIS2_PLACEMENT_3D ( 'NONE', #2451, #1028, #16393 ) ;
#16151=DIRECTION ( 'NONE',  ( -1.000000000000000000, -0.000000000000000000, -0.000000000000000000 ) ) ;
#16153=EDGE_CURVE ( 'NONE', #15934, #16801, #4375, .T. ) ;
#16154=CARTESIAN_POINT ( 'NONE',  ( 10.00000000000000000, -55.83748330407401284, -7.813799127873885197 ) ) ;
#16157=ORIENTED_EDGE ( 'NONE', *, *, #9915, .F. ) ;
#16160=DIRECTION ( 'NONE',  ( -1.000000000000000000, 0.000000000000000000, 0.000000000000000000 ) ) ;
#16165=VERTEX_POINT ( 'NONE', #12865 ) ;
#16166=ORIENTED_EDGE ( 'NONE', *, *, #524, .F. ) ;
#16167=DIRECTION ( 'NONE',  ( -1.000000000000000000, 0.000000000000000000, 0.000000000000000000 ) ) ;
#16170=DIRECTION ( 'NONE',  ( -1.000000000000000000, 0.000000000000000000, 0.000000000000000000 ) ) ;
#16171=AXIS2_PLACEMENT_3D ( 'NONE', #10224, #11932, #16225 ) ;
#16177=CARTESIAN_POINT ( 'NONE',  ( 10.00000000000000000, -55.74967257055877212, -7.478235706489567924 ) ) ;
#16179=CARTESIAN_POINT ( 'NONE',  ( 10.00000000000000000, 0.000000000000000000, 0.000000000000000000 ) ) ;
#16180=EDGE_CURVE ( 'NONE', #657, #2530, #4238, .T. ) ;
#16181=ORIENTED_EDGE ( 'NONE', *, *, #17845, .T. ) ;
#16189=EDGE_CURVE ( 'NONE', #14103, #1805, #894, .T. ) ;
#16190=VECTOR ( 'NONE', #8386, 1000.000000000000000 ) ;
#16192=CARTESIAN_POINT ( 'NONE',  ( 0.000000000000000000, 53.89344778774812283, 16.10733642026502110 ) ) ;
#16194=ADVANCED_FACE ( 'NONE', ( #18664 ), #5439, .T. ) ;
#16196=CIRCLE ( 'NONE', #2203, 24.00000000002400569 ) ;
#16199=LINE ( 'NONE', #3152, #8250 ) ;
#16206=CARTESIAN_POINT ( 'NONE',  ( 10.00000000000000000, 41.62350880771921169, 47.29147401531969308 ) ) ;
#16209=ORIENTED_EDGE ( 'NONE', *, *, #12967, .F. ) ;
#16212=FACE_OUTER_BOUND ( 'NONE', #5923, .T. ) ;
#16215=ORIENTED_EDGE ( 'NONE', *, *, #4086, .F. ) ;
#16216=EDGE_CURVE ( 'NONE', #15951, #6735, #15965, .T. ) ;
#16221=EDGE_CURVE ( 'NONE', #2222, #17488, #1372, .T. ) ;
#16223=CARTESIAN_POINT ( 'NONE',  ( 10.00000000000000000, 42.79754323328179311, -13.90576474687299680 ) ) ;
#16224=DIRECTION ( 'NONE',  ( 0.000000000000000000, 1.000000000000000000, 3.469446951950144779E-15 ) ) ;
#16225=DIRECTION ( 'NONE',  ( 0.000000000000000000, 0.000000000000000000, 1.000000000000000000 ) ) ;
#16231=CYLINDRICAL_SURFACE ( 'NONE', #575, 63.00000000006298961 ) ;
#16234=DIRECTION ( 'NONE',  ( -1.000000000000000000, 0.000000000000000000, -0.000000000000000000 ) ) ;
#16239=ADVANCED_FACE ( 'NONE', ( #1519 ), #454, .T. ) ;
#16243=LINE ( 'NONE', #7576, #2905 ) ;
#16244=CARTESIAN_POINT ( 'NONE',  ( 5.000000000000000000, -47.29147401531926675, -41.62350880771970196 ) ) ;
#16248=ORIENTED_EDGE ( 'NONE', *, *, #3612, .F. ) ;
#16252=( GEOMETRIC_REPRESENTATION_CONTEXT ( 3 ) GLOBAL_UNCERTAINTY_ASSIGNED_CONTEXT ( ( #17018 ) ) GLOBAL_UNIT_ASSIGNED_CONTEXT ( ( #2840, #13217, #13037 ) ) REPRESENTATION_CONTEXT ( 'NONE', 'WORKASPACE' ) );
#16258=FILL_AREA_STYLE ('',( #11516 ) ) ;
#16262=CIRCLE ( 'NONE', #2890, 24.00000000002399858 ) ;
#16263=ORIENTED_EDGE ( 'NONE', *, *, #15287, .F. ) ;
#16265=DIRECTION ( 'NONE',  ( -1.000000000000000000, 0.000000000000000000, -0.000000000000000000 ) ) ;
#16270=EDGE_CURVE ( 'NONE', #6404, #10818, #4708, .T. ) ;
#16272=DIRECTION ( 'NONE',  ( 0.000000000000000000, 0.000000000000000000, 1.000000000000000000 ) ) ;
#16275=CARTESIAN_POINT ( 'NONE',  ( 10.00000000000000000, 9.823366686501460165, -55.51919907100641893 ) ) ;
#16278=VERTEX_POINT ( 'NONE', #17890 ) ;
#16284=ORIENTED_EDGE ( 'NONE', *, *, #14323, .T. ) ;
#16289=ORIENTED_EDGE ( 'NONE', *, *, #8259, .F. ) ;
#16296=ORIENTED_EDGE ( 'NONE', *, *, #4432, .T. ) ;
#16297=FACE_OUTER_BOUND ( 'NONE', #1396, .T. ) ;
#16304=AXIS2_PLACEMENT_3D ( 'NONE', #5641, #3831, #5462 ) ;
#16308=ORIENTED_EDGE ( 'NONE', *, *, #15431, .T. ) ;
#16309=VERTEX_POINT ( 'NONE', #95 ) ;
#16310=DIRECTION ( 'NONE',  ( -1.000000000000000000, 0.000000000000000000, 0.000000000000000000 ) ) ;
#16311=CYLINDRICAL_SURFACE ( 'NONE', #9422, 24.00000000002399858 ) ;
#16312=AXIS2_PLACEMENT_3D ( 'NONE', #13235, #10101, #15912 ) ;
#16313=CARTESIAN_POINT ( 'NONE',  ( 10.00000000000000000, -56.37237871411034718, 25.01730853553617351 ) ) ;
#16315=AXIS2_PLACEMENT_3D ( 'NONE', #15720, #2475, #5233 ) ;
#16316=CYLINDRICAL_SURFACE ( 'NONE', #6300, 2.649999999999999467 ) ;
#16317=DIRECTION ( 'NONE',  ( -1.000000000000000000, 0.000000000000000000, -0.000000000000000000 ) ) ;
#16326=VERTEX_POINT ( 'NONE', #8927 ) ;
#16327=ORIENTED_EDGE ( 'NONE', *, *, #2202, .T. ) ;
#16329=EDGE_CURVE ( 'NONE', #7239, #16626, #11884, .T. ) ;
#16332=DIRECTION ( 'NONE',  ( 1.000000000000000000, 0.000000000000000000, 0.000000000000000000 ) ) ;
#16334=VERTEX_POINT ( 'NONE', #13510 ) ;
#16338=AXIS2_PLACEMENT_3D ( 'NONE', #9686, #14067, #7015 ) ;
#16339=VECTOR ( 'NONE', #2564, 1000.000000000000000 ) ;
#16341=CYLINDRICAL_SURFACE ( 'NONE', #15070, 24.00000000002399858 ) ;
#16342=FACE_OUTER_BOUND ( 'NONE', #5156, .T. ) ;
#16343=FACE_OUTER_BOUND ( 'NONE', #10168, .T. ) ;
#16348=ORIENTED_EDGE ( 'NONE', *, *, #1094, .F. ) ;
#16351=CIRCLE ( 'NONE', #6916, 63.00000000006298961 ) ;
#16352=LINE ( 'NONE', #17592, #11441 ) ;
#16353=DIRECTION ( 'NONE',  ( 0.000000000000000000, 0.000000000000000000, 1.000000000000000000 ) ) ;
#16354=VECTOR ( 'NONE', #4990, 1000.000000000000000 ) ;
#16356=VERTEX_POINT ( 'NONE', #655 ) ;
#16359=CARTESIAN_POINT ( 'NONE',  ( 0.000000000000000000, -54.20017844242534721, 32.11449294037177538 ) ) ;
#16361=ORIENTED_EDGE ( 'NONE', *, *, #11424, .T. ) ;
#16362=CARTESIAN_POINT ( 'NONE',  ( 0.000000000000000000, -55.33199130079777461, -10.11537145609435306 ) ) ;
#16366=CARTESIAN_POINT ( 'NONE',  ( 10.00000000000000000, 34.13306034420251223, -44.70888270294124567 ) ) ;
#16371=VERTEX_POINT ( 'NONE', #16652 ) ;
#16375=ORIENTED_EDGE ( 'NONE', *, *, #67, .F. ) ;
#16377=CARTESIAN_POINT ( 'NONE',  ( 5.000000000000000000, 48.50907078259439942, -40.19788616105557111 ) ) ;
#16380=DIRECTION ( 'NONE',  ( -1.000000000000000000, 0.000000000000000000, 0.000000000000000000 ) ) ;
#16381=ORIENTED_EDGE ( 'NONE', *, *, #630, .F. ) ;
#16382=DIRECTION ( 'NONE',  ( -1.000000000000000000, 0.000000000000000000, -0.000000000000000000 ) ) ;
#16389=EDGE_CURVE ( 'NONE', #13820, #4463, #9210, .T. ) ;
#16390=AXIS2_PLACEMENT_3D ( 'NONE', #5932, #6035, #3093 ) ;
#16393=DIRECTION ( 'NONE',  ( 0.000000000000000000, 0.000000000000000000, 1.000000000000000000 ) ) ;
#16395=ORIENTED_EDGE ( 'NONE', *, *, #1376, .T. ) ;
#16400=DIRECTION ( 'NONE',  ( -1.000000000000000000, 0.000000000000000000, 0.000000000000000000 ) ) ;
#16401=CARTESIAN_POINT ( 'NONE',  ( 10.00000000000000000, 26.71881558261730660, 49.49802920186232313 ) ) ;
#16403=DIRECTION ( 'NONE',  ( 0.000000000000000000, 0.000000000000000000, 1.000000000000000000 ) ) ;
#16404=ORIENTED_EDGE ( 'NONE', *, *, #9995, .F. ) ;
#16407=DIRECTION ( 'NONE',  ( -1.000000000000000000, 0.000000000000000000, 0.000000000000000000 ) ) ;
#16409=CIRCLE ( 'NONE', #11229, 63.00000000006298961 ) ;
#16411=ORIENTED_EDGE ( 'NONE', *, *, #16270, .T. ) ;
#16412=EDGE_LOOP ( 'NONE', ( #2315, #8115, #6758, #5999 ) ) ;
#16413=VERTEX_POINT ( 'NONE', #3610 ) ;
#16416=DIRECTION ( 'NONE',  ( 0.000000000000000000, -0.8910065241883722287, 0.4539904997395383668 ) ) ;
#16418=VECTOR ( 'NONE', #18114, 1000.000000000000000 ) ;
#16424=ORIENTED_EDGE ( 'NONE', *, *, #7362, .F. ) ;
#16426=DIRECTION ( 'NONE',  ( 0.000000000000000000, 0.1564344650402243464, 0.9876883405951388806 ) ) ;
#16432=DIRECTION ( 'NONE',  ( 0.000000000000000000, 0.4539904997395479147, -0.8910065241883673437 ) ) ;
#16433=ORIENTED_EDGE ( 'NONE', *, *, #17266, .T. ) ;
#16435=CIRCLE ( 'NONE', #15523, 56.24900000005625600 ) ;
#16439=ORIENTED_EDGE ( 'NONE', *, *, #10895, .T. ) ;
#16441=DIRECTION ( 'NONE',  ( 0.000000000000000000, 0.000000000000000000, 1.000000000000000000 ) ) ;
#16442=EDGE_CURVE ( 'NONE', #4722, #8684, #16262, .T. ) ;
#16447=DIRECTION ( 'NONE',  ( 0.000000000000000000, -0.1564344650402171299, -0.9876883405951398798 ) ) ;
#16448=DIRECTION ( 'NONE',  ( 1.000000000000000000, 0.000000000000000000, 0.000000000000000000 ) ) ;
#16452=ADVANCED_FACE ( 'NONE', ( #946 ), #12352, .T. ) ;
#16455=EDGE_CURVE ( 'NONE', #12567, #10719, #7779, .T. ) ;
#16456=AXIS2_PLACEMENT_3D ( 'NONE', #2917, #8723, #2637 ) ;
#16458=ORIENTED_EDGE ( 'NONE', *, *, #17395, .T. ) ;
#16461=ORIENTED_EDGE ( 'NONE', *, *, #9246, .T. ) ;
#16463=CARTESIAN_POINT ( 'NONE',  ( 0.000000000000000000, 42.79754323328179311, -13.90576474687299680 ) ) ;
#16467=ADVANCED_FACE ( 'NONE', ( #10821 ), #15408, .T. ) ;
#16468=DIRECTION ( 'NONE',  ( -1.000000000000000000, -0.000000000000000000, -0.000000000000000000 ) ) ;
#16471=VERTEX_POINT ( 'NONE', #12262 ) ;
#16472=DIRECTION ( 'NONE',  ( 0.000000000000000000, 0.8090169943749486725, -0.5877852522924714718 ) ) ;
#16475=LINE ( 'NONE', #9220, #10537 ) ;
#16481=ORIENTED_EDGE ( 'NONE', *, *, #4802, .F. ) ;
#16482=CARTESIAN_POINT ( 'NONE',  ( 0.000000000000000000, -53.92768374110879392, -16.45250512421912603 ) ) ;
#16483=ORIENTED_EDGE ( 'NONE', *, *, #1777, .F. ) ;
#16486=AXIS2_PLACEMENT_3D ( 'NONE', #1612, #7414, #3140 ) ;
#16487=CARTESIAN_POINT ( 'NONE',  ( 10.00000000000000000, 0.000000000000000000, 0.000000000000000000 ) ) ;
#16488=CARTESIAN_POINT ( 'NONE',  ( 4.999999999999999112, -5.876895005581972420, -62.72529079327814117 ) ) ;
#16490=VERTEX_POINT ( 'NONE', #558 ) ;
#16502=DIRECTION ( 'NONE',  ( -1.000000000000000000, 0.000000000000000000, -0.000000000000000000 ) ) ;
#16503=CARTESIAN_POINT ( 'NONE',  ( 10.00000000000000000, 0.000000000000000000, 0.000000000000000000 ) ) ;
#16507=ORIENTED_EDGE ( 'NONE', *, *, #7143, .F. ) ;
#16508=DIRECTION ( 'NONE',  ( 1.000000000000000000, -0.000000000000000000, -0.000000000000000000 ) ) ;
#16509=VERTEX_POINT ( 'NONE', #750 ) ;
#16515=DIRECTION ( 'NONE',  ( -1.000000000000000000, 0.000000000000000000, 0.000000000000000000 ) ) ;
#16516=ORIENTED_EDGE ( 'NONE', *, *, #4369, .F. ) ;
#16519=CYLINDRICAL_SURFACE ( 'NONE', #8108, 24.00000000002400213 ) ;
#16526=CYLINDRICAL_SURFACE ( 'NONE', #9603, 24.00000000002399858 ) ;
#16528=FACE_OUTER_BOUND ( 'NONE', #620, .T. ) ;
#16538=ORIENTED_EDGE ( 'NONE', *, *, #10869, .F. ) ;
#16539=CARTESIAN_POINT ( 'NONE',  ( 10.00000000000000000, -56.37237871411034718, 1.017308535512174261 ) ) ;
#16542=EDGE_CURVE ( 'NONE', #1960, #9593, #5628, .T. ) ;
#16543=DIRECTION ( 'NONE',  ( 1.000000000000000000, -0.000000000000000000, 0.000000000000000000 ) ) ;
#16544=VERTEX_POINT ( 'NONE', #3092 ) ;
#16545=VERTEX_POINT ( 'NONE', #8801 ) ;
#16546=DIRECTION ( 'NONE',  ( -1.000000000000000000, 0.000000000000000000, 0.000000000000000000 ) ) ;
#16547=EDGE_CURVE ( 'NONE', #3360, #16545, #1010, .T. ) ;
#16550=ORIENTED_EDGE ( 'NONE', *, *, #17599, .T. ) ;
#16556=CARTESIAN_POINT ( 'NONE',  ( 0.000000000000000000, -47.29147401531926675, -41.62350880771970196 ) ) ;
#16558=DIRECTION ( 'NONE',  ( -1.000000000000000000, 0.000000000000000000, 0.000000000000000000 ) ) ;
#16559=DIRECTION ( 'NONE',  ( 0.000000000000000000, 0.000000000000000000, 1.000000000000000000 ) ) ;
#16564=ADVANCED_FACE ( 'NONE', ( #5508 ), #6033, .T. ) ;
#16565=EDGE_CURVE ( 'NONE', #3234, #7366, #15612, .T. ) ;
#16577=VERTEX_POINT ( 'NONE', #6935 ) ;
#16580=CARTESIAN_POINT ( 'NONE',  ( 10.00000000000000000, 24.33982105418971642, -50.71018745830419050 ) ) ;
#16582=ADVANCED_FACE ( 'NONE', ( #17467 ), #7364, .T. ) ;
#16586=CARTESIAN_POINT ( 'NONE',  ( 10.00000000000000000, 0.000000000000000000, 0.000000000000000000 ) ) ;
#16589=EDGE_CURVE ( 'NONE', #16829, #17686, #3986, .T. ) ;
#16595=DIRECTION ( 'NONE',  ( 1.000000000000000000, 0.000000000000000000, -0.000000000000000000 ) ) ;
#16598=CYLINDRICAL_SURFACE ( 'NONE', #6243, 24.00000000002400213 ) ;
#16599=ORIENTED_EDGE ( 'NONE', *, *, #10895, .F. ) ;
#16601=AXIS2_PLACEMENT_3D ( 'NONE', #15669, #14248, #7006 ) ;
#16603=CARTESIAN_POINT ( 'NONE',  ( 10.00000000000000000, 16.10733642026559309, -53.89344778774794520 ) ) ;
#16606=VERTEX_POINT ( 'NONE', #4415 ) ;
#16608=ORIENTED_EDGE ( 'NONE', *, *, #13908, .F. ) ;
#16612=DIRECTION ( 'NONE',  ( -1.000000000000000000, -0.000000000000000000, -0.000000000000000000 ) ) ;
#16614=CIRCLE ( 'NONE', #18750, 24.00000000002399858 ) ;
#16617=DIRECTION ( 'NONE',  ( 0.000000000000000000, 0.000000000000000000, 1.000000000000000000 ) ) ;
#16620=AXIS2_PLACEMENT_3D ( 'NONE', #10996, #16733, #6526 ) ;
#16625=CARTESIAN_POINT ( 'NONE',  ( 10.00000000000000000, 0.000000000000000000, 0.000000000000000000 ) ) ;
#16626=VERTEX_POINT ( 'NONE', #9876 ) ;
#16632=CIRCLE ( 'NONE', #14759, 56.24900000005627021 ) ;
#16635=EDGE_CURVE ( 'NONE', #13520, #16959, #5248, .T. ) ;
#16642=VECTOR ( 'NONE', #18504, 1000.000000000000000 ) ;
#16651=CIRCLE ( 'NONE', #15132, 63.00000000006298961 ) ;
#16652=CARTESIAN_POINT ( 'NONE',  ( 0.000000000000000000, 33.71303790549275448, 53.22058882792209289 ) ) ;
#16653=DIRECTION ( 'NONE',  ( -1.000000000000000000, 0.000000000000000000, 0.000000000000000000 ) ) ;
#16654=EDGE_LOOP ( 'NONE', ( #4841, #2909, #10088, #8747 ) ) ;
#16657=DIRECTION ( 'NONE',  ( 0.000000000000000000, 0.000000000000000000, 1.000000000000000000 ) ) ;
#16665=CIRCLE ( 'NONE', #18804, 24.00000000002400213 ) ;
#16667=CIRCLE ( 'NONE', #5104, 63.00000000006298961 ) ;
#16673=DIRECTION ( 'NONE',  ( -1.000000000000000000, -0.000000000000000000, 0.000000000000000000 ) ) ;
#16676=AXIS2_PLACEMENT_3D ( 'NONE', #9844, #1368, #18513 ) ;
#16677=EDGE_CURVE ( 'NONE', #4773, #15536, #11653, .T. ) ;
#16685=EDGE_CURVE ( 'NONE', #18250, #8867, #384, .T. ) ;
#16688=ORIENTED_EDGE ( 'NONE', *, *, #18566, .T. ) ;
#16689=EDGE_CURVE ( 'NONE', #10808, #4800, #7370, .T. ) ;
#16690=ORIENTED_EDGE ( 'NONE', *, *, #615, .T. ) ;
#16692=VECTOR ( 'NONE', #15237, 1000.000000000000000 ) ;
#16696=VECTOR ( 'NONE', #3794, 1000.000000000000000 ) ;
#16697=ORIENTED_EDGE ( 'NONE', *, *, #11323, .T. ) ;
#16709=ORIENTED_EDGE ( 'NONE', *, *, #7147, .F. ) ;
#16712=CIRCLE ( 'NONE', #1202, 24.00000000002399858 ) ;
#16715=CARTESIAN_POINT ( 'NONE',  ( 10.00000000000000000, -62.72529079327802748, -5.876895005583096854 ) ) ;
#16716=ORIENTED_EDGE ( 'NONE', *, *, #11280, .F. ) ;
#16717=ORIENTED_EDGE ( 'NONE', *, *, #11567, .F. ) ;
#16719=DIRECTION ( 'NONE',  ( -1.000000000000000000, -0.000000000000000000, -0.000000000000000000 ) ) ;
#16724=AXIS2_PLACEMENT_3D ( 'NONE', #16503, #13936, #2410 ) ;
#16725=DIRECTION ( 'NONE',  ( -1.000000000000000000, 0.000000000000000000, 0.000000000000000000 ) ) ;
#16729=DIRECTION ( 'NONE',  ( -1.000000000000000000, -0.000000000000000000, -0.000000000000000000 ) ) ;
#16730=ORIENTED_EDGE ( 'NONE', *, *, #5547, .F. ) ;
#16732=ORIENTED_EDGE ( 'NONE', *, *, #12052, .T. ) ;
#16733=DIRECTION ( 'NONE',  ( -1.000000000000000000, -0.000000000000000000, -0.000000000000000000 ) ) ;
#16736=VERTEX_POINT ( 'NONE', #13380 ) ;
#16737=ORIENTED_EDGE ( 'NONE', *, *, #767, .F. ) ;
#16739=DIRECTION ( 'NONE',  ( -1.000000000000000000, 0.000000000000000000, 0.000000000000000000 ) ) ;
#16744=DIRECTION ( 'NONE',  ( 0.000000000000000000, 0.000000000000000000, -1.000000000000000000 ) ) ;
#16753=EDGE_LOOP ( 'NONE', ( #13537, #7725, #16076, #4541 ) ) ;
#16754=EDGE_CURVE ( 'NONE', #5801, #6887, #3562, .T. ) ;
#16756=CYLINDRICAL_SURFACE ( 'NONE', #11333, 63.00000000006298961 ) ;
#16770=CARTESIAN_POINT ( 'NONE',  ( 0.000000000000000000, -53.22058882792220658, 33.71303790549256263 ) ) ;
#16773=CARTESIAN_POINT ( 'NONE',  ( 0.000000000000000000, -55.83748330407413363, 7.813799127873079620 ) ) ;
#16776=DIRECTION ( 'NONE',  ( 0.000000000000000000, 0.000000000000000000, -1.000000000000000000 ) ) ;
#16777=CARTESIAN_POINT ( 'NONE',  ( 5.000000000000000000, -47.29147401531984229, 41.62350880771904826 ) ) ;
#16778=ORIENTED_EDGE ( 'NONE', *, *, #3069, .T. ) ;
#16779=DIRECTION ( 'NONE',  ( -1.000000000000000000, -0.000000000000000000, -0.000000000000000000 ) ) ;
#16781=ORIENTED_EDGE ( 'NONE', *, *, #7270, .T. ) ;
#16786=VERTEX_POINT ( 'NONE', #2413 ) ;
#16788=CARTESIAN_POINT ( 'NONE',  ( 10.00000000000000000, 56.37237871411034007, 25.01730853553658207 ) ) ;
#16791=CARTESIAN_POINT ( 'NONE',  ( 0.000000000000000000, -32.11449294037157642, -54.20017844242546090 ) ) ;
#16794=DIRECTION ( 'NONE',  ( -1.000000000000000000, -0.000000000000000000, 0.000000000000000000 ) ) ;
#16797=ORIENTED_EDGE ( 'NONE', *, *, #6335, .F. ) ;
#16801=VERTEX_POINT ( 'NONE', #8123 ) ;
#16802=CARTESIAN_POINT ( 'NONE',  ( -10.00000000000000000, 0.000000000000000000, 0.000000000000000000 ) ) ;
#16806=ORIENTED_EDGE ( 'NONE', *, *, #10265, .F. ) ;
#16807=EDGE_CURVE ( 'NONE', #16626, #8925, #2523, .T. ) ;
#16808=EDGE_CURVE ( 'NONE', #6735, #1940, #9512, .T. ) ;
#16810=CARTESIAN_POINT ( 'NONE',  ( -10.00000000000000000, 0.000000000000000000, 0.000000000000000000 ) ) ;
#16817=CIRCLE ( 'NONE', #8604, 56.24900000005625600 ) ;
#16819=DIRECTION ( 'NONE',  ( 0.000000000000000000, 0.000000000000000000, 1.000000000000000000 ) ) ;
#16825=DIRECTION ( 'NONE',  ( 0.000000000000000000, -0.7071067811865535679, 0.7071067811865413555 ) ) ;
#16827=ORIENTED_EDGE ( 'NONE', *, *, #15124, .T. ) ;
#16829=VERTEX_POINT ( 'NONE', #8319 ) ;
#16830=DIRECTION ( 'NONE',  ( -1.000000000000000000, 0.000000000000000000, -0.000000000000000000 ) ) ;
#16832=CIRCLE ( 'NONE', #2842, 2.649999999999999467 ) ;
#16838=DIRECTION ( 'NONE',  ( 0.000000000000000000, 0.000000000000000000, -1.000000000000000000 ) ) ;
#16845=ORIENTED_EDGE ( 'NONE', *, *, #11249, .T. ) ;
#16848=CARTESIAN_POINT ( 'NONE',  ( 10.00000000000000000, 0.000000000000000000, 0.000000000000000000 ) ) ;
#16859=CARTESIAN_POINT ( 'NONE',  ( 0.000000000000000000, -46.20417134726153563, 32.31183295104756326 ) ) ;
#16868=MECHANICAL_DESIGN_GEOMETRIC_PRESENTATION_REPRESENTATION('',(#14130),#16252);
#16869=CARTESIAN_POINT ( 'NONE',  ( 10.00000000000000000, 1.335003989222417697, -56.23315539212688918 ) ) ;
#16871=EDGE_CURVE ( 'NONE', #5833, #14748, #16817, .T. ) ;
#16885=CARTESIAN_POINT ( 'NONE',  ( 0.000000000000000000, -5.120903701083534543E-13, -42.35000000000000142 ) ) ;
#16886=CYLINDRICAL_SURFACE ( 'NONE', #4915, 24.00000000002400213 ) ;
#16891=DIRECTION ( 'NONE',  ( -1.000000000000000000, -0.000000000000000000, 0.000000000000000000 ) ) ;
#16892=DIRECTION ( 'NONE',  ( 0.000000000000000000, 0.9510565162951523099, 0.3090169943749515036 ) ) ;
#16901=DIRECTION ( 'NONE',  ( 0.000000000000000000, 0.4539904997395412534, 0.8910065241883707854 ) ) ;
#16902=CARTESIAN_POINT ( 'NONE',  ( 10.00000000000000000, 0.000000000000000000, 0.000000000000000000 ) ) ;
#16909=CIRCLE ( 'NONE', #13854, 56.24900000005625600 ) ;
#16913=EDGE_CURVE ( 'NONE', #8709, #2515, #18612, .T. ) ;
#16920=EDGE_CURVE ( 'NONE', #3669, #6075, #13829, .T. ) ;
#16922=DIRECTION ( 'NONE',  ( 0.000000000000000000, 0.000000000000000000, 1.000000000000000000 ) ) ;
#16924=AXIS2_PLACEMENT_3D ( 'NONE', #56, #1380, #18622 ) ;
#16926=AXIS2_PLACEMENT_3D ( 'NONE', #14330, #15763, #12904 ) ;
#16929=DIRECTION ( 'NONE',  ( 0.000000000000000000, 0.000000000000000000, 1.000000000000000000 ) ) ;
#16934=DIRECTION ( 'NONE',  ( -1.000000000000000000, 0.000000000000000000, -0.000000000000000000 ) ) ;
#16937=CARTESIAN_POINT ( 'NONE',  ( 10.00000000000000000, 0.000000000000000000, 0.000000000000000000 ) ) ;
#16941=ADVANCED_FACE ( 'NONE', ( #11059 ), #16886, .T. ) ;
#16942=VERTEX_POINT ( 'NONE', #10309 ) ;
#16943=AXIS2_PLACEMENT_3D ( 'NONE', #16773, #17915, #9522 ) ;
#16944=ADVANCED_FACE ( 'NONE', ( #16117 ), #2982, .F. ) ;
#16945=DIRECTION ( 'NONE',  ( -1.000000000000000000, 0.000000000000000000, -0.000000000000000000 ) ) ;
#16948=ORIENTED_EDGE ( 'NONE', *, *, #11490, .F. ) ;
#16949=ORIENTED_EDGE ( 'NONE', *, *, #383, .F. ) ;
#16950=AXIS2_PLACEMENT_3D ( 'NONE', #11531, #2766, #17067 ) ;
#16951=VERTEX_POINT ( 'NONE', #17367 ) ;
#16953=CARTESIAN_POINT ( 'NONE',  ( 10.00000000000000000, 34.13306034420251223, -44.70888270294124567 ) ) ;
#16955=VECTOR ( 'NONE', #9880, 1000.000000000000000 ) ;
#16957=VECTOR ( 'NONE', #10774, 1000.000000000000000 ) ;
#16959=VERTEX_POINT ( 'NONE', #8780 ) ;
#16960=DIRECTION ( 'NONE',  ( 0.000000000000000000, 0.9876883405951371042, 0.1564344650402347547 ) ) ;
#16963=CARTESIAN_POINT ( 'NONE',  ( 10.00000000000000000, 0.000000000000000000, 0.000000000000000000 ) ) ;
#16969=ORIENTED_EDGE ( 'NONE', *, *, #14850, .T. ) ;
#16974=DIRECTION ( 'NONE',  ( 1.000000000000000000, 0.000000000000000000, -0.000000000000000000 ) ) ;
#16975=AXIS2_PLACEMENT_3D ( 'NONE', #11864, #1949, #9381 ) ;
#16979=VERTEX_POINT ( 'NONE', #2879 ) ;
#16982=VECTOR ( 'NONE', #17132, 1000.000000000000000 ) ;
#16983=ORIENTED_EDGE ( 'NONE', *, *, #9650, .F. ) ;
#16984=AXIS2_PLACEMENT_3D ( 'NONE', #13455, #9062, #3359 ) ;
#16985=FACE_OUTER_BOUND ( 'NONE', #5564, .T. ) ;
#16986=( LENGTH_UNIT ( ) NAMED_UNIT ( * ) SI_UNIT ( .MILLI., .METRE. ) );
#16988=AXIS2_PLACEMENT_3D ( 'NONE', #17517, #7326, #5616 ) ;
#16990=CARTESIAN_POINT ( 'NONE',  ( 0.000000000000000000, 45.00825343885021113, 33.95787273855260935 ) ) ;
#16994=DIRECTION ( 'NONE',  ( 0.000000000000000000, 0.9510565162951545304, -0.3090169943749446202 ) ) ;
#16995=DIRECTION ( 'NONE',  ( 0.000000000000000000, 1.000000000000000000, 3.491481338843133355E-15 ) ) ;
#16997=LINE ( 'NONE', #15265, #11225 ) ;
#17002=VECTOR ( 'NONE', #14820, 1000.000000000000000 ) ;
#17005=CARTESIAN_POINT ( 'NONE',  ( 10.00000000000000000, 55.83748330407408389, -7.813799127873475747 ) ) ;
#17008=DIRECTION ( 'NONE',  ( -1.000000000000000000, 0.000000000000000000, -0.000000000000000000 ) ) ;
#17016=CARTESIAN_POINT ( 'NONE',  ( -10.00000000000000000, 0.000000000000000000, 0.000000000000000000 ) ) ;
#17017=CIRCLE ( 'NONE', #1195, 63.00000000006298961 ) ;
#17018=UNCERTAINTY_MEASURE_WITH_UNIT (LENGTH_MEASURE( 1.000000000000000082E-05 ), #2840, 'distance_accuracy_value', 'NONE');
#17022=DIRECTION ( 'NONE',  ( -1.000000000000000000, 0.000000000000000000, -0.000000000000000000 ) ) ;
#17025=EDGE_LOOP ( 'NONE', ( #16411, #12595, #5516, #16424 ) ) ;
#17031=AXIS2_PLACEMENT_3D ( 'NONE', #17726, #3255, #16403 ) ;
#17033=EDGE_CURVE ( 'NONE', #10536, #3234, #12795, .T. ) ;
#17034=DIRECTION ( 'NONE',  ( 0.000000000000000000, 0.9510565162951521989, 0.3090169943749515036 ) ) ;
#17040=ORIENTED_EDGE ( 'NONE', *, *, #3612, .T. ) ;
#17045=EDGE_LOOP ( 'NONE', ( #17643, #4460, #3212, #9240 ) ) ;
#17057=CARTESIAN_POINT ( 'NONE',  ( 0.000000000000000000, 53.06836994729258805, -18.64666490672316712 ) ) ;
#17059=EDGE_CURVE ( 'NONE', #18246, #2561, #12983, .T. ) ;
#17061=EDGE_CURVE ( 'NONE', #17928, #16109, #14491, .T. ) ;
#17063=EDGE_CURVE ( 'NONE', #5694, #7722, #17541, .T. ) ;
#17064=ORIENTED_EDGE ( 'NONE', *, *, #8580, .F. ) ;
#17065=CARTESIAN_POINT ( 'NONE',  ( 10.00000000000000000, 53.29895248911700634, -18.38754094778185788 ) ) ;
#17066=DIRECTION ( 'NONE',  ( 0.000000000000000000, 0.000000000000000000, 1.000000000000000000 ) ) ;
#17067=DIRECTION ( 'NONE',  ( 0.000000000000000000, 0.3090169943749480619, -0.9510565162951533091 ) ) ;
#17070=CYLINDRICAL_SURFACE ( 'NONE', #11818, 2.649999999999999467 ) ;
#17072=LINE ( 'NONE', #4104, #3848 ) ;
#17073=VERTEX_POINT ( 'NONE', #15839 ) ;
#17075=VECTOR ( 'NONE', #5592, 1000.000000000000000 ) ;
#17076=DIRECTION ( 'NONE',  ( 0.000000000000000000, 0.000000000000000000, 1.000000000000000000 ) ) ;
#17082=ORIENTED_EDGE ( 'NONE', *, *, #5281, .F. ) ;
#17087=DIRECTION ( 'NONE',  ( -1.000000000000000000, -0.000000000000000000, -0.000000000000000000 ) ) ;
#17095=CARTESIAN_POINT ( 'NONE',  ( 0.000000000000000000, -16.10733642026522006, 53.89344778774805889 ) ) ;
#17104=CARTESIAN_POINT ( 'NONE',  ( 5.000000000000000000, 41.62350880771986539, -47.29147401531912465 ) ) ;
#17112=CARTESIAN_POINT ( 'NONE',  ( 10.00000000000000000, -49.76630880786327538, 26.49895292617986797 ) ) ;
#17118=ORIENTED_EDGE ( 'NONE', *, *, #15067, .F. ) ;
#17120=EDGE_CURVE ( 'NONE', #7406, #12720, #4675, .T. ) ;
#17123=VECTOR ( 'NONE', #9982, 1000.000000000000000 ) ;
#17129=VERTEX_POINT ( 'NONE', #4865 ) ;
#17132=DIRECTION ( 'NONE',  ( -1.000000000000000000, 0.000000000000000000, 0.000000000000000000 ) ) ;
#17136=DIRECTION ( 'NONE',  ( 0.000000000000000000, 0.000000000000000000, 1.000000000000000000 ) ) ;
#17139=VERTEX_POINT ( 'NONE', #209 ) ;
#17141=CIRCLE ( 'NONE', #4057, 63.00000000006298961 ) ;
#17145=CIRCLE ( 'NONE', #13177, 24.00000000002399858 ) ;
#17146=ORIENTED_EDGE ( 'NONE', *, *, #7016, .T. ) ;
#17148=ORIENTED_EDGE ( 'NONE', *, *, #15067, .T. ) ;
#17149=CARTESIAN_POINT ( 'NONE',  ( 10.00000000000000000, 39.14194549634421350, -40.58063702438301590 ) ) ;
#17150=DIRECTION ( 'NONE',  ( -1.000000000000000000, -0.000000000000000000, -0.000000000000000000 ) ) ;
#17151=DIRECTION ( 'NONE',  ( 0.000000000000000000, 0.4539904997395412534, 0.8910065241883707854 ) ) ;
#17162=CARTESIAN_POINT ( 'NONE',  ( 4.999999999999999112, -32.11449294037157642, -54.20017844242546090 ) ) ;
#17165=ADVANCED_FACE ( 'NONE', ( #11912 ), #10394, .T. ) ;
#17166=VERTEX_POINT ( 'NONE', #4768 ) ;
#17168=DIRECTION ( 'NONE',  ( 0.000000000000000000, -0.1564344650402170467, -0.9876883405951398798 ) ) ;
#17171=ORIENTED_EDGE ( 'NONE', *, *, #7145, .T. ) ;
#17173=CARTESIAN_POINT ( 'NONE',  ( 5.000000000000000000, -4.007856633822952652, -62.87238730325625369 ) ) ;
#17181=CARTESIAN_POINT ( 'NONE',  ( 5.000000000000000000, -57.83923611457302627, -24.97244012287564274 ) ) ;
#17184=DIRECTION ( 'NONE',  ( 0.000000000000000000, 1.000000000000000000, 3.469446951950144779E-15 ) ) ;
#17186=CARTESIAN_POINT ( 'NONE',  ( 0.000000000000000000, 50.71018745830443919, 24.33982105418919417 ) ) ;
#17187=ORIENTED_EDGE ( 'NONE', *, *, #18177, .T. ) ;
#17189=EDGE_CURVE ( 'NONE', #14080, #16577, #17639, .T. ) ;
#17191=DIRECTION ( 'NONE',  ( 0.000000000000000000, 0.9876883405951382144, -0.1564344650402274828 ) ) ;
#17193=DIRECTION ( 'NONE',  ( -1.000000000000000000, -0.000000000000000000, -0.000000000000000000 ) ) ;
#17198=DIRECTION ( 'NONE',  ( -1.000000000000000000, 0.000000000000000000, -0.000000000000000000 ) ) ;
#17202=ORIENTED_EDGE ( 'NONE', *, *, #2281, .T. ) ;
#17205=ORIENTED_EDGE ( 'NONE', *, *, #12608, .T. ) ;
#17214=DIRECTION ( 'NONE',  ( -1.000000000000000000, 0.000000000000000000, 0.000000000000000000 ) ) ;
#17215=ORIENTED_EDGE ( 'NONE', *, *, #16589, .F. ) ;
#17220=CARTESIAN_POINT ( 'NONE',  ( 0.000000000000000000, -44.70888270294135936, -34.13306034420235591 ) ) ;
#17224=DIRECTION ( 'NONE',  ( 0.000000000000000000, 0.000000000000000000, 1.000000000000000000 ) ) ;
#17229=CARTESIAN_POINT ( 'NONE',  ( 10.00000000000000000, 58.55669782892461228, 23.24033432160457835 ) ) ;
#17233=CARTESIAN_POINT ( 'NONE',  ( 10.00000000000000000, 18.64666490672371424, 53.06836994729241042 ) ) ;
#17235=AXIS2_PLACEMENT_3D ( 'NONE', #15370, #8607, #17191 ) ;
#17236=AXIS2_PLACEMENT_3D ( 'NONE', #9391, #15293, #2240 ) ;
#17239=AXIS2_PLACEMENT_3D ( 'NONE', #8330, #4137, #14125 ) ;
#17242=VECTOR ( 'NONE', #304, 1000.000000000000000 ) ;
#17246=FACE_OUTER_BOUND ( 'NONE', #15525, .T. ) ;
#17248=FACE_BOUND ( 'NONE', #10107, .T. ) ;
#17255=LINE ( 'NONE', #17162, #18518 ) ;
#17259=CIRCLE ( 'NONE', #16025, 24.00000000002399858 ) ;
#17260=ORIENTED_EDGE ( 'NONE', *, *, #12735, .T. ) ;
#17266=EDGE_CURVE ( 'NONE', #15951, #12029, #17506, .T. ) ;
#17267=CYLINDRICAL_SURFACE ( 'NONE', #17365, 56.24900000005625600 ) ;
#17269=ORIENTED_EDGE ( 'NONE', *, *, #14389, .F. ) ;
#17284=DIRECTION ( 'NONE',  ( -1.000000000000000000, -0.000000000000000000, -0.000000000000000000 ) ) ;
#17292=AXIS2_PLACEMENT_3D ( 'NONE', #16017, #7343, #8588 ) ;
#17293=EDGE_CURVE ( 'NONE', #9928, #8389, #668, .T. ) ;
#17301=ORIENTED_EDGE ( 'NONE', *, *, #14797, .F. ) ;
#17309=ORIENTED_EDGE ( 'NONE', *, *, #18415, .F. ) ;
#17319=ORIENTED_EDGE ( 'NONE', *, *, #11917, .T. ) ;
#17321=ORIENTED_EDGE ( 'NONE', *, *, #18748, .F. ) ;
#17323=ORIENTED_EDGE ( 'NONE', *, *, #17120, .T. ) ;
#17324=DIRECTION ( 'NONE',  ( -1.000000000000000000, 0.000000000000000000, 0.000000000000000000 ) ) ;
#17330=VERTEX_POINT ( 'NONE', #10363 ) ;
#17334=ORIENTED_EDGE ( 'NONE', *, *, #10525, .F. ) ;
#17344=CARTESIAN_POINT ( 'NONE',  ( 0.000000000000000000, 7.813799127874054840, -55.83748330407399152 ) ) ;
#17353=VECTOR ( 'NONE', #4063, 1000.000000000000000 ) ;
#17361=CARTESIAN_POINT ( 'NONE',  ( 10.00000000000000178, 0.000000000000000000, 30.00000000000000000 ) ) ;
#17364=CARTESIAN_POINT ( 'NONE',  ( 10.00000000000000000, 7.478235706489787304, -55.74967257055874370 ) ) ;
#17365=AXIS2_PLACEMENT_3D ( 'NONE', #983, #18303, #4116 ) ;
#17367=CARTESIAN_POINT ( 'NONE',  ( 10.00000000000000000, 56.23315539212690339, 1.335003989221828835 ) ) ;
#17372=CYLINDRICAL_SURFACE ( 'NONE', #9540, 56.24900000005625600 ) ;
#17373=CARTESIAN_POINT ( 'NONE',  ( 10.00000000000000000, -24.97244012287460535, -57.83923611457345970 ) ) ;
#17374=ORIENTED_EDGE ( 'NONE', *, *, #1783, .F. ) ;
#17383=ORIENTED_EDGE ( 'NONE', *, *, #12963, .T. ) ;
#17384=AXIS2_PLACEMENT_3D ( 'NONE', #3024, #10347, #10249 ) ;
#17389=ORIENTED_EDGE ( 'NONE', *, *, #4086, .T. ) ;
#17390=EDGE_CURVE ( 'NONE', #16165, #16942, #18581, .T. ) ;
#17395=EDGE_CURVE ( 'NONE', #484, #10707, #13461, .T. ) ;
#17398=EDGE_CURVE ( 'NONE', #657, #1081, #15437, .T. ) ;
#17399=CARTESIAN_POINT ( 'NONE',  ( 10.00000000000000000, 0.000000000000000000, 0.000000000000000000 ) ) ;
#17400=CIRCLE ( 'NONE', #3406, 56.24900000005625600 ) ;
#17401=CARTESIAN_POINT ( 'NONE',  ( 5.000000000000000000, 40.19788616105680035, -48.50907078259338334 ) ) ;
#17402=ORIENTED_EDGE ( 'NONE', *, *, #7041, .F. ) ;
#17404=ORIENTED_EDGE ( 'NONE', *, *, #6778, .T. ) ;
#17405=CARTESIAN_POINT ( 'NONE',  ( 10.00000000000000000, -18.38754094778203552, -53.29895248911694239 ) ) ;
#17414=DIRECTION ( 'NONE',  ( 0.000000000000000000, 0.3090169943749481174, -0.9510565162951533091 ) ) ;
#17415=ORIENTED_EDGE ( 'NONE', *, *, #717, .T. ) ;
#17416=DIRECTION ( 'NONE',  ( -1.000000000000000000, 0.000000000000000000, 0.000000000000000000 ) ) ;
#17420=ORIENTED_EDGE ( 'NONE', *, *, #5272, .T. ) ;
#17422=ORIENTED_EDGE ( 'NONE', *, *, #10084, .T. ) ;
#17423=CARTESIAN_POINT ( 'NONE',  ( 0.000000000000000000, 0.000000000000000000, 0.000000000000000000 ) ) ;
#17425=CARTESIAN_POINT ( 'NONE',  ( 10.00000000000000000, 0.000000000000000000, 0.000000000000000000 ) ) ;
#17429=DIRECTION ( 'NONE',  ( 0.000000000000000000, -0.4539904997395542430, 0.8910065241883641241 ) ) ;
#17431=DIRECTION ( 'NONE',  ( 0.000000000000000000, 0.000000000000000000, -1.000000000000000000 ) ) ;
#17435=CARTESIAN_POINT ( 'NONE',  ( 0.000000000000000000, 0.000000000000000000, 0.000000000000000000 ) ) ;
#17436=ORIENTED_EDGE ( 'NONE', *, *, #10063, .T. ) ;
#17439=ADVANCED_FACE ( 'NONE', ( #14382 ), #1254, .T. ) ;
#17440=VECTOR ( 'NONE', #18428, 1000.000000000000000 ) ;
#17442=ORIENTED_EDGE ( 'NONE', *, *, #18560, .T. ) ;
#17444=CARTESIAN_POINT ( 'NONE',  ( 10.00000000000000000, 39.14194549634364506, 40.58063702438359144 ) ) ;
#17446=FACE_OUTER_BOUND ( 'NONE', #9871, .T. ) ;
#17447=CARTESIAN_POINT ( 'NONE',  ( 0.000000000000000000, -18.38754094778203552, -53.29895248911694239 ) ) ;
#17448=DIRECTION ( 'NONE',  ( 0.000000000000000000, 0.000000000000000000, 1.000000000000000000 ) ) ;
#17452=DIRECTION ( 'NONE',  ( -1.000000000000000000, 0.000000000000000000, 0.000000000000000000 ) ) ;
#17455=VECTOR ( 'NONE', #11667, 1000.000000000000000 ) ;
#17460=ADVANCED_FACE ( 'NONE', ( #14007 ), #11139, .T. ) ;
#17461=ORIENTED_EDGE ( 'NONE', *, *, #5520, .F. ) ;
#17462=AXIS2_PLACEMENT_3D ( 'NONE', #10976, #15358, #2313 ) ;
#17463=LINE ( 'NONE', #5569, #13568 ) ;
#17464=CARTESIAN_POINT ( 'NONE',  ( 10.00000000000000000, -50.71018745830461683, 24.33982105418882469 ) ) ;
#17465=DIRECTION ( 'NONE',  ( 0.000000000000000000, 0.7071067811865440200, 0.7071067811865511255 ) ) ;
#17466=FACE_OUTER_BOUND ( 'NONE', #16412, .T. ) ;
#17467=FACE_OUTER_BOUND ( 'NONE', #1633, .T. ) ;
#17468=CARTESIAN_POINT ( 'NONE',  ( 10.00000000000000000, 0.000000000000000000, 0.000000000000000000 ) ) ;
#17477=ORIENTED_EDGE ( 'NONE', *, *, #12203, .F. ) ;
#17488=VERTEX_POINT ( 'NONE', #968 ) ;
#17492=ORIENTED_EDGE ( 'NONE', *, *, #4286, .F. ) ;
#17501=CARTESIAN_POINT ( 'NONE',  ( 0.000000000000000000, 5.876895005582427167, 62.72529079327809853 ) ) ;
#17506=LINE ( 'NONE', #11524, #11909 ) ;
#17507=ORIENTED_EDGE ( 'NONE', *, *, #16547, .F. ) ;
#17510=AXIS2_PLACEMENT_3D ( 'NONE', #1116, #13971, #8348 ) ;
#17513=CARTESIAN_POINT ( 'NONE',  ( 10.00000000000000000, -9.823366686501049827, 55.51919907100648999 ) ) ;
#17516=DIRECTION ( 'NONE',  ( 0.000000000000000000, -0.8910065241883722287, 0.4539904997395383668 ) ) ;
#17517=CARTESIAN_POINT ( 'NONE',  ( 10.00000000000000000, 0.000000000000000000, 0.000000000000000000 ) ) ;
#17521=ORIENTED_EDGE ( 'NONE', *, *, #9059, .T. ) ;
#17522=CARTESIAN_POINT ( 'NONE',  ( 10.00000000000000000, 9.823366686500662581, 55.51919907100656104 ) ) ;
#17523=AXIS2_PLACEMENT_3D ( 'NONE', #10672, #6678, #5146 ) ;
#17524=ADVANCED_FACE ( 'NONE', ( #10097 ), #13231, .T. ) ;
#17528=DIRECTION ( 'NONE',  ( -1.000000000000000000, 0.000000000000000000, -0.000000000000000000 ) ) ;
#17537=CARTESIAN_POINT ( 'NONE',  ( 0.000000000000000000, -40.70683587897985234, 38.81885513159974010 ) ) ;
#17539=CARTESIAN_POINT ( 'NONE',  ( 0.000000000000000000, 16.10733642026482570, 53.89344778774818678 ) ) ;
#17540=DIRECTION ( 'NONE',  ( -1.000000000000000000, 0.000000000000000000, 0.000000000000000000 ) ) ;
#17541=LINE ( 'NONE', #13078, #13134 ) ;
#17544=ORIENTED_EDGE ( 'NONE', *, *, #18358, .F. ) ;
#17547=EDGE_CURVE ( 'NONE', #8173, #16278, #12954, .T. ) ;
#17552=VECTOR ( 'NONE', #16673, 1000.000000000000000 ) ;
#17554=ORIENTED_EDGE ( 'NONE', *, *, #14651, .T. ) ;
#17556=CIRCLE ( 'NONE', #12998, 24.00000000002399148 ) ;
#17560=CIRCLE ( 'NONE', #11494, 24.00000000002399858 ) ;
#17561=AXIS2_PLACEMENT_3D ( 'NONE', #11110, #2454, #12547 ) ;
#17565=CARTESIAN_POINT ( 'NONE',  ( 10.00000000000000000, 0.000000000000000000, 0.000000000000000000 ) ) ;
#17566=CARTESIAN_POINT ( 'NONE',  ( -10.00000000000000000, 0.000000000000000000, 0.000000000000000000 ) ) ;
#17568=EDGE_LOOP ( 'NONE', ( #8593, #12986, #17762, #15374 ) ) ;
#17573=ORIENTED_EDGE ( 'NONE', *, *, #7511, .T. ) ;
#17574=DIRECTION ( 'NONE',  ( 0.000000000000000000, -0.8910065241883626808, -0.4539904997395571296 ) ) ;
#17580=ADVANCED_FACE ( 'NONE', ( #189 ), #5988, .T. ) ;
#17582=DIRECTION ( 'NONE',  ( -1.000000000000000000, -0.000000000000000000, -0.000000000000000000 ) ) ;
#17583=DIRECTION ( 'NONE',  ( 0.000000000000000000, 0.000000000000000000, 1.000000000000000000 ) ) ;
#17585=CARTESIAN_POINT ( 'NONE',  ( 10.00000000000000000, 53.22058882792196499, 33.71303790549294632 ) ) ;
#17592=CARTESIAN_POINT ( 'NONE',  ( 5.000000000000000000, -53.22058882792172341, -33.71303790549333712 ) ) ;
#17594=ORIENTED_EDGE ( 'NONE', *, *, #9778, .F. ) ;
#17595=ORIENTED_EDGE ( 'NONE', *, *, #1120, .F. ) ;
#17597=VERTEX_POINT ( 'NONE', #6085 ) ;
#17599=EDGE_CURVE ( 'NONE', #16028, #10905, #11627, .T. ) ;
#17608=DIRECTION ( 'NONE',  ( -1.000000000000000000, -0.000000000000000000, -0.000000000000000000 ) ) ;
#17609=CARTESIAN_POINT ( 'NONE',  ( 10.00000000000000000, -26.45033635316118747, 36.40576474687271258 ) ) ;
#17610=CARTESIAN_POINT ( 'NONE',  ( 10.00000000000000000, 53.89344778774834310, -16.10733642026427148 ) ) ;
#17612=CARTESIAN_POINT ( 'NONE',  ( 10.00000000000000000, 49.76630880786309064, 26.49895292618021614 ) ) ;
#17614=EDGE_CURVE ( 'NONE', #11942, #607, #5840, .T. ) ;
#17615=DIRECTION ( 'NONE',  ( 0.000000000000000000, 0.000000000000000000, 1.000000000000000000 ) ) ;
#17621=EDGE_LOOP ( 'NONE', ( #14603, #2198, #7311, #8790 ) ) ;
#17628=ADVANCED_FACE ( 'NONE', ( #14746 ), #4294, .T. ) ;
#17632=DIRECTION ( 'NONE',  ( 0.000000000000000000, 0.000000000000000000, 1.000000000000000000 ) ) ;
#17633=ORIENTED_EDGE ( 'NONE', *, *, #5026, .F. ) ;
#17636=EDGE_CURVE ( 'NONE', #2561, #16544, #10130, .T. ) ;
#17637=CARTESIAN_POINT ( 'NONE',  ( 10.00000000000000000, -50.71018745830461683, 24.33982105418882469 ) ) ;
#17639=LINE ( 'NONE', #16488, #1577 ) ;
#17643=ORIENTED_EDGE ( 'NONE', *, *, #12889, .T. ) ;
#17646=ORIENTED_EDGE ( 'NONE', *, *, #14936, .T. ) ;
#17647=ADVANCED_FACE ( 'NONE', ( #7327 ), #101, .T. ) ;
#17650=ORIENTED_EDGE ( 'NONE', *, *, #18677, .T. ) ;
#17652=APPLICATION_CONTEXT ( 'automotive_design' ) ;
#17653=EDGE_CURVE ( 'NONE', #4800, #701, #5898, .T. ) ;
#17654=( GEOMETRIC_REPRESENTATION_CONTEXT ( 3 ) GLOBAL_UNCERTAINTY_ASSIGNED_CONTEXT ( ( #632 ) ) GLOBAL_UNIT_ASSIGNED_CONTEXT ( ( #16986, #9737, #12787 ) ) REPRESENTATION_CONTEXT ( 'NONE', 'WORKASPACE' ) );
#17657=CARTESIAN_POINT ( 'NONE',  ( -10.00000000000000000, 0.000000000000000000, 0.000000000000000000 ) ) ;
#17659=CARTESIAN_POINT ( 'NONE',  ( 10.00000000000000000, 38.81885513159988932, 40.70683587897971734 ) ) ;
#17661=DIRECTION ( 'NONE',  ( -1.000000000000000000, -0.000000000000000000, 0.000000000000000000 ) ) ;
#17669=FACE_OUTER_BOUND ( 'NONE', #5092, .T. ) ;
#17674=CARTESIAN_POINT ( 'NONE',  ( 0.000000000000000000, 58.55669782892493203, -23.24033432160376478 ) ) ;
#17676=CARTESIAN_POINT ( 'NONE',  ( 4.999999999999999112, -61.03368945066424800, -15.61693798565561409 ) ) ;
#17677=ORIENTED_EDGE ( 'NONE', *, *, #16808, .F. ) ;
#17679=AXIS2_PLACEMENT_3D ( 'NONE', #12048, #13492, #16441 ) ;
#17680=ORIENTED_EDGE ( 'NONE', *, *, #3460, .T. ) ;
#17681=CARTESIAN_POINT ( 'NONE',  ( -10.00000000000000000, 0.000000000000000000, 0.000000000000000000 ) ) ;
#17683=DIRECTION ( 'NONE',  ( -1.000000000000000000, 0.000000000000000000, -0.000000000000000000 ) ) ;
#17686=VERTEX_POINT ( 'NONE', #6175 ) ;
#17688=DIRECTION ( 'NONE',  ( -1.000000000000000000, 0.000000000000000000, 0.000000000000000000 ) ) ;
#17691=CIRCLE ( 'NONE', #9475, 63.00000000006298961 ) ;
#17693=DIRECTION ( 'NONE',  ( -1.000000000000000000, -0.000000000000000000, 0.000000000000000000 ) ) ;
#17697=DIRECTION ( 'NONE',  ( -1.000000000000000000, -0.000000000000000000, -0.000000000000000000 ) ) ;
#17698=DIRECTION ( 'NONE',  ( -1.000000000000000000, 0.000000000000000000, -0.000000000000000000 ) ) ;
#17701=CARTESIAN_POINT ( 'NONE',  ( 0.000000000000000000, -5.117658387065794099E-13, -47.64999999999999858 ) ) ;
#17707=DIRECTION ( 'NONE',  ( 0.000000000000000000, 0.000000000000000000, 1.000000000000000000 ) ) ;
#17710=DIRECTION ( 'NONE',  ( -1.000000000000000000, 0.000000000000000000, 0.000000000000000000 ) ) ;
#17712=VERTEX_POINT ( 'NONE', #17791 ) ;
#17714=DIRECTION ( 'NONE',  ( -1.000000000000000000, 0.000000000000000000, -0.000000000000000000 ) ) ;
#17715=AXIS2_PLACEMENT_3D ( 'NONE', #8406, #18221, #6601 ) ;
#17720=ADVANCED_FACE ( 'NONE', ( #13515 ), #4745, .T. ) ;
#17721=ADVANCED_FACE ( 'NONE', ( #10739 ), #15036, .T. ) ;
#17726=CARTESIAN_POINT ( 'NONE',  ( 10.00000000000000000, -45.00825343884996954, -33.95787273855293620 ) ) ;
#17729=DIRECTION ( 'NONE',  ( 0.000000000000000000, 0.3090169943749411785, 0.9510565162951556406 ) ) ;
#17735=VERTEX_POINT ( 'NONE', #7787 ) ;
#17737=EDGE_LOOP ( 'NONE', ( #18765, #14455, #5409, #5136 ) ) ;
#17740=DIRECTION ( 'NONE',  ( -1.000000000000000000, -0.000000000000000000, 0.000000000000000000 ) ) ;
#17744=CARTESIAN_POINT ( 'NONE',  ( 5.000000000000000000, 23.24033432160521784, -58.55669782892436359 ) ) ;
#17746=LINE ( 'NONE', #1933, #5640 ) ;
#17757=DIRECTION ( 'NONE',  ( 0.000000000000000000, 0.000000000000000000, 1.000000000000000000 ) ) ;
#17759=DIRECTION ( 'NONE',  ( 1.000000000000000000, -0.000000000000000000, -0.000000000000000000 ) ) ;
#17762=ORIENTED_EDGE ( 'NONE', *, *, #12078, .F. ) ;
#17763=DIRECTION ( 'NONE',  ( -1.000000000000000000, -0.000000000000000000, -0.000000000000000000 ) ) ;
#17770=EDGE_LOOP ( 'NONE', ( #3797, #14104, #13543, #12071 ) ) ;
#17772=ADVANCED_FACE ( 'NONE', ( #6463 ), #12269, .T. ) ;
#17773=CARTESIAN_POINT ( 'NONE',  ( 10.00000000000000000, 0.000000000000000000, 56.24900000005625600 ) ) ;
#17779=VECTOR ( 'NONE', #18582, 1000.000000000000000 ) ;
#17786=CARTESIAN_POINT ( 'NONE',  ( 0.000000000000000000, -26.45033635316118747, 36.40576474687271258 ) ) ;
#17787=ORIENTED_EDGE ( 'NONE', *, *, #8474, .F. ) ;
#17789=ADVANCED_FACE ( 'NONE', ( #10932 ), #16756, .T. ) ;
#17791=CARTESIAN_POINT ( 'NONE',  ( 0.000000000000000000, -34.13306034420152457, -44.70888270294198463 ) ) ;
#17792=CARTESIAN_POINT ( 'NONE',  ( 0.000000000000000000, 18.38754094778241210, 53.29895248911682870 ) ) ;
#17793=VERTEX_POINT ( 'NONE', #12649 ) ;
#17794=DIRECTION ( 'NONE',  ( 0.000000000000000000, 0.8910065241883656784, 0.4539904997395510788 ) ) ;
#17795=CARTESIAN_POINT ( 'NONE',  ( 0.000000000000000000, -53.06836994729219725, -18.64666490672428623 ) ) ;
#17797=ORIENTED_EDGE ( 'NONE', *, *, #14074, .F. ) ;
#17799=DIRECTION ( 'NONE',  ( -1.000000000000000000, -0.000000000000000000, 0.000000000000000000 ) ) ;
#17800=AXIS2_PLACEMENT_3D ( 'NONE', #18160, #15499, #9779 ) ;
#17801=AXIS2_PLACEMENT_3D ( 'NONE', #11310, #12646, #2261 ) ;
#17802=AXIS2_PLACEMENT_3D ( 'NONE', #15299, #7963, #3689 ) ;
#17805=CIRCLE ( 'NONE', #11427, 56.24900000005627021 ) ;
#17806=ORIENTED_EDGE ( 'NONE', *, *, #2583, .T. ) ;
#17810=CARTESIAN_POINT ( 'NONE',  ( 10.00000000000000000, 0.000000000000000000, 0.000000000000000000 ) ) ;
#17815=ORIENTED_EDGE ( 'NONE', *, *, #12861, .T. ) ;
#17819=AXIS2_PLACEMENT_3D ( 'NONE', #3569, #3929, #17943 ) ;
#17823=AXIS2_PLACEMENT_3D ( 'NONE', #7761, #17683, #8914 ) ;
#17827=VERTEX_POINT ( 'NONE', #15417 ) ;
#17828=ORIENTED_EDGE ( 'NONE', *, *, #896, .F. ) ;
#17829=DIRECTION ( 'NONE',  ( 0.000000000000000000, 0.000000000000000000, -1.000000000000000000 ) ) ;
#17832=CIRCLE ( 'NONE', #14785, 30.00000000000000000 ) ;
#17834=DIRECTION ( 'NONE',  ( -1.000000000000000000, 0.000000000000000000, 0.000000000000000000 ) ) ;
#17835=ADVANCED_FACE ( 'NONE', ( #13991 ), #8078, .T. ) ;
#17836=CIRCLE ( 'NONE', #11769, 24.00000000002399858 ) ;
#17839=CIRCLE ( 'NONE', #7194, 24.00000000002399858 ) ;
#17840=DIRECTION ( 'NONE',  ( -1.000000000000000000, 0.000000000000000000, -0.000000000000000000 ) ) ;
#17842=CARTESIAN_POINT ( 'NONE',  ( 10.00000000000000000, -42.79754323328189969, -11.25576474687263229 ) ) ;
#17843=ORIENTED_EDGE ( 'NONE', *, *, #11679, .F. ) ;
#17845=EDGE_CURVE ( 'NONE', #16942, #7722, #5245, .T. ) ;
#17857=EDGE_CURVE ( 'NONE', #6557, #12264, #2551, .T. ) ;
#17858=AXIS2_PLACEMENT_3D ( 'NONE', #11724, #1714, #18063 ) ;
#17860=CARTESIAN_POINT ( 'NONE',  ( 10.00000000000000000, 55.83748330407408389, -7.813799127873475747 ) ) ;
#17863=CARTESIAN_POINT ( 'NONE',  ( 0.000000000000000000, 0.000000000000000000, 0.000000000000000000 ) ) ;
#17866=CARTESIAN_POINT ( 'NONE',  ( 10.00000000000000000, 0.000000000000000000, 0.000000000000000000 ) ) ;
#17868=ORIENTED_EDGE ( 'NONE', *, *, #6779, .T. ) ;
#17873=FACE_OUTER_BOUND ( 'NONE', #7715, .T. ) ;
#17875=ORIENTED_EDGE ( 'NONE', *, *, #13687, .T. ) ;
#17876=ORIENTED_EDGE ( 'NONE', *, *, #1783, .T. ) ;
#17877=LINE ( 'NONE', #4547, #6594 ) ;
#17880=AXIS2_PLACEMENT_3D ( 'NONE', #17405, #9976, #9877 ) ;
#17881=CIRCLE ( 'NONE', #4216, 24.00000000002400569 ) ;
#17885=EDGE_CURVE ( 'NONE', #2652, #2958, #88, .T. ) ;
#17888=ORIENTED_EDGE ( 'NONE', *, *, #13067, .F. ) ;
#17889=CARTESIAN_POINT ( 'NONE',  ( 10.00000000000000000, 7.478235706488965739, 55.74967257055886449 ) ) ;
#17890=CARTESIAN_POINT ( 'NONE',  ( 10.00000000000000000, 32.11449294037269198, -54.20017844242477878 ) ) ;
#17895=CARTESIAN_POINT ( 'NONE',  ( 10.00000000000000000, 9.823366686500662581, 55.51919907100656104 ) ) ;
#17898=EDGE_LOOP ( 'NONE', ( #16948, #7680, #4428, #13785 ) ) ;
#17901=EDGE_LOOP ( 'NONE', ( #8997, #11615 ) ) ;
#17905=AXIS2_PLACEMENT_3D ( 'NONE', #3706, #6746, #8077 ) ;
#17906=VECTOR ( 'NONE', #9545, 1000.000000000000000 ) ;
#17913=AXIS2_PLACEMENT_3D ( 'NONE', #5600, #2749, #4442 ) ;
#17915=DIRECTION ( 'NONE',  ( -1.000000000000000000, 0.000000000000000000, 0.000000000000000000 ) ) ;
#17924=ADVANCED_FACE ( 'NONE', ( #2650 ), #1138, .T. ) ;
#17925=VECTOR ( 'NONE', #16558, 1000.000000000000000 ) ;
#17926=ORIENTED_EDGE ( 'NONE', *, *, #1120, .T. ) ;
#17928=VERTEX_POINT ( 'NONE', #4543 ) ;
#17938=DIRECTION ( 'NONE',  ( 0.000000000000000000, -0.7071067811865389130, -0.7071067811865561215 ) ) ;
#17941=ORIENTED_EDGE ( 'NONE', *, *, #16689, .T. ) ;
#17943=DIRECTION ( 'NONE',  ( 0.000000000000000000, 0.000000000000000000, 1.000000000000000000 ) ) ;
#17945=CARTESIAN_POINT ( 'NONE',  ( 0.000000000000000000, 0.000000000000000000, 0.000000000000000000 ) ) ;
#17946=ORIENTED_EDGE ( 'NONE', *, *, #50, .F. ) ;
#17948=DIRECTION ( 'NONE',  ( -1.000000000000000000, -0.000000000000000000, 0.000000000000000000 ) ) ;
#17950=CARTESIAN_POINT ( 'NONE',  ( 0.000000000000000000, 0.000000000000000000, 0.000000000000000000 ) ) ;
#17952=AXIS2_PLACEMENT_3D ( 'NONE', #1948, #13679, #2054 ) ;
#17955=DIRECTION ( 'NONE',  ( 0.000000000000000000, -0.5877852522924801315, 0.8090169943749421222 ) ) ;
#17960=CARTESIAN_POINT ( 'NONE',  ( 10.00000000000000000, -1.335003989221234200, -56.23315539212691760 ) ) ;
#17964=AXIS2_PLACEMENT_3D ( 'NONE', #5551, #2406, #8221 ) ;
#17967=FACE_OUTER_BOUND ( 'NONE', #665, .T. ) ;
#17971=EDGE_CURVE ( 'NONE', #5879, #5044, #16196, .T. ) ;
#17989=ORIENTED_EDGE ( 'NONE', *, *, #669, .T. ) ;
#17990=VECTOR ( 'NONE', #18421, 1000.000000000000000 ) ;
#17991=DIRECTION ( 'NONE',  ( -1.000000000000000000, 0.000000000000000000, 0.000000000000000000 ) ) ;
#17993=CARTESIAN_POINT ( 'NONE',  ( 10.00000000000000000, 44.70888270294211253, -34.13306034420136825 ) ) ;
#17995=ADVANCED_FACE ( 'NONE', ( #10076 ), #1678, .T. ) ;
#18005=ORIENTED_EDGE ( 'NONE', *, *, #4122, .T. ) ;
#18009=VERTEX_POINT ( 'NONE', #18735 ) ;
#18011=AXIS2_PLACEMENT_3D ( 'NONE', #9988, #15807, #4806 ) ;
#18012=ORIENTED_EDGE ( 'NONE', *, *, #11983, .F. ) ;
#18013=AXIS2_PLACEMENT_3D ( 'NONE', #13890, #4181, #8464 ) ;
#18019=DIRECTION ( 'NONE',  ( 0.000000000000000000, -0.8090169943749531134, 0.5877852522924653655 ) ) ;
#18021=CARTESIAN_POINT ( 'NONE',  ( 5.000000000000000000, -61.03368945066446827, 15.61693798565473656 ) ) ;
#18022=EDGE_CURVE ( 'NONE', #15880, #16509, #4652, .T. ) ;
#18025=DIRECTION ( 'NONE',  ( 1.000000000000000000, 0.000000000000000000, 0.000000000000000000 ) ) ;
#18026=ORIENTED_EDGE ( 'NONE', *, *, #13438, .T. ) ;
#18037=DIRECTION ( 'NONE',  ( 0.000000000000000000, 0.000000000000000000, 1.000000000000000000 ) ) ;
#18043=DIRECTION ( 'NONE',  ( 0.000000000000000000, 0.000000000000000000, 1.000000000000000000 ) ) ;
#18045=LINE ( 'NONE', #17676, #16354 ) ;
#18048=ORIENTED_EDGE ( 'NONE', *, *, #3166, .F. ) ;
#18050=ORIENTED_EDGE ( 'NONE', *, *, #13834, .T. ) ;
#18051=DIRECTION ( 'NONE',  ( -1.000000000000000000, -0.000000000000000000, 0.000000000000000000 ) ) ;
#18052=DIRECTION ( 'NONE',  ( -1.000000000000000000, -0.000000000000000000, -0.000000000000000000 ) ) ;
#18057=CIRCLE ( 'NONE', #14414, 24.00000000002399858 ) ;
#18063=DIRECTION ( 'NONE',  ( 0.000000000000000000, -0.7071067811865535679, 0.7071067811865414665 ) ) ;
#18066=ADVANCED_FACE ( 'NONE', ( #4997 ), #3491, .T. ) ;
#18082=CYLINDRICAL_SURFACE ( 'NONE', #3752, 24.00000000002399858 ) ;
#18085=EDGE_CURVE ( 'NONE', #10072, #6237, #16832, .T. ) ;
#18086=ADVANCED_FACE ( 'NONE', ( #17873 ), #3312, .T. ) ;
#18087=ORIENTED_EDGE ( 'NONE', *, *, #18132, .T. ) ;
#18090=CARTESIAN_POINT ( 'NONE',  ( 10.00000000000000000, -56.37237871411032586, -1.017308535512989609 ) ) ;
#18092=FACE_OUTER_BOUND ( 'NONE', #1961, .T. ) ;
#18093=ADVANCED_FACE ( 'NONE', ( #1869 ), #15212, .T. ) ;
#18096=CARTESIAN_POINT ( 'NONE',  ( 10.00000000000000000, 61.03368945066456064, -15.61693798565434399 ) ) ;
#18098=DIRECTION ( 'NONE',  ( -1.000000000000000000, 0.000000000000000000, 0.000000000000000000 ) ) ;
#18099=ORIENTED_EDGE ( 'NONE', *, *, #15790, .F. ) ;
#18102=CARTESIAN_POINT ( 'NONE',  ( 10.00000000000000000, 16.45250512421934630, -53.92768374110874419 ) ) ;
#18103=VERTEX_POINT ( 'NONE', #12157 ) ;
#18104=ORIENTED_EDGE ( 'NONE', *, *, #10869, .T. ) ;
#18108=EDGE_LOOP ( 'NONE', ( #7138, #13668, #5584, #12799 ) ) ;
#18111=DIRECTION ( 'NONE',  ( -1.000000000000000000, 0.000000000000000000, 0.000000000000000000 ) ) ;
#18112=ADVANCED_FACE ( 'NONE', ( #3210 ), #7669, .T. ) ;
#18113=CARTESIAN_POINT ( 'NONE',  ( 10.00000000000000000, -49.49802920186203892, -26.71881558261783951 ) ) ;
#18114=DIRECTION ( 'NONE',  ( -1.000000000000000000, 0.000000000000000000, 0.000000000000000000 ) ) ;
#18115=LINE ( 'NONE', #3370, #7818 ) ;
#18118=DIRECTION ( 'NONE',  ( -1.000000000000000000, 0.000000000000000000, 0.000000000000000000 ) ) ;
#18119=ORIENTED_EDGE ( 'NONE', *, *, #8913, .F. ) ;
#18126=VERTEX_POINT ( 'NONE', #10630 ) ;
#18130=DIRECTION ( 'NONE',  ( -1.000000000000000000, -0.000000000000000000, -0.000000000000000000 ) ) ;
#18132=EDGE_CURVE ( 'NONE', #17139, #4385, #99, .T. ) ;
#18133=AXIS2_PLACEMENT_3D ( 'NONE', #3475, #10510, #10699 ) ;
#18134=AXIS2_PLACEMENT_3D ( 'NONE', #17435, #4384, #2960 ) ;
#18135=ADVANCED_FACE ( 'NONE', ( #17967 ), #15018, .T. ) ;
#18140=DIRECTION ( 'NONE',  ( -1.000000000000000000, 0.000000000000000000, 0.000000000000000000 ) ) ;
#18145=VERTEX_POINT ( 'NONE', #9287 ) ;
#18152=CIRCLE ( 'NONE', #12681, 24.00000000002400569 ) ;
#18159=EDGE_CURVE ( 'NONE', #11786, #4356, #15579, .T. ) ;
#18160=CARTESIAN_POINT ( 'NONE',  ( 0.000000000000000000, 0.000000000000000000, 0.000000000000000000 ) ) ;
#18161=CIRCLE ( 'NONE', #13624, 2.649999999999999467 ) ;
#18166=ORIENTED_EDGE ( 'NONE', *, *, #12369, .T. ) ;
#18173=DIRECTION ( 'NONE',  ( -1.000000000000000000, 0.000000000000000000, -0.000000000000000000 ) ) ;
#18177=EDGE_CURVE ( 'NONE', #17129, #1734, #1921, .T. ) ;
#18179=ADVANCED_FACE ( 'NONE', ( #12622 ), #12530, .T. ) ;
#18181=CYLINDRICAL_SURFACE ( 'NONE', #15170, 2.649999999999999467 ) ;
#18182=CARTESIAN_POINT ( 'NONE',  ( 10.00000000000000000, -5.117658387065794099E-13, -47.64999999999999858 ) ) ;
#18185=AXIS2_PLACEMENT_3D ( 'NONE', #3367, #13554, #16224 ) ;
#18189=VERTEX_POINT ( 'NONE', #6909 ) ;
#18190=CARTESIAN_POINT ( 'NONE',  ( 10.00000000000000178, 0.000000000000000000, 0.000000000000000000 ) ) ;
#18193=CARTESIAN_POINT ( 'NONE',  ( 10.00000000000000000, 26.71881558261799228, -49.49802920186195365 ) ) ;
#18195=CARTESIAN_POINT ( 'NONE',  ( 0.000000000000000000, 0.000000000000000000, 0.000000000000000000 ) ) ;
#18199=DIRECTION ( 'NONE',  ( -1.000000000000000000, -0.000000000000000000, 0.000000000000000000 ) ) ;
#18200=EDGE_CURVE ( 'NONE', #9128, #16979, #17141, .T. ) ;
#18201=EDGE_CURVE ( 'NONE', #1691, #6509, #14687, .T. ) ;
#18202=EDGE_CURVE ( 'NONE', #5083, #6509, #15918, .T. ) ;
#18209=VERTEX_POINT ( 'NONE', #6632 ) ;
#18213=EDGE_CURVE ( 'NONE', #4773, #13137, #12441, .T. ) ;
#18218=DIRECTION ( 'NONE',  ( 1.000000000000000000, -0.000000000000000000, -0.000000000000000000 ) ) ;
#18221=DIRECTION ( 'NONE',  ( -1.000000000000000000, -0.000000000000000000, -0.000000000000000000 ) ) ;
#18224=CARTESIAN_POINT ( 'NONE',  ( 10.00000000000000000, 53.22058882792246237, -33.71303790549217183 ) ) ;
#18225=VERTEX_POINT ( 'NONE', #15294 ) ;
#18228=CYLINDRICAL_SURFACE ( 'NONE', #6185, 56.24900000005625600 ) ;
#18237=CIRCLE ( 'NONE', #15503, 56.24900000005625600 ) ;
#18243=FACE_OUTER_BOUND ( 'NONE', #14952, .T. ) ;
#18245=CARTESIAN_POINT ( 'NONE',  ( 10.00000000000000000, -18.64666490672335186, -53.06836994729252410 ) ) ;
#18246=VERTEX_POINT ( 'NONE', #5196 ) ;
#18250=VERTEX_POINT ( 'NONE', #1111 ) ;
#18252=DIRECTION ( 'NONE',  ( -1.000000000000000000, 0.000000000000000000, 0.000000000000000000 ) ) ;
#18257=ADVANCED_FACE ( 'NONE', ( #12724 ), #8049, .T. ) ;
#18263=EDGE_LOOP ( 'NONE', ( #6937, #16215, #10311, #6203 ) ) ;
#18278=CARTESIAN_POINT ( 'NONE',  ( 10.00000000000000000, 0.000000000000000000, 0.000000000000000000 ) ) ;
#18282=DIRECTION ( 'NONE',  ( 0.000000000000000000, 0.000000000000000000, 1.000000000000000000 ) ) ;
#18293=LINE ( 'NONE', #15540, #7995 ) ;
#18295=EDGE_LOOP ( 'NONE', ( #2848, #15967, #4914, #5957 ) ) ;
#18296=ORIENTED_EDGE ( 'NONE', *, *, #18656, .F. ) ;
#18299=ORIENTED_EDGE ( 'NONE', *, *, #4927, .F. ) ;
#18301=LINE ( 'NONE', #789, #18441 ) ;
#18302=EDGE_CURVE ( 'NONE', #18755, #12710, #927, .T. ) ;
#18303=DIRECTION ( 'NONE',  ( -1.000000000000000000, -0.000000000000000000, 0.000000000000000000 ) ) ;
#18307=EDGE_CURVE ( 'NONE', #11293, #8684, #9670, .T. ) ;
#18313=VERTEX_POINT ( 'NONE', #5935 ) ;
#18314=CARTESIAN_POINT ( 'NONE',  ( 10.00000000000000000, 50.69000562871642046, 24.68609584167177218 ) ) ;
#18318=DIRECTION ( 'NONE',  ( -1.000000000000000000, 0.000000000000000000, 0.000000000000000000 ) ) ;
#18320=VECTOR ( 'NONE', #14197, 1000.000000000000000 ) ;
#18322=VERTEX_POINT ( 'NONE', #11379 ) ;
#18326=CYLINDRICAL_SURFACE ( 'NONE', #5344, 24.00000000002399858 ) ;
#18329=CYLINDRICAL_SURFACE ( 'NONE', #12404, 2.649999999999999467 ) ;
#18331=AXIS2_PLACEMENT_3D ( 'NONE', #16937, #14700, #51 ) ;
#18334=VECTOR ( 'NONE', #16974, 1000.000000000000000 ) ;
#18339=CARTESIAN_POINT ( 'NONE',  ( 5.000000000000000000, -41.62350880771954564, 47.29147401531940886 ) ) ;
#18342=ORIENTED_EDGE ( 'NONE', *, *, #2199, .T. ) ;
#18350=VERTEX_POINT ( 'NONE', #16144 ) ;
#18352=ORIENTED_EDGE ( 'NONE', *, *, #3262, .T. ) ;
#18358=EDGE_CURVE ( 'NONE', #4317, #657, #11676, .T. ) ;
#18360=AXIS2_PLACEMENT_3D ( 'NONE', #13565, #16234, #15089 ) ;
#18361=DIRECTION ( 'NONE',  ( -1.000000000000000000, 0.000000000000000000, 0.000000000000000000 ) ) ;
#18362=DIRECTION ( 'NONE',  ( -1.000000000000000000, -0.000000000000000000, -0.000000000000000000 ) ) ;
#18363=VERTEX_POINT ( 'NONE', #58 ) ;
#18366=CARTESIAN_POINT ( 'NONE',  ( 10.00000000000000000, -18.64666490672335186, -53.06836994729252410 ) ) ;
#18368=EDGE_CURVE ( 'NONE', #2985, #18678, #3097, .T. ) ;
#18370=EDGE_CURVE ( 'NONE', #16606, #1536, #11048, .T. ) ;
#18372=CARTESIAN_POINT ( 'NONE',  ( 10.00000000000000000, 26.45033635316149301, 36.40576474687247099 ) ) ;
#18374=CYLINDRICAL_SURFACE ( 'NONE', #6284, 24.00000000002399858 ) ;
#18380=CARTESIAN_POINT ( 'NONE',  ( 0.000000000000000000, -1.335003989221234200, -56.23315539212691760 ) ) ;
#18382=DIRECTION ( 'NONE',  ( -1.000000000000000000, 0.000000000000000000, 0.000000000000000000 ) ) ;
#18386=ORIENTED_EDGE ( 'NONE', *, *, #10693, .F. ) ;
#18390=AXIS2_PLACEMENT_3D ( 'NONE', #3979, #4071, #5296 ) ;
#18391=LINE ( 'NONE', #12589, #7865 ) ;
#18393=CARTESIAN_POINT ( 'NONE',  ( 10.00000000000000000, 0.000000000000000000, 0.000000000000000000 ) ) ;
#18394=DIRECTION ( 'NONE',  ( -1.000000000000000000, 0.000000000000000000, -0.000000000000000000 ) ) ;
#18395=CARTESIAN_POINT ( 'NONE',  ( 0.000000000000000000, 0.000000000000000000, 0.000000000000000000 ) ) ;
#18396=CARTESIAN_POINT ( 'NONE',  ( 0.000000000000000000, 0.000000000000000000, 0.000000000000000000 ) ) ;
#18398=ORIENTED_EDGE ( 'NONE', *, *, #7857, .F. ) ;
#18399=CARTESIAN_POINT ( 'NONE',  ( 10.00000000000000000, 46.27827401617404490, 31.97297851452441364 ) ) ;
#18409=AXIS2_PLACEMENT_3D ( 'NONE', #6712, #16612, #715 ) ;
#18410=DIRECTION ( 'NONE',  ( -1.000000000000000000, -0.000000000000000000, -0.000000000000000000 ) ) ;
#18414=VECTOR ( 'NONE', #17324, 1000.000000000000000 ) ;
#18415=EDGE_CURVE ( 'NONE', #11571, #13362, #14698, .T. ) ;
#18417=DIRECTION ( 'NONE',  ( -1.000000000000000000, 0.000000000000000000, -0.000000000000000000 ) ) ;
#18421=DIRECTION ( 'NONE',  ( -1.000000000000000000, 0.000000000000000000, 0.000000000000000000 ) ) ;
#18423=CIRCLE ( 'NONE', #1412, 24.00000000002399858 ) ;
#18424=CARTESIAN_POINT ( 'NONE',  ( 10.00000000000000000, 0.000000000000000000, 0.000000000000000000 ) ) ;
#18428=DIRECTION ( 'NONE',  ( -1.000000000000000000, 0.000000000000000000, 0.000000000000000000 ) ) ;
#18430=ORIENTED_EDGE ( 'NONE', *, *, #4590, .F. ) ;
#18433=CARTESIAN_POINT ( 'NONE',  ( 0.000000000000000000, -55.51919907100644735, -9.823366686501268319 ) ) ;
#18437=AXIS2_PLACEMENT_3D ( 'NONE', #7374, #4528, #10337 ) ;
#18438=CIRCLE ( 'NONE', #7770, 24.00000000002399858 ) ;
#18439=AXIS2_PLACEMENT_3D ( 'NONE', #4312, #3249, #4582 ) ;
#18440=EDGE_CURVE ( 'NONE', #1108, #6670, #11485, .T. ) ;
#18441=VECTOR ( 'NONE', #10768, 1000.000000000000000 ) ;
#18445=DIRECTION ( 'NONE',  ( 0.000000000000000000, -0.7071067811865535679, 0.7071067811865414665 ) ) ;
#18450=ORIENTED_EDGE ( 'NONE', *, *, #111, .F. ) ;
#18458=CIRCLE ( 'NONE', #18753, 63.00000000006298961 ) ;
#18459=CARTESIAN_POINT ( 'NONE',  ( 10.00000000000000000, 49.49802920186260735, -26.71881558261677370 ) ) ;
#18460=DIRECTION ( 'NONE',  ( 1.000000000000000000, 0.000000000000000000, 0.000000000000000000 ) ) ;
#18461=AXIS2_PLACEMENT_3D ( 'NONE', #5206, #12741, #18445 ) ;
#18464=CIRCLE ( 'NONE', #7195, 24.00000000002399858 ) ;
#18468=CARTESIAN_POINT ( 'NONE',  ( 0.000000000000000000, -33.71303790549312396, 53.22058882792185841 ) ) ;
#18469=LINE ( 'NONE', #16953, #9163 ) ;
#18470=VECTOR ( 'NONE', #18394, 1000.000000000000000 ) ;
#18480=FACE_OUTER_BOUND ( 'NONE', #12512, .T. ) ;
#18492=ORIENTED_EDGE ( 'NONE', *, *, #3183, .T. ) ;
#18495=ORIENTED_EDGE ( 'NONE', *, *, #7511, .F. ) ;
#18498=CIRCLE ( 'NONE', #5112, 24.00000000002399858 ) ;
#18500=AXIS2_PLACEMENT_3D ( 'NONE', #8698, #4248, #16039 ) ;
#18503=CARTESIAN_POINT ( 'NONE',  ( 10.00000000000000000, -1.335003989222025123, 56.23315539212689629 ) ) ;
#18504=DIRECTION ( 'NONE',  ( 1.000000000000000000, -0.000000000000000000, -0.000000000000000000 ) ) ;
#18505=DIRECTION ( 'NONE',  ( 1.000000000000000000, 0.000000000000000000, 0.000000000000000000 ) ) ;
#18507=CARTESIAN_POINT ( 'NONE',  ( 10.00000000000000000, -9.823366686501049827, 55.51919907100648999 ) ) ;
#18509=CARTESIAN_POINT ( 'NONE',  ( 10.00000000000000000, 0.000000000000000000, 0.000000000000000000 ) ) ;
#18510=ORIENTED_EDGE ( 'NONE', *, *, #8556, .T. ) ;
#18511=EDGE_CURVE ( 'NONE', #11459, #9292, #4664, .T. ) ;
#18513=DIRECTION ( 'NONE',  ( 0.000000000000000000, 0.000000000000000000, 1.000000000000000000 ) ) ;
#18518=VECTOR ( 'NONE', #4108, 1000.000000000000000 ) ;
#18519=ADVANCED_FACE ( 'NONE', ( #3471 ), #2040, .T. ) ;
#18520=CARTESIAN_POINT ( 'NONE',  ( 0.000000000000000000, 0.000000000000000000, 0.000000000000000000 ) ) ;
#18521=VERTEX_POINT ( 'NONE', #14994 ) ;
#18522=AXIS2_PLACEMENT_3D ( 'NONE', #18782, #6980, #15836 ) ;
#18526=DIRECTION ( 'NONE',  ( 0.000000000000000000, 0.9876883405951383255, -0.1564344650402276493 ) ) ;
#18527=AXIS2_PLACEMENT_3D ( 'NONE', #6198, #16120, #1825 ) ;
#18529=FACE_OUTER_BOUND ( 'NONE', #15292, .T. ) ;
#18533=EDGE_LOOP ( 'NONE', ( #12748, #18087 ) ) ;
#18535=CARTESIAN_POINT ( 'NONE',  ( 10.00000000000000000, -39.14194549634336084, -40.58063702438384013 ) ) ;
#18536=CARTESIAN_POINT ( 'NONE',  ( 10.00000000000000000, 0.000000000000000000, 0.000000000000000000 ) ) ;
#18539=DIRECTION ( 'NONE',  ( -1.000000000000000000, 0.000000000000000000, 0.000000000000000000 ) ) ;
#18541=DIRECTION ( 'NONE',  ( -1.000000000000000000, -0.000000000000000000, 0.000000000000000000 ) ) ;
#18542=AXIS2_PLACEMENT_3D ( 'NONE', #16275, #16382, #13059 ) ;
#18543=EDGE_CURVE ( 'NONE', #11085, #4094, #13183, .T. ) ;
#18550=EDGE_CURVE ( 'NONE', #7064, #16165, #5587, .T. ) ;
#18551=CIRCLE ( 'NONE', #2120, 2.649999999999999467 ) ;
#18554=CARTESIAN_POINT ( 'NONE',  ( 4.999999999999999112, -61.47135697633788709, 13.79392154159114092 ) ) ;
#18556=ORIENTED_EDGE ( 'NONE', *, *, #3579, .F. ) ;
#18560=EDGE_CURVE ( 'NONE', #15930, #11128, #10781, .T. ) ;
#18561=FACE_OUTER_BOUND ( 'NONE', #1065, .T. ) ;
#18566=EDGE_CURVE ( 'NONE', #13852, #475, #15616, .T. ) ;
#18569=DIRECTION ( 'NONE',  ( -1.000000000000000000, -0.000000000000000000, 0.000000000000000000 ) ) ;
#18572=ORIENTED_EDGE ( 'NONE', *, *, #17120, .F. ) ;
#18575=DIRECTION ( 'NONE',  ( 0.000000000000000000, -0.9876883405951359940, -0.1564344650402419989 ) ) ;
#18576=CARTESIAN_POINT ( 'NONE',  ( -10.00000000000000000, 0.000000000000000000, 0.000000000000000000 ) ) ;
#18577=CARTESIAN_POINT ( 'NONE',  ( 10.00000000000000000, -33.95787273855277988, 45.00825343885009033 ) ) ;
#18578=FACE_BOUND ( 'NONE', #14889, .T. ) ;
#18581=LINE ( 'NONE', #1341, #18320 ) ;
#18582=DIRECTION ( 'NONE',  ( 1.000000000000000000, -0.000000000000000000, -0.000000000000000000 ) ) ;
#18589=DIRECTION ( 'NONE',  ( 0.000000000000000000, -0.3090169943749548898, 0.9510565162951511997 ) ) ;
#18593=DIRECTION ( 'NONE',  ( -1.000000000000000000, 0.000000000000000000, 0.000000000000000000 ) ) ;
#18598=CARTESIAN_POINT ( 'NONE',  ( 5.000000000000000000, 24.97244012287581327, -57.83923611457294101 ) ) ;
#18599=DIRECTION ( 'NONE',  ( -1.000000000000000000, 0.000000000000000000, 0.000000000000000000 ) ) ;
#18606=EDGE_LOOP ( 'NONE', ( #14666, #12247, #6430, #5193 ) ) ;
#18610=CARTESIAN_POINT ( 'NONE',  ( -10.00000000000000000, 0.000000000000000000, 0.000000000000000000 ) ) ;
#18612=CIRCLE ( 'NONE', #14351, 56.24900000005625600 ) ;
#18616=LINE ( 'NONE', #15856, #4809 ) ;
#18617=DIRECTION ( 'NONE',  ( -1.000000000000000000, -0.000000000000000000, -0.000000000000000000 ) ) ;
#18622=DIRECTION ( 'NONE',  ( 0.000000000000000000, 0.000000000000000000, 1.000000000000000000 ) ) ;
#18634=AXIS2_PLACEMENT_3D ( 'NONE', #14899, #699, #605 ) ;
#18638=ORIENTED_EDGE ( 'NONE', *, *, #12990, .T. ) ;
#18646=ORIENTED_EDGE ( 'NONE', *, *, #17547, .F. ) ;
#18650=VECTOR ( 'NONE', #3868, 1000.000000000000000 ) ;
#18652=CARTESIAN_POINT ( 'NONE',  ( 10.00000000000000000, 1.335003989222417697, -56.23315539212688918 ) ) ;
#18655=ADVANCED_FACE ( 'NONE', ( #3843 ), #18228, .T. ) ;
#18656=EDGE_CURVE ( 'NONE', #16471, #15168, #9843, .T. ) ;
#18660=ADVANCED_FACE ( 'NONE', ( #8233 ), #13835, .T. ) ;
#18661=CIRCLE ( 'NONE', #10442, 24.00000000002399858 ) ;
#18663=DIRECTION ( 'NONE',  ( 0.000000000000000000, -0.8910065241883626808, -0.4539904997395568520 ) ) ;
#18664=FACE_OUTER_BOUND ( 'NONE', #5577, .T. ) ;
#18665=CARTESIAN_POINT ( 'NONE',  ( 5.000000000000000000, -24.97244012287543669, 57.83923611457311154 ) ) ;
#18670=CARTESIAN_POINT ( 'NONE',  ( 10.00000000000000000, -26.49895292617967257, -49.76630880786338196 ) ) ;
#18671=ORIENTED_EDGE ( 'NONE', *, *, #3579, .T. ) ;
#18674=LINE ( 'NONE', #11629, #9384 ) ;
#18675=LINE ( 'NONE', #15338, #2524 ) ;
#18677=EDGE_CURVE ( 'NONE', #11098, #16951, #18661, .T. ) ;
#18678=VERTEX_POINT ( 'NONE', #8326 ) ;
#18681=EDGE_LOOP ( 'NONE', ( #18296, #27, #18005, #123 ) ) ;
#18684=DIRECTION ( 'NONE',  ( -1.000000000000000000, -0.000000000000000000, 0.000000000000000000 ) ) ;
#18687=CARTESIAN_POINT ( 'NONE',  ( 10.00000000000000000, 1.017308535513159695, -56.37237871411032586 ) ) ;
#18692=VERTEX_POINT ( 'NONE', #7933 ) ;
#18693=DIRECTION ( 'NONE',  ( 1.000000000000000000, 0.000000000000000000, 0.000000000000000000 ) ) ;
#18700=VERTEX_POINT ( 'NONE', #14122 ) ;
#18701=AXIS2_PLACEMENT_3D ( 'NONE', #16463, #14561, #10553 ) ;
#18704=DIRECTION ( 'NONE',  ( 1.000000000000000000, 0.000000000000000000, 0.000000000000000000 ) ) ;
#18705=FACE_OUTER_BOUND ( 'NONE', #2738, .T. ) ;
#18707=DIRECTION ( 'NONE',  ( -1.000000000000000000, 0.000000000000000000, 0.000000000000000000 ) ) ;
#18714=ORIENTED_EDGE ( 'NONE', *, *, #6787, .T. ) ;
#18716=ORIENTED_EDGE ( 'NONE', *, *, #3545, .F. ) ;
#18721=ADVANCED_FACE ( 'NONE', ( #13750 ), #10883, .T. ) ;
#18722=CIRCLE ( 'NONE', #8377, 56.24900000005624889 ) ;
#18733=ORIENTED_EDGE ( 'NONE', *, *, #7130, .F. ) ;
#18734=CARTESIAN_POINT ( 'NONE',  ( 10.00000000000000000, 50.69000562871642046, -24.68609584167177218 ) ) ;
#18735=CARTESIAN_POINT ( 'NONE',  ( 0.000000000000000000, 31.97297851452492168, -46.27827401617368963 ) ) ;
#18738=VERTEX_POINT ( 'NONE', #3662 ) ;
#18742=CIRCLE ( 'NONE', #15393, 2.649999999999999467 ) ;
#18745=AXIS2_PLACEMENT_3D ( 'NONE', #5186, #12322, #15479 ) ;
#18746=AXIS2_PLACEMENT_3D ( 'NONE', #14423, #7091, #4335 ) ;
#18748=EDGE_CURVE ( 'NONE', #79, #3360, #2869, .T. ) ;
#18750=AXIS2_PLACEMENT_3D ( 'NONE', #6993, #11366, #17184 ) ;
#18753=AXIS2_PLACEMENT_3D ( 'NONE', #16963, #3919, #7046 ) ;
#18754=CIRCLE ( 'NONE', #2327, 24.00000000002399503 ) ;
#18755=VERTEX_POINT ( 'NONE', #8131 ) ;
#18757=CIRCLE ( 'NONE', #1421, 24.00000000002399858 ) ;
#18759=DIRECTION ( 'NONE',  ( -1.000000000000000000, 0.000000000000000000, 0.000000000000000000 ) ) ;
#18761=EDGE_CURVE ( 'NONE', #11459, #18189, #18057, .T. ) ;
#18762=DIRECTION ( 'NONE',  ( -1.000000000000000000, -0.000000000000000000, 0.000000000000000000 ) ) ;
#18764=DIRECTION ( 'NONE',  ( -1.000000000000000000, -0.000000000000000000, 0.000000000000000000 ) ) ;
#18765=ORIENTED_EDGE ( 'NONE', *, *, #18159, .F. ) ;
#18769=EDGE_LOOP ( 'NONE', ( #16717, #9134, #3912, #8247 ) ) ;
#18772=CIRCLE ( 'NONE', #10545, 24.00000000002399858 ) ;
#18773=AXIS2_PLACEMENT_3D ( 'NONE', #10651, #10825, #15137 ) ;
#18774=ORIENTED_EDGE ( 'NONE', *, *, #13401, .T. ) ;
#18779=CYLINDRICAL_SURFACE ( 'NONE', #7922, 24.00000000002399503 ) ;
#18780=AXIS2_PLACEMENT_3D ( 'NONE', #13328, #16265, #361 ) ;
#18782=CARTESIAN_POINT ( 'NONE',  ( 10.00000000000000000, 18.38754094778241210, 53.29895248911682870 ) ) ;
#18785=ADVANCED_FACE ( 'NONE', ( #2884 ), #17372, .T. ) ;
#18788=EDGE_CURVE ( 'NONE', #9128, #18103, #1367, .T. ) ;
#18794=CIRCLE ( 'NONE', #6011, 24.00000000002399858 ) ;
#18797=EDGE_CURVE ( 'NONE', #12056, #4178, #8335, .T. ) ;
#18799=CARTESIAN_POINT ( 'NONE',  ( 0.000000000000000000, 0.000000000000000000, 0.000000000000000000 ) ) ;
#18804=AXIS2_PLACEMENT_3D ( 'NONE', #10884, #805, #16892 ) ;
#18807=AXIS2_PLACEMENT_3D ( 'NONE', #17810, #10576, #9147 ) ;
#18809=CARTESIAN_POINT ( 'NONE',  ( 10.00000000000000000, -44.70888270294186384, 34.13306034420170931 ) ) ;
#18863=COLOUR_RGB('Sky Blue',0.24,0.69,0.87);
#18864=FILL_AREA_STYLE_COLOUR('',#18863);
#18865=FILL_AREA_STYLE('',(#18864));
#18866=SURFACE_STYLE_FILL_AREA(#18865);
#18867=SURFACE_SIDE_STYLE('',(#18866));
#18868=SURFACE_STYLE_USAGE(.BOTH.,#18867);
#18869=PRESENTATION_STYLE_ASSIGNMENT((#18868));
ENDSEC;
END-ISO-10303-21;
